ISO-10303-21;
HEADER;
FILE_DESCRIPTION (('STEP AP214'),
    '1' );
FILE_NAME ('slotted set screw dog point_iso_ISO 7435 - M5 x 25-S.step',
    '2026-10-06T08:51:13',
    ( '' ),
    ( '' ),
    'SwSTEP 2.0',
    'SolidWorks 2021',
    '' );
FILE_SCHEMA (( 'AUTOMOTIVE_DESIGN' ));
ENDSEC;

DATA;
#22=AXIS2_PLACEMENT_3D ( 'NONE', #116807, #105905, #95043 ) ;
#57=AXIS2_PLACEMENT_3D ( 'NONE', #43785, #22010, #66260 ) ;
#102=DIRECTION ( 'NONE',  ( 1.201410254241279878E-16, -1.000000000000000000, 8.881784197001252323E-16 ) ) ;
#108=DIRECTION ( 'NONE',  ( -1.000000000000000000, -1.224606353822377258E-16, -0.000000000000000000 ) ) ;
#142=VECTOR ( 'NONE', #39114, 999.9999999999998863 ) ;
#170=ORIENTED_EDGE ( 'NONE', *, *, #86072, .F. ) ;
#204=FACE_OUTER_BOUND ( 'NONE', #73708, .T. ) ;
#221=AXIS2_PLACEMENT_3D ( 'NONE', #111679, #101498, #113810 ) ;
#259=DIRECTION ( 'NONE',  ( 0.000000000000000000, -1.000000000000000000, 0.000000000000000000 ) ) ;
#271=ADVANCED_FACE ( 'NONE', ( #128367 ), #102071, .T. ) ;
#273=AXIS2_PLACEMENT_3D ( 'NONE', #107756, #108445, #21491 ) ;
#300=DIRECTION ( 'NONE',  ( -1.000000000000000000, -1.224606353822377258E-16, -0.000000000000000000 ) ) ;
#316=EDGE_CURVE ( 'NONE', #33411, #102047, #58129, .T. ) ;
#335=CIRCLE ( 'NONE', #118423, 2.256103126841972895 ) ;
#357=DIRECTION ( 'NONE',  ( -1.000000000000000000, -1.224606353822377258E-16, -0.000000000000000000 ) ) ;
#379=EDGE_CURVE ( 'NONE', #60214, #42523, #120557, .T. ) ;
#438=LINE ( 'NONE', #139913, #105981 ) ;
#446=DIRECTION ( 'NONE',  ( 0.000000000000000000, 1.000000000000000000, 0.000000000000000000 ) ) ;
#464=DIRECTION ( 'NONE',  ( -1.000000000000000000, -1.224606353822377258E-16, -0.000000000000000000 ) ) ;
#473=ORIENTED_EDGE ( 'NONE', *, *, #137601, .F. ) ;
#487=CARTESIAN_POINT ( 'NONE',  ( -12.69999999999998153, -0.3999999999999997446, -2.467792535850613866 ) ) ;
#526=CARTESIAN_POINT ( 'NONE',  ( 13.92145407031093818, 4.584330080086930965E-16, 0.000000000000000000 ) ) ;
#551=DIRECTION ( 'NONE',  ( -0.5735764363510499342, -0.8191520442889891340, 0.000000000000000000 ) ) ;
#560=CARTESIAN_POINT ( 'NONE',  ( 1.516262732464673579, 3.821174125832445049E-16, 0.000000000000000000 ) ) ;
#570=CARTESIAN_POINT ( 'NONE',  ( -12.69999999999998153, 0.000000000000000000, 0.000000000000000000 ) ) ;
#591=CARTESIAN_POINT ( 'NONE',  ( 6.066782984417857350, 2.500000000000000444, 0.000000000000000000 ) ) ;
#646=AXIS2_PLACEMENT_3D ( 'NONE', #17941, #17261, #27404 ) ;
#648=ORIENTED_EDGE ( 'NONE', *, *, #75395, .F. ) ;
#697=CARTESIAN_POINT ( 'NONE',  ( 14.70692117890024697, 3.061616997868383634E-16, -2.500000000000000444 ) ) ;
#698=DIRECTION ( 'NONE',  ( 0.000000000000000000, 1.000000000000000000, 0.000000000000000000 ) ) ;
#704=CIRCLE ( 'NONE', #121067, 2.500000000000000444 ) ;
#730=DIRECTION ( 'NONE',  ( 0.000000000000000000, 1.000000000000000000, 0.000000000000000000 ) ) ;
#764=VERTEX_POINT ( 'NONE', #93687 ) ;
#777=VECTOR ( 'NONE', #141746, 1000.000000000000000 ) ;
#798=CARTESIAN_POINT ( 'NONE',  ( 16.44013779566152778, 4.333342374871280669E-31, 2.500000000000000444 ) ) ;
#824=DIRECTION ( 'NONE',  ( 0.000000000000000000, -1.000000000000000000, 0.000000000000000000 ) ) ;
#849=CARTESIAN_POINT ( 'NONE',  ( 6.540657738503846907, 4.202752102959690472E-16, 0.000000000000000000 ) ) ;
#860=FACE_OUTER_BOUND ( 'NONE', #101516, .T. ) ;
#863=EDGE_CURVE ( 'NONE', #97217, #125896, #73846, .T. ) ;
#918=ORIENTED_EDGE ( 'NONE', *, *, #46748, .T. ) ;
#938=DIRECTION ( 'NONE',  ( 1.000000000000000000, 1.224606353822377258E-16, 0.000000000000000000 ) ) ;
#966=CIRCLE ( 'NONE', #12566, 2.500000000000000444 ) ;
#1037=CARTESIAN_POINT ( 'NONE',  ( 7.014532492589830248, 3.821174125832445049E-16, 0.000000000000000000 ) ) ;
#1049=LINE ( 'NONE', #80102, #117244 ) ;
#1095=DIRECTION ( 'NONE',  ( 0.000000000000000000, 0.000000000000000000, 1.000000000000000000 ) ) ;
#1150=DIRECTION ( 'NONE',  ( -1.000000000000000000, -1.224606353822377258E-16, -0.000000000000000000 ) ) ;
#1152=CARTESIAN_POINT ( 'NONE',  ( 18.63425672184678916, 2.500000000000000888, 0.000000000000000000 ) ) ;
#1184=ORIENTED_EDGE ( 'NONE', *, *, #18214, .F. ) ;
#1214=DIRECTION ( 'NONE',  ( -1.000000000000000000, -0.000000000000000000, -0.000000000000000000 ) ) ;
#1227=DIRECTION ( 'NONE',  ( 1.000000000000000000, 1.224606353822377258E-16, 0.000000000000000000 ) ) ;
#1236=CARTESIAN_POINT ( 'NONE',  ( 17.06332250466817158, 4.584330080086930965E-16, 0.000000000000000000 ) ) ;
#1253=DIRECTION ( 'NONE',  ( -1.000000000000000000, -0.000000000000000000, -0.000000000000000000 ) ) ;
#1282=ORIENTED_EDGE ( 'NONE', *, *, #97105, .T. ) ;
#1294=VERTEX_POINT ( 'NONE', #23239 ) ;
#1308=ORIENTED_EDGE ( 'NONE', *, *, #103071, .F. ) ;
#1335=CARTESIAN_POINT ( 'NONE',  ( -12.69999999999998153, 0.000000000000000000, 0.000000000000000000 ) ) ;
#1352=ORIENTED_EDGE ( 'NONE', *, *, #9974, .T. ) ;
#1364=ORIENTED_EDGE ( 'NONE', *, *, #130588, .F. ) ;
#1373=CARTESIAN_POINT ( 'NONE',  ( 14.08373646989360317, 3.821174125832445049E-16, 0.000000000000000000 ) ) ;
#1381=DIRECTION ( 'NONE',  ( -1.000000000000000000, -1.224606353822377258E-16, -0.000000000000000000 ) ) ;
#1390=CARTESIAN_POINT ( 'NONE',  ( 13.60986171580761805, 2.055000000000001048, 0.000000000000000000 ) ) ;
#1415=ORIENTED_EDGE ( 'NONE', *, *, #40573, .F. ) ;
#1449=DIRECTION ( 'NONE',  ( 0.000000000000000000, -1.000000000000000000, 0.000000000000000000 ) ) ;
#1486=DIRECTION ( 'NONE',  ( -0.5735764363510501562, 0.8191520442889890230, 1.003171929053521419E-16 ) ) ;
#1524=CARTESIAN_POINT ( 'NONE',  ( 0.2569208697893812232, 0.4000000000000001332, -2.015694669338588429 ) ) ;
#1542=ORIENTED_EDGE ( 'NONE', *, *, #29424, .T. ) ;
#1602=DIRECTION ( 'NONE',  ( 0.000000000000000000, 0.000000000000000000, 1.000000000000000000 ) ) ;
#1641=VECTOR ( 'NONE', #73871, 1000.000000000000000 ) ;
#1644=ORIENTED_EDGE ( 'NONE', *, *, #29808, .T. ) ;
#1668=CARTESIAN_POINT ( 'NONE',  ( 17.53719725875415847, -2.055000000000000160, 2.789133085058097101E-16 ) ) ;
#1671=DIRECTION ( 'NONE',  ( 0.5735764363510448272, -0.8191520442889927978, 1.003171929053526103E-16 ) ) ;
#1692=ORIENTED_EDGE ( 'NONE', *, *, #17914, .F. ) ;
#1721=CYLINDRICAL_SURFACE ( 'NONE', #111874, 2.500000000000000444 ) ;
#1751=ORIENTED_EDGE ( 'NONE', *, *, #15487, .T. ) ;
#1769=VECTOR ( 'NONE', #10352, 999.9999999999998863 ) ;
#1859=VERTEX_POINT ( 'NONE', #40419 ) ;
#1885=VERTEX_POINT ( 'NONE', #137576 ) ;
#1917=ORIENTED_EDGE ( 'NONE', *, *, #129818, .F. ) ;
#1923=FACE_OUTER_BOUND ( 'NONE', #35629, .T. ) ;
#1956=DIRECTION ( 'NONE',  ( 1.000000000000000000, 1.224606353822377258E-16, 0.000000000000000000 ) ) ;
#1959=ORIENTED_EDGE ( 'NONE', *, *, #8760, .F. ) ;
#1999=CIRCLE ( 'NONE', #120081, 2.500000000000000444 ) ;
#2014=ORIENTED_EDGE ( 'NONE', *, *, #119442, .T. ) ;
#2030=DIRECTION ( 'NONE',  ( -1.000000000000000000, -0.000000000000000000, -0.000000000000000000 ) ) ;
#2049=DIRECTION ( 'NONE',  ( -1.000000000000000000, -0.000000000000000000, -0.000000000000000000 ) ) ;
#2082=CIRCLE ( 'NONE', #101676, 2.337593264352433753 ) ;
#2122=AXIS2_PLACEMENT_3D ( 'NONE', #122165, #33778, #1095 ) ;
#2141=DIRECTION ( 'NONE',  ( 0.000000000000000000, -1.000000000000000000, 0.000000000000000000 ) ) ;
#2148=CONICAL_SURFACE ( 'NONE', #101736, 2.055000000000000604, 0.9599310885968764806 ) ;
#2196=ORIENTED_EDGE ( 'NONE', *, *, #93811, .F. ) ;
#2202=EDGE_CURVE ( 'NONE', #73650, #141344, #10329, .T. ) ;
#2295=AXIS2_PLACEMENT_3D ( 'NONE', #9383, #118893, #30472 ) ;
#2312=DIRECTION ( 'NONE',  ( -1.000000000000000000, -1.224606353822377258E-16, -0.000000000000000000 ) ) ;
#2317=ORIENTED_EDGE ( 'NONE', *, *, #64119, .F. ) ;
#2344=LINE ( 'NONE', #89388, #121115 ) ;
#2371=DIRECTION ( 'NONE',  ( -1.000000000000000000, -1.224606353822377258E-16, -0.000000000000000000 ) ) ;
#2436=AXIS2_PLACEMENT_3D ( 'NONE', #34265, #48017, #79241 ) ;
#2454=ADVANCED_FACE ( 'NONE', ( #123170 ), #106896, .T. ) ;
#2459=VERTEX_POINT ( 'NONE', #26691 ) ;
#2478=VERTEX_POINT ( 'NONE', #34723 ) ;
#2489=ORIENTED_EDGE ( 'NONE', *, *, #103276, .T. ) ;
#2499=CONICAL_SURFACE ( 'NONE', #21043, 2.500000000000000444, 0.9599310885968830309 ) ;
#2504=AXIS2_PLACEMENT_3D ( 'NONE', #42971, #19052, #8827 ) ;
#2535=ORIENTED_EDGE ( 'NONE', *, *, #137252, .T. ) ;
#2543=CIRCLE ( 'NONE', #78972, 2.500000000000000444 ) ;
#2557=ORIENTED_EDGE ( 'NONE', *, *, #30106, .F. ) ;
#2582=ADVANCED_FACE ( 'NONE', ( #48442 ), #132418, .T. ) ;
#2585=FACE_OUTER_BOUND ( 'NONE', #26863, .T. ) ;
#2627=( NAMED_UNIT ( * ) PLANE_ANGLE_UNIT ( ) SI_UNIT ( $, .RADIAN. ) );
#2646=CARTESIAN_POINT ( 'NONE',  ( 14.39532882439692862, 4.202752102959690472E-16, 0.000000000000000000 ) ) ;
#2719=DIRECTION ( 'NONE',  ( 0.000000000000000000, -1.000000000000000000, 0.000000000000000000 ) ) ;
#2726=CIRCLE ( 'NONE', #21261, 2.500000000000000444 ) ;
#2783=DIRECTION ( 'NONE',  ( 0.000000000000000000, 1.000000000000000000, 0.000000000000000000 ) ) ;
#2785=CARTESIAN_POINT ( 'NONE',  ( 14.70692117890024697, 4.584330080086930965E-16, 0.000000000000000000 ) ) ;
#2837=ORIENTED_EDGE ( 'NONE', *, *, #60531, .F. ) ;
#2850=DIRECTION ( 'NONE',  ( -0.5735764363510499342, -0.8191520442889891340, 0.000000000000000000 ) ) ;
#2853=CARTESIAN_POINT ( 'NONE',  ( 13.92145407031093818, 4.584330080086930965E-16, 0.000000000000000000 ) ) ;
#2857=EDGE_LOOP ( 'NONE', ( #25330, #20229, #67010, #104199, #27651 ) ) ;
#2868=VECTOR ( 'NONE', #133428, 1000.000000000000000 ) ;
#2870=ORIENTED_EDGE ( 'NONE', *, *, #102075, .F. ) ;
#2891=EDGE_CURVE ( 'NONE', #22488, #17542, #102172, .T. ) ;
#2955=DIRECTION ( 'NONE',  ( 1.055184596092948005E-16, -1.000000000000000000, 0.000000000000000000 ) ) ;
#2962=ORIENTED_EDGE ( 'NONE', *, *, #137949, .T. ) ;
#2977=EDGE_CURVE ( 'NONE', #47310, #141344, #83707, .T. ) ;
#3019=CARTESIAN_POINT ( 'NONE',  ( 22.25000000000000000, 2.143131898507868051E-16, -1.749999999999999778 ) ) ;
#3047=CIRCLE ( 'NONE', #37746, 2.055000000000000604 ) ;
#3145=ORIENTED_EDGE ( 'NONE', *, *, #127067, .F. ) ;
#3180=DIRECTION ( 'NONE',  ( -1.000000000000000000, -0.000000000000000000, -0.000000000000000000 ) ) ;
#3182=CARTESIAN_POINT ( 'NONE',  ( -12.69999999999998153, 0.000000000000000000, 0.000000000000000000 ) ) ;
#3202=AXIS2_PLACEMENT_3D ( 'NONE', #95350, #15606, #27230 ) ;
#3203=FACE_OUTER_BOUND ( 'NONE', #60981, .T. ) ;
#3222=DIRECTION ( 'NONE',  ( 1.000000000000000000, 1.224606353822377258E-16, 0.000000000000000000 ) ) ;
#3239=DIRECTION ( 'NONE',  ( 0.000000000000000000, -1.000000000000000000, 0.000000000000000000 ) ) ;
#3241=CARTESIAN_POINT ( 'NONE',  ( 15.65467068707222076, 3.821174125832445049E-16, 0.000000000000000000 ) ) ;
#3245=FACE_OUTER_BOUND ( 'NONE', #85822, .T. ) ;
#3250=EDGE_CURVE ( 'NONE', #59344, #57263, #10207, .T. ) ;
#3256=LINE ( 'NONE', #11260, #31794 ) ;
#3257=CARTESIAN_POINT ( 'NONE',  ( 8.897059064271770623, 2.055000000000001048, 2.516649172247811554E-16 ) ) ;
#3259=VERTEX_POINT ( 'NONE', #36434 ) ;
#3342=DIRECTION ( 'NONE',  ( 0.5735764363510444941, 0.8191520442889929088, 0.000000000000000000 ) ) ;
#3385=DIRECTION ( 'NONE',  ( -1.000000000000000000, -0.000000000000000000, -0.000000000000000000 ) ) ;
#3386=FACE_OUTER_BOUND ( 'NONE', #133859, .T. ) ;
#3396=CARTESIAN_POINT ( 'NONE',  ( 17.84878961325748037, 0.000000000000000000, 2.500000000000000444 ) ) ;
#3398=EDGE_CURVE ( 'NONE', #23744, #75950, #70501, .T. ) ;
#3401=EDGE_LOOP ( 'NONE', ( #15786, #93571, #6767, #130445, #60464 ) ) ;
#3426=CONICAL_SURFACE ( 'NONE', #107545, 2.500000000000000444, 0.9599310885968830309 ) ;
#3431=CARTESIAN_POINT ( 'NONE',  ( 21.66240673564756491, 0.000000000000000000, 2.337593264352432421 ) ) ;
#3433=DIRECTION ( 'NONE',  ( -1.000000000000000000, -0.000000000000000000, -0.000000000000000000 ) ) ;
#3434=ORIENTED_EDGE ( 'NONE', *, *, #32196, .T. ) ;
#3438=DIRECTION ( 'NONE',  ( 1.734723475976806848E-16, -1.000000000000000000, 0.000000000000000000 ) ) ;
#3448=CARTESIAN_POINT ( 'NONE',  ( 15.96626304157554266, -2.055000000000000160, 0.000000000000000000 ) ) ;
#3481=DIRECTION ( 'NONE',  ( 2.110369192185896011E-16, -1.000000000000000000, 0.000000000000000000 ) ) ;
#3486=ORIENTED_EDGE ( 'NONE', *, *, #135795, .F. ) ;
#3491=DIRECTION ( 'NONE',  ( -1.000000000000000000, -1.224606353822377258E-16, -0.000000000000000000 ) ) ;
#3495=ORIENTED_EDGE ( 'NONE', *, *, #11216, .F. ) ;
#3532=LINE ( 'NONE', #60114, #123960 ) ;
#3623=ORIENTED_EDGE ( 'NONE', *, *, #98383, .F. ) ;
#3657=DIRECTION ( 'NONE',  ( 1.318980745116185161E-16, -1.000000000000000000, 0.000000000000000000 ) ) ;
#3697=EDGE_LOOP ( 'NONE', ( #121818, #10630, #4080, #97755, #67196 ) ) ;
#3703=AXIS2_PLACEMENT_3D ( 'NONE', #62105, #118597, #52623 ) ;
#3716=CIRCLE ( 'NONE', #101022, 2.500000000000000444 ) ;
#3854=CARTESIAN_POINT ( 'NONE',  ( 2.924914550060624840, 2.500000000000000888, 0.000000000000000000 ) ) ;
#4013=EDGE_CURVE ( 'NONE', #140226, #13056, #3047, .T. ) ;
#4045=DIRECTION ( 'NONE',  ( -1.000000000000000000, -1.224606353822377258E-16, -0.000000000000000000 ) ) ;
#4074=DIRECTION ( 'NONE',  ( -1.000000000000000000, -1.224606353822377258E-16, -0.000000000000000000 ) ) ;
#4080=ORIENTED_EDGE ( 'NONE', *, *, #128523, .T. ) ;
#4101=DIRECTION ( 'NONE',  ( -0.5735764363510501562, 0.8191520442889890230, 1.003171929053521419E-16 ) ) ;
#4117=DIRECTION ( 'NONE',  ( -0.5735764363510499342, -0.8191520442889891340, 0.000000000000000000 ) ) ;
#4137=ORIENTED_EDGE ( 'NONE', *, *, #54109, .T. ) ;
#4164=CARTESIAN_POINT ( 'NONE',  ( 21.15294044719737698, 3.821174125832445049E-16, 0.000000000000000000 ) ) ;
#4179=EDGE_LOOP ( 'NONE', ( #14215, #46831, #63893, #116608 ) ) ;
#4186=CARTESIAN_POINT ( 'NONE',  ( 10.15640092694706453, 2.500000000000000444, 3.061616997868383634E-16 ) ) ;
#4196=ORIENTED_EDGE ( 'NONE', *, *, #34004, .T. ) ;
#4318=AXIS2_PLACEMENT_3D ( 'NONE', #118898, #85544, #74719 ) ;
#4331=CIRCLE ( 'NONE', #13596, 2.500000000000000444 ) ;
#4339=CARTESIAN_POINT ( 'NONE',  ( 13.13598696172163116, 4.584330080086930965E-16, 0.000000000000000000 ) ) ;
#4369=VECTOR ( 'NONE', #85219, 1000.000000000000000 ) ;
#4390=CARTESIAN_POINT ( 'NONE',  ( 17.06332250466817158, 2.500000000000000888, 0.000000000000000000 ) ) ;
#4391=EDGE_CURVE ( 'NONE', #140149, #25103, #11878, .T. ) ;
#4426=FACE_OUTER_BOUND ( 'NONE', #3697, .T. ) ;
#4445=EDGE_CURVE ( 'NONE', #10019, #47408, #54978, .T. ) ;
#4517=DIRECTION ( 'NONE',  ( -0.7071067811865477948, 8.659560562354931626E-17, -0.7071067811865473507 ) ) ;
#4526=ORIENTED_EDGE ( 'NONE', *, *, #316, .F. ) ;
#4582=CONICAL_SURFACE ( 'NONE', #104167, 2.055000000000000604, 0.9599310885968764806 ) ;
#4667=DIRECTION ( 'NONE',  ( -1.000000000000000000, -1.224606353822377258E-16, -0.000000000000000000 ) ) ;
#4677=CARTESIAN_POINT ( 'NONE',  ( -12.69999999999998153, 0.000000000000000000, 0.000000000000000000 ) ) ;
#4717=AXIS2_PLACEMENT_3D ( 'NONE', #4339, #49385, #36341 ) ;
#4725=AXIS2_PLACEMENT_3D ( 'NONE', #121034, #54395, #45659 ) ;
#4747=ADVANCED_FACE ( 'NONE', ( #58474 ), #126748, .T. ) ;
#4753=CIRCLE ( 'NONE', #108884, 2.500000000000000444 ) ;
#4781=CIRCLE ( 'NONE', #136774, 2.500000000000000444 ) ;
#4798=AXIS2_PLACEMENT_3D ( 'NONE', #29231, #93785, #7459 ) ;
#4811=CONICAL_SURFACE ( 'NONE', #28055, 2.055000000000000604, 0.9599310885968764806 ) ;
#4841=EDGE_CURVE ( 'NONE', #122222, #29201, #103660, .T. ) ;
#4904=DIRECTION ( 'NONE',  ( -1.000000000000000000, -1.224606353822377258E-16, -0.000000000000000000 ) ) ;
#4926=EDGE_CURVE ( 'NONE', #76525, #1885, #142929, .T. ) ;
#4945=ORIENTED_EDGE ( 'NONE', *, *, #20200, .T. ) ;
#4982=LINE ( 'NONE', #83315, #44758 ) ;
#5065=CONICAL_SURFACE ( 'NONE', #104651, 2.055000000000000604, 0.9599310885968764806 ) ;
#5078=CIRCLE ( 'NONE', #116157, 2.500000000000000444 ) ;
#5092=VERTEX_POINT ( 'NONE', #16686 ) ;
#5114=AXIS2_PLACEMENT_3D ( 'NONE', #44288, #78329, #2141 ) ;
#5130=EDGE_CURVE ( 'NONE', #764, #19509, #55072, .T. ) ;
#5157=CARTESIAN_POINT ( 'NONE',  ( 4.658131166821905644, 2.500000000000001776, 3.061616997868385113E-16 ) ) ;
#5194=VERTEX_POINT ( 'NONE', #94947 ) ;
#5206=EDGE_CURVE ( 'NONE', #1885, #45596, #78255, .T. ) ;
#5228=ORIENTED_EDGE ( 'NONE', *, *, #117649, .T. ) ;
#5281=EDGE_CURVE ( 'NONE', #29556, #93024, #122416, .T. ) ;
#5327=VECTOR ( 'NONE', #90535, 999.9999999999998863 ) ;
#5332=CIRCLE ( 'NONE', #114116, 2.500000000000000444 ) ;
#5371=EDGE_CURVE ( 'NONE', #40384, #19769, #74495, .T. ) ;
#5382=ORIENTED_EDGE ( 'NONE', *, *, #78695, .T. ) ;
#5396=CONICAL_SURFACE ( 'NONE', #100322, 2.055000000000000604, 0.9599310885968764806 ) ;
#5404=CARTESIAN_POINT ( 'NONE',  ( 14.70692117890024697, 0.000000000000000000, 2.500000000000000444 ) ) ;
#5464=EDGE_CURVE ( 'NONE', #63294, #58140, #24845, .T. ) ;
#5479=CARTESIAN_POINT ( 'NONE',  ( 5.755190629914537226, -2.055000000000000160, 0.000000000000000000 ) ) ;
#5487=CARTESIAN_POINT ( 'NONE',  ( 4.184256412735922304, 4.202752102959690472E-16, 0.000000000000000000 ) ) ;
#5490=DIRECTION ( 'NONE',  ( -0.000000000000000000, 0.000000000000000000, -1.000000000000000000 ) ) ;
#5537=EDGE_CURVE ( 'NONE', #136698, #137282, #11680, .T. ) ;
#5548=DIRECTION ( 'NONE',  ( -1.000000000000000000, -1.224606353822377258E-16, -0.000000000000000000 ) ) ;
#5573=CARTESIAN_POINT ( 'NONE',  ( -12.69999999999998153, 0.000000000000000000, 2.500000000000000444 ) ) ;
#5620=AXIS2_PLACEMENT_3D ( 'NONE', #24962, #16210, #114131 ) ;
#5635=LINE ( 'NONE', #49909, #38624 ) ;
#5646=CARTESIAN_POINT ( 'NONE',  ( 19.58200623001875940, 3.061616997868383634E-16, -2.500000000000000444 ) ) ;
#5663=DIRECTION ( 'NONE',  ( -1.000000000000000000, -1.224606353822377258E-16, -0.000000000000000000 ) ) ;
#5667=ORIENTED_EDGE ( 'NONE', *, *, #102531, .F. ) ;
#5670=EDGE_LOOP ( 'NONE', ( #52680, #134963, #33535, #24789, #7325 ) ) ;
#5690=DIRECTION ( 'NONE',  ( 8.673617379884034239E-17, -1.000000000000000000, 0.000000000000000000 ) ) ;
#5701=VERTEX_POINT ( 'NONE', #49380 ) ;
#5704=CARTESIAN_POINT ( 'NONE',  ( 3.087196949643290278, -2.500000000000000444, 0.000000000000000000 ) ) ;
#5719=EDGE_CURVE ( 'NONE', #19509, #127065, #137072, .T. ) ;
#5755=ORIENTED_EDGE ( 'NONE', *, *, #86999, .T. ) ;
#5758=EDGE_LOOP ( 'NONE', ( #106567, #106554, #117757, #33928, #96740 ) ) ;
#5761=DIRECTION ( 'NONE',  ( -1.000000000000000000, -1.224606353822377258E-16, -0.000000000000000000 ) ) ;
#5767=DIRECTION ( 'NONE',  ( -1.000000000000000000, -1.224606353822377258E-16, -0.000000000000000000 ) ) ;
#5907=ORIENTED_EDGE ( 'NONE', *, *, #75688, .T. ) ;
#5935=CARTESIAN_POINT ( 'NONE',  ( 0.2569208697893814453, 4.202752102959690472E-16, 0.000000000000000000 ) ) ;
#5944=CIRCLE ( 'NONE', #114720, 2.055000000000000604 ) ;
#5952=CONICAL_SURFACE ( 'NONE', #10620, 2.055000000000000604, 0.9599310885968764806 ) ;
#5969=FACE_OUTER_BOUND ( 'NONE', #49967, .T. ) ;
#5972=EDGE_LOOP ( 'NONE', ( #131728, #84926, #48273, #75427, #99710 ) ) ;
#5981=CARTESIAN_POINT ( 'NONE',  ( 2.924914550060625285, 4.584330080086930965E-16, 0.000000000000000000 ) ) ;
#5990=DIRECTION ( 'NONE',  ( -1.000000000000000000, -0.000000000000000000, -0.000000000000000000 ) ) ;
#5998=DIRECTION ( 'NONE',  ( -0.5735764363510501562, 0.8191520442889890230, 1.003171929053521419E-16 ) ) ;
#6001=EDGE_CURVE ( 'NONE', #75950, #130884, #33651, .T. ) ;
#6007=CARTESIAN_POINT ( 'NONE',  ( 6.229065384000522343, 3.061616997868383634E-16, -2.500000000000000444 ) ) ;
#6137=EDGE_CURVE ( 'NONE', #10551, #40384, #70840, .T. ) ;
#6139=AXIS2_PLACEMENT_3D ( 'NONE', #95089, #106667, #108796 ) ;
#6144=ORIENTED_EDGE ( 'NONE', *, *, #86457, .T. ) ;
#6215=ORIENTED_EDGE ( 'NONE', *, *, #86557, .T. ) ;
#6236=FACE_OUTER_BOUND ( 'NONE', #5972, .T. ) ;
#6284=CARTESIAN_POINT ( 'NONE',  ( 20.67906569311139009, 2.055000000000001048, 0.000000000000000000 ) ) ;
#6318=EDGE_CURVE ( 'NONE', #130467, #69156, #43095, .T. ) ;
#6322=DIRECTION ( 'NONE',  ( 0.000000000000000000, -1.000000000000000000, 0.000000000000000000 ) ) ;
#6330=CIRCLE ( 'NONE', #119775, 2.500000000000000444 ) ;
#6345=CARTESIAN_POINT ( 'NONE',  ( 0.2569208697893813342, -0.4000000000000003553, 2.015694669338588429 ) ) ;
#6454=DIRECTION ( 'NONE',  ( -1.000000000000000000, -1.224606353822377258E-16, -0.000000000000000000 ) ) ;
#6462=CARTESIAN_POINT ( 'NONE',  ( 0.8348607551137282590, -0.4000000000000004108, 2.317232462839659224 ) ) ;
#6525=CARTESIAN_POINT ( 'NONE',  ( 17.06332250466817158, 4.584330080086930965E-16, 0.000000000000000000 ) ) ;
#6532=EDGE_CURVE ( 'NONE', #97836, #130434, #135579, .T. ) ;
#6534=CARTESIAN_POINT ( 'NONE',  ( 17.53719725875415847, 2.055000000000001048, 2.516649172247811554E-16 ) ) ;
#6571=DIRECTION ( 'NONE',  ( -1.000000000000000000, -1.224606353822377258E-16, -0.000000000000000000 ) ) ;
#6580=AXIS2_PLACEMENT_3D ( 'NONE', #96258, #27446, #5690 ) ;
#6587=ORIENTED_EDGE ( 'NONE', *, *, #69438, .F. ) ;
#6606=ORIENTED_EDGE ( 'NONE', *, *, #112550, .F. ) ;
#6756=AXIS2_PLACEMENT_3D ( 'NONE', #69386, #4045, #26578 ) ;
#6767=ORIENTED_EDGE ( 'NONE', *, *, #58442, .T. ) ;
#6770=AXIS2_PLACEMENT_3D ( 'NONE', #82820, #103124, #139358 ) ;
#6771=AXIS2_PLACEMENT_3D ( 'NONE', #84893, #28387, #8022 ) ;
#6775=LINE ( 'NONE', #61265, #88050 ) ;
#6837=AXIS2_PLACEMENT_3D ( 'NONE', #108678, #17419, #94966 ) ;
#6877=AXIS2_PLACEMENT_3D ( 'NONE', #99312, #63878, #140689 ) ;
#6911=DIRECTION ( 'NONE',  ( -1.000000000000000000, -1.224606353822377258E-16, -0.000000000000000000 ) ) ;
#6917=EDGE_CURVE ( 'NONE', #82553, #40629, #91577, .T. ) ;
#6945=CONICAL_SURFACE ( 'NONE', #34855, 2.500000000000000444, 0.9599310885968830309 ) ;
#6950=CARTESIAN_POINT ( 'NONE',  ( 17.22560490425083657, 3.821174125832445049E-16, 0.000000000000000000 ) ) ;
#6969=ORIENTED_EDGE ( 'NONE', *, *, #108372, .T. ) ;
#6975=CIRCLE ( 'NONE', #6877, 2.500000000000000444 ) ;
#6996=AXIS2_PLACEMENT_3D ( 'NONE', #132727, #45014, #66720 ) ;
#7004=VECTOR ( 'NONE', #110129, 1000.000000000000000 ) ;
#7072=CARTESIAN_POINT ( 'NONE',  ( 20.99065804761471199, 3.061616997868383634E-16, -2.500000000000000444 ) ) ;
#7083=ORIENTED_EDGE ( 'NONE', *, *, #132071, .F. ) ;
#7084=EDGE_CURVE ( 'NONE', #141344, #142044, #54643, .T. ) ;
#7107=VERTEX_POINT ( 'NONE', #119511 ) ;
#7114=CARTESIAN_POINT ( 'NONE',  ( 3.398789304146613510, 2.055000000000001048, 2.516649172247811554E-16 ) ) ;
#7178=DIRECTION ( 'NONE',  ( 0.000000000000000000, -1.000000000000000000, 0.000000000000000000 ) ) ;
#7210=CIRCLE ( 'NONE', #92939, 2.055000000000000604 ) ;
#7243=VERTEX_POINT ( 'NONE', #86220 ) ;
#7245=LINE ( 'NONE', #42792, #31142 ) ;
#7325=ORIENTED_EDGE ( 'NONE', *, *, #97452, .F. ) ;
#7343=ORIENTED_EDGE ( 'NONE', *, *, #88408, .T. ) ;
#7357=CIRCLE ( 'NONE', #102294, 2.500000000000000444 ) ;
#7392=LINE ( 'NONE', #105984, #12548 ) ;
#7411=ORIENTED_EDGE ( 'NONE', *, *, #135225, .T. ) ;
#7415=DIRECTION ( 'NONE',  ( 0.000000000000000000, 1.000000000000000000, 0.000000000000000000 ) ) ;
#7433=CARTESIAN_POINT ( 'NONE',  ( 0.1161069444170876597, 0.000000000000000000, 0.000000000000000000 ) ) ;
#7459=DIRECTION ( 'NONE',  ( 0.000000000000000000, 1.000000000000000000, 0.000000000000000000 ) ) ;
#7476=EDGE_LOOP ( 'NONE', ( #45369, #64873, #133284, #73093, #26038 ) ) ;
#7480=MECHANICAL_DESIGN_GEOMETRIC_PRESENTATION_REPRESENTATION('',(#7580),#65486);
#7489=ORIENTED_EDGE ( 'NONE', *, *, #8888, .T. ) ;
#7491=DIRECTION ( 'NONE',  ( -1.000000000000000000, -1.224606353822377258E-16, -0.000000000000000000 ) ) ;
#7499=ORIENTED_EDGE ( 'NONE', *, *, #35203, .T. ) ;
#7558=CARTESIAN_POINT ( 'NONE',  ( 10.94186803553636977, -2.500000000000001776, 0.000000000000000000 ) ) ;
#7566=CARTESIAN_POINT ( 'NONE',  ( 20.36747333860806819, 3.821174125832445049E-16, 0.000000000000000000 ) ) ;
#7580=STYLED_ITEM ( 'NONE', ( #91899 ), #15274 ) ;
#7626=VERTEX_POINT ( 'NONE', #112781 ) ;
#7633=ORIENTED_EDGE ( 'NONE', *, *, #11134, .T. ) ;
#7659=ADVANCED_FACE ( 'NONE', ( #89599 ), #137426, .T. ) ;
#7697=CARTESIAN_POINT ( 'NONE',  ( 15.96626304157554266, 4.202752102959690472E-16, 0.000000000000000000 ) ) ;
#7704=AXIS2_PLACEMENT_3D ( 'NONE', #139289, #97135, #138553 ) ;
#7707=DIRECTION ( 'NONE',  ( -1.000000000000000000, -0.000000000000000000, -0.000000000000000000 ) ) ;
#7711=CARTESIAN_POINT ( 'NONE',  ( -12.69999999999998153, 0.000000000000000000, 2.500000000000000444 ) ) ;
#7777=CARTESIAN_POINT ( 'NONE',  ( 0.7307956238753654521, 0.4000000000000001887, -2.467792535850613866 ) ) ;
#7818=AXIS2_PLACEMENT_3D ( 'NONE', #93770, #106765, #116234 ) ;
#7849=ORIENTED_EDGE ( 'NONE', *, *, #10496, .T. ) ;
#7874=ORIENTED_EDGE ( 'NONE', *, *, #129606, .F. ) ;
#7994=ORIENTED_EDGE ( 'NONE', *, *, #122358, .T. ) ;
#8017=VERTEX_POINT ( 'NONE', #130830 ) ;
#8022=DIRECTION ( 'NONE',  ( 0.000000000000000000, -1.000000000000000000, 0.000000000000000000 ) ) ;
#8058=FACE_OUTER_BOUND ( 'NONE', #120417, .T. ) ;
#8072=EDGE_LOOP ( 'NONE', ( #74486, #117067, #47553, #62042, #86616, #35873, #19633, #1364, #55333, #142617, #117900, #89041, #96499, #38836, #66152, #122881, #87505, #81982 ) ) ;
#8077=CARTESIAN_POINT ( 'NONE',  ( 2.301729841053981485, 3.061616997868383141E-16, -2.500000000000000444 ) ) ;
#8133=CIRCLE ( 'NONE', #40574, 2.337593264352433753 ) ;
#8134=DIRECTION ( 'NONE',  ( -1.000000000000000000, -0.000000000000000000, -0.000000000000000000 ) ) ;
#8159=DIRECTION ( 'NONE',  ( 0.000000000000000000, 1.000000000000000000, 0.000000000000000000 ) ) ;
#8197=ORIENTED_EDGE ( 'NONE', *, *, #117320, .T. ) ;
#8206=EDGE_CURVE ( 'NONE', #141465, #124724, #80725, .T. ) ;
#8229=AXIS2_PLACEMENT_3D ( 'NONE', #70448, #35668, #79893 ) ;
#8232=LINE ( 'NONE', #120561, #97284 ) ;
#8259=ORIENTED_EDGE ( 'NONE', *, *, #23507, .F. ) ;
#8329=EDGE_CURVE ( 'NONE', #66627, #118938, #81985, .T. ) ;
#8358=CARTESIAN_POINT ( 'NONE',  ( 16.75173015016484968, 4.202752102959690472E-16, 0.000000000000000000 ) ) ;
#8379=CARTESIAN_POINT ( 'NONE',  ( 13.29826936130429260, 2.500000000000003109, 3.061616997868386592E-16 ) ) ;
#8459=LINE ( 'NONE', #128850, #137307 ) ;
#8513=AXIS2_PLACEMENT_3D ( 'NONE', #17703, #136642, #103293 ) ;
#8573=DIRECTION ( 'NONE',  ( -1.000000000000000000, -0.000000000000000000, -0.000000000000000000 ) ) ;
#8583=ADVANCED_FACE ( 'NONE', ( #126014 ), #26684, .T. ) ;
#8596=DIRECTION ( 'NONE',  ( 0.000000000000000000, -1.000000000000000000, 0.000000000000000000 ) ) ;
#8622=AXIS2_PLACEMENT_3D ( 'NONE', #41792, #84591, #73700 ) ;
#8639=EDGE_CURVE ( 'NONE', #139082, #39184, #60788, .T. ) ;
#8681=AXIS2_PLACEMENT_3D ( 'NONE', #135288, #123696, #134567 ) ;
#8760=EDGE_CURVE ( 'NONE', #76190, #106463, #33455, .T. ) ;
#8776=VERTEX_POINT ( 'NONE', #27581 ) ;
#8799=LINE ( 'NONE', #74124, #88338 ) ;
#8827=DIRECTION ( 'NONE',  ( 1.734723475976806848E-16, -1.000000000000000000, 0.000000000000000000 ) ) ;
#8838=ORIENTED_EDGE ( 'NONE', *, *, #133355, .F. ) ;
#8888=EDGE_CURVE ( 'NONE', #99466, #40629, #137807, .T. ) ;
#8896=AXIS2_PLACEMENT_3D ( 'NONE', #129697, #86222, #96329 ) ;
#8899=AXIS2_PLACEMENT_3D ( 'NONE', #109558, #142903, #74827 ) ;
#8901=DIRECTION ( 'NONE',  ( -1.000000000000000000, -0.000000000000000000, -0.000000000000000000 ) ) ;
#8905=CARTESIAN_POINT ( 'NONE',  ( 20.67906569311139009, 4.202752102959690472E-16, 0.000000000000000000 ) ) ;
#8925=CARTESIAN_POINT ( 'NONE',  ( 0.000000000000000000, 0.000000000000000000, 0.000000000000000000 ) ) ;
#8929=CIRCLE ( 'NONE', #41372, 2.500000000000000444 ) ;
#9001=CARTESIAN_POINT ( 'NONE',  ( 20.20519093902540320, 4.584330080086930965E-16, 0.000000000000000000 ) ) ;
#9004=VECTOR ( 'NONE', #1486, 999.9999999999998863 ) ;
#9030=CARTESIAN_POINT ( 'NONE',  ( 7.014532492589830248, 0.000000000000000000, 2.500000000000000444 ) ) ;
#9048=ORIENTED_EDGE ( 'NONE', *, *, #139614, .T. ) ;
#9054=EDGE_LOOP ( 'NONE', ( #51162, #97972, #36292, #37376, #99045 ) ) ;
#9094=ORIENTED_EDGE ( 'NONE', *, *, #35669, .F. ) ;
#9104=CARTESIAN_POINT ( 'NONE',  ( 7.799999601179139042, 3.821174125832445049E-16, 0.000000000000000000 ) ) ;
#9105=EDGE_CURVE ( 'NONE', #83522, #122249, #65640, .T. ) ;
#9120=CIRCLE ( 'NONE', #106309, 2.055000000000000604 ) ;
#9149=CARTESIAN_POINT ( 'NONE',  ( 2.613322195557305605, 4.202752102959690472E-16, 0.000000000000000000 ) ) ;
#9285=DIRECTION ( 'NONE',  ( -1.000000000000000000, -1.224606353822377258E-16, -0.000000000000000000 ) ) ;
#9383=CARTESIAN_POINT ( 'NONE',  ( 9.208651418775088970, 4.584330080086930965E-16, 0.000000000000000000 ) ) ;
#9387=EDGE_CURVE ( 'NONE', #19769, #131428, #86651, .T. ) ;
#9402=AXIS2_PLACEMENT_3D ( 'NONE', #21941, #110359, #55310 ) ;
#9429=EDGE_LOOP ( 'NONE', ( #118865, #106263, #56842, #37729, #69593 ) ) ;
#9443=ORIENTED_EDGE ( 'NONE', *, *, #52987, .T. ) ;
#9478=LINE ( 'NONE', #20364, #139071 ) ;
#9518=ORIENTED_EDGE ( 'NONE', *, *, #72885, .T. ) ;
#9532=EDGE_CURVE ( 'NONE', #29201, #118149, #12381, .T. ) ;
#9541=VERTEX_POINT ( 'NONE', #48136 ) ;
#9544=ORIENTED_EDGE ( 'NONE', *, *, #39977, .T. ) ;
#9548=CARTESIAN_POINT ( 'NONE',  ( -12.69999999999998153, 0.4000000000000001887, -2.467792535850613866 ) ) ;
#9566=CARTESIAN_POINT ( 'NONE',  ( 1.827855086967997478, 2.055000000000001048, 2.516649172247811554E-16 ) ) ;
#9570=FACE_OUTER_BOUND ( 'NONE', #135441, .T. ) ;
#9611=DIRECTION ( 'NONE',  ( -1.000000000000000000, -1.224606353822377258E-16, -0.000000000000000000 ) ) ;
#9613=EDGE_CURVE ( 'NONE', #94686, #1885, #139717, .T. ) ;
#9629=CARTESIAN_POINT ( 'NONE',  ( 5.281315875828549444, 2.500000000000000888, 0.000000000000000000 ) ) ;
#9656=CONICAL_SURFACE ( 'NONE', #93087, 2.500000000000000444, 0.9599310885968830309 ) ;
#9678=CARTESIAN_POINT ( 'NONE',  ( 14.70692117890024697, 4.584330080086930965E-16, 0.000000000000000000 ) ) ;
#9684=EDGE_LOOP ( 'NONE', ( #87362, #82904, #35603, #37501, #124588 ) ) ;
#9716=CIRCLE ( 'NONE', #63059, 2.500000000000000444 ) ;
#9730=EDGE_LOOP ( 'NONE', ( #9094, #136529, #100923, #31263, #98684 ) ) ;
#9738=ADVANCED_FACE ( 'NONE', ( #82909 ), #37981, .T. ) ;
#9877=LINE ( 'NONE', #98337, #57107 ) ;
#9919=CARTESIAN_POINT ( 'NONE',  ( 12.82439460721831104, 2.055000000000001048, 2.516649172247811554E-16 ) ) ;
#9923=CARTESIAN_POINT ( 'NONE',  ( 2.301729841053981485, 3.821174125832445049E-16, 0.000000000000000000 ) ) ;
#9935=AXIS2_PLACEMENT_3D ( 'NONE', #134722, #3433, #135429 ) ;
#9950=VERTEX_POINT ( 'NONE', #140572 ) ;
#9974=EDGE_CURVE ( 'NONE', #76525, #126332, #98089, .T. ) ;
#9978=CARTESIAN_POINT ( 'NONE',  ( 4.658131166821905644, 3.821174125832445049E-16, 0.000000000000000000 ) ) ;
#10019=VERTEX_POINT ( 'NONE', #37989 ) ;
#10062=EDGE_CURVE ( 'NONE', #122249, #14269, #79621, .T. ) ;
#10089=EDGE_CURVE ( 'NONE', #73407, #20849, #10107, .T. ) ;
#10107=CIRCLE ( 'NONE', #128209, 2.500000000000000444 ) ;
#10150=DIRECTION ( 'NONE',  ( 0.000000000000000000, 0.000000000000000000, 1.000000000000000000 ) ) ;
#10183=EDGE_LOOP ( 'NONE', ( #1692, #16563, #61399, #95948, #113499 ) ) ;
#10207=CIRCLE ( 'NONE', #130598, 2.500000000000000444 ) ;
#10208=ORIENTED_EDGE ( 'NONE', *, *, #10062, .T. ) ;
#10233=DIRECTION ( 'NONE',  ( 8.673617379884034239E-17, -1.000000000000000000, 0.000000000000000000 ) ) ;
#10242=DIRECTION ( 'NONE',  ( 0.000000000000000000, -1.000000000000000000, 0.000000000000000000 ) ) ;
#10245=VERTEX_POINT ( 'NONE', #53100 ) ;
#10329=CIRCLE ( 'NONE', #107512, 2.500000000000000444 ) ;
#10352=DIRECTION ( 'NONE',  ( -0.5735764363510501562, 0.8191520442889890230, 1.003171929053521419E-16 ) ) ;
#10415=ORIENTED_EDGE ( 'NONE', *, *, #68268, .T. ) ;
#10417=AXIS2_PLACEMENT_3D ( 'NONE', #114412, #59356, #138316 ) ;
#10421=ORIENTED_EDGE ( 'NONE', *, *, #27291, .F. ) ;
#10494=CARTESIAN_POINT ( 'NONE',  ( 15.96626304157554266, -2.055000000000000160, 2.789133085058097101E-16 ) ) ;
#10496=EDGE_CURVE ( 'NONE', #76190, #2459, #38513, .T. ) ;
#10512=DIRECTION ( 'NONE',  ( -0.5735764363510499342, -0.8191520442889891340, 0.000000000000000000 ) ) ;
#10523=ORIENTED_EDGE ( 'NONE', *, *, #49564, .F. ) ;
#10525=AXIS2_PLACEMENT_3D ( 'NONE', #106353, #38290, #140441 ) ;
#10532=DIRECTION ( 'NONE',  ( 0.000000000000000000, -1.000000000000000000, 0.000000000000000000 ) ) ;
#10551=VERTEX_POINT ( 'NONE', #108007 ) ;
#10570=EDGE_LOOP ( 'NONE', ( #114052, #35978, #38792, #54289, #40878 ) ) ;
#10602=ADVANCED_FACE ( 'NONE', ( #19600 ), #30852, .T. ) ;
#10620=AXIS2_PLACEMENT_3D ( 'NONE', #103607, #36251, #58764 ) ;
#10626=DIRECTION ( 'NONE',  ( 1.000000000000000000, 1.224606353822377258E-16, 0.000000000000000000 ) ) ;
#10630=ORIENTED_EDGE ( 'NONE', *, *, #39621, .T. ) ;
#10685=CARTESIAN_POINT ( 'NONE',  ( 17.84878961325748037, 4.584330080086930965E-16, 0.000000000000000000 ) ) ;
#10693=CARTESIAN_POINT ( 'NONE',  ( 1.629999999999999893, -0.3999999999999997446, -2.303088455023527104 ) ) ;
#10750=ORIENTED_EDGE ( 'NONE', *, *, #77954, .T. ) ;
#10751=EDGE_CURVE ( 'NONE', #5194, #59910, #110863, .T. ) ;
#10864=DIRECTION ( 'NONE',  ( -1.000000000000000000, -1.224606353822377258E-16, -0.000000000000000000 ) ) ;
#10865=CARTESIAN_POINT ( 'NONE',  ( 20.99065804761471199, 2.500000000000000888, 0.000000000000000000 ) ) ;
#10868=CARTESIAN_POINT ( 'NONE',  ( 6.540657738503846907, 2.055000000000001048, 0.000000000000000000 ) ) ;
#10886=ADVANCED_FACE ( 'NONE', ( #125351 ), #70210, .T. ) ;
#10931=EDGE_LOOP ( 'NONE', ( #11713, #85734, #85442, #73324, #103170, #102916 ) ) ;
#10970=CARTESIAN_POINT ( 'NONE',  ( 20.99065804761471199, 2.500000000000000444, 0.000000000000000000 ) ) ;
#11048=CARTESIAN_POINT ( 'NONE',  ( -12.69999999999998153, 0.000000000000000000, 0.000000000000000000 ) ) ;
#11049=EDGE_LOOP ( 'NONE', ( #8259, #137665, #101322, #77516, #98232, #79687 ) ) ;
#11087=DIRECTION ( 'NONE',  ( -0.5735764363510501562, 0.8191520442889890230, 1.003171929053521419E-16 ) ) ;
#11090=ORIENTED_EDGE ( 'NONE', *, *, #122748, .T. ) ;
#11096=CARTESIAN_POINT ( 'NONE',  ( 0.9387690737794647244, -0.3999999999999998002, -2.166563419957292957 ) ) ;
#11111=ADVANCED_FACE ( 'NONE', ( #64924 ), #98740, .T. ) ;
#11134=EDGE_CURVE ( 'NONE', #51507, #7626, #1049, .T. ) ;
#11168=ADVANCED_FACE ( 'NONE', ( #3203 ), #17705, .T. ) ;
#11216=EDGE_CURVE ( 'NONE', #78997, #12173, #3716, .T. ) ;
#11221=EDGE_CURVE ( 'NONE', #12102, #12477, #84785, .T. ) ;
#11223=CARTESIAN_POINT ( 'NONE',  ( -12.69999999999998153, 0.000000000000000000, 0.000000000000000000 ) ) ;
#11258=DIRECTION ( 'NONE',  ( -1.000000000000000000, -0.000000000000000000, -0.000000000000000000 ) ) ;
#11260=CARTESIAN_POINT ( 'NONE',  ( 9.208651418775088970, -2.500000000000000000, 3.061616997868383634E-16 ) ) ;
#11262=CARTESIAN_POINT ( 'NONE',  ( 9.682526172861077640, -2.055000000000000160, 2.789133085058097101E-16 ) ) ;
#11311=CARTESIAN_POINT ( 'NONE',  ( 11.72733514412567857, 3.061616997868383634E-16, -2.500000000000000444 ) ) ;
#11425=EDGE_CURVE ( 'NONE', #108094, #51277, #71051, .T. ) ;
#11444=CIRCLE ( 'NONE', #64678, 2.055000000000000604 ) ;
#11452=FACE_OUTER_BOUND ( 'NONE', #99432, .T. ) ;
#11453=AXIS2_PLACEMENT_3D ( 'NONE', #118588, #51932, #109142 ) ;
#11472=DIRECTION ( 'NONE',  ( 0.000000000000000000, 0.000000000000000000, 1.000000000000000000 ) ) ;
#11527=ORIENTED_EDGE ( 'NONE', *, *, #132226, .F. ) ;
#11550=AXIS2_PLACEMENT_3D ( 'NONE', #6950, #115718, #84579 ) ;
#11582=CARTESIAN_POINT ( 'NONE',  ( 2.301729841053981485, -4.814824860968089633E-32, 2.500000000000000444 ) ) ;
#11587=ORIENTED_EDGE ( 'NONE', *, *, #27688, .T. ) ;
#11602=CARTESIAN_POINT ( 'NONE',  ( 18.63425672184678916, 4.584330080086930965E-16, 0.000000000000000000 ) ) ;
#11616=VERTEX_POINT ( 'NONE', #34255 ) ;
#11667=CARTESIAN_POINT ( 'NONE',  ( 8.423184310185783730, 0.000000000000000000, 2.500000000000000444 ) ) ;
#11680=LINE ( 'NONE', #9548, #36340 ) ;
#11691=CARTESIAN_POINT ( 'NONE',  ( 2.139447441471317379, -9.629649721936179265E-32, 2.500000000000000444 ) ) ;
#11713=ORIENTED_EDGE ( 'NONE', *, *, #15487, .F. ) ;
#11718=DIRECTION ( 'NONE',  ( 0.000000000000000000, -1.000000000000000000, 0.000000000000000000 ) ) ;
#11783=EDGE_LOOP ( 'NONE', ( #142176, #89925, #96218, #918, #58583 ) ) ;
#11817=ADVANCED_FACE ( 'NONE', ( #84891 ), #135907, .T. ) ;
#11837=ORIENTED_EDGE ( 'NONE', *, *, #16759, .F. ) ;
#11878=LINE ( 'NONE', #43822, #36446 ) ;
#11900=DIRECTION ( 'NONE',  ( -1.000000000000000000, -1.224606353822377258E-16, -0.000000000000000000 ) ) ;
#11920=VERTEX_POINT ( 'NONE', #107352 ) ;
#11950=AXIS2_PLACEMENT_3D ( 'NONE', #52293, #41419, #52996 ) ;
#11975=CARTESIAN_POINT ( 'NONE',  ( 17.53719725875415847, 4.202752102959690472E-16, 0.000000000000000000 ) ) ;
#11987=ORIENTED_EDGE ( 'NONE', *, *, #120889, .T. ) ;
#11999=EDGE_CURVE ( 'NONE', #103339, #84629, #22460, .T. ) ;
#12012=AXIS2_PLACEMENT_3D ( 'NONE', #2853, #103585, #48512 ) ;
#12025=CIRCLE ( 'NONE', #49120, 2.055000000000000604 ) ;
#12033=DIRECTION ( 'NONE',  ( 0.000000000000000000, -1.000000000000000000, 0.000000000000000000 ) ) ;
#12057=EDGE_CURVE ( 'NONE', #58140, #108385, #41013, .T. ) ;
#12089=VECTOR ( 'NONE', #99728, 1000.000000000000000 ) ;
#12090=ORIENTED_EDGE ( 'NONE', *, *, #32051, .T. ) ;
#12102=VERTEX_POINT ( 'NONE', #13723 ) ;
#12106=VERTEX_POINT ( 'NONE', #77612 ) ;
#12139=DIRECTION ( 'NONE',  ( 0.000000000000000000, -1.000000000000000000, 0.000000000000000000 ) ) ;
#12146=DIRECTION ( 'NONE',  ( 0.000000000000000000, -1.000000000000000000, 0.000000000000000000 ) ) ;
#12169=CARTESIAN_POINT ( 'NONE',  ( 4.495848767239241539, 2.500000000000000888, 0.000000000000000000 ) ) ;
#12173=VERTEX_POINT ( 'NONE', #5704 ) ;
#12261=ORIENTED_EDGE ( 'NONE', *, *, #6917, .F. ) ;
#12268=ORIENTED_EDGE ( 'NONE', *, *, #112550, .T. ) ;
#12270=CARTESIAN_POINT ( 'NONE',  ( 11.25346039003969523, 4.202752102959690472E-16, 0.000000000000000000 ) ) ;
#12293=AXIS2_PLACEMENT_3D ( 'NONE', #107322, #108721, #118173 ) ;
#12310=ORIENTED_EDGE ( 'NONE', *, *, #105507, .T. ) ;
#12372=CONICAL_SURFACE ( 'NONE', #68011, 2.500000000000000444, 0.9599310885968830309 ) ;
#12381=CIRCLE ( 'NONE', #123477, 2.500000000000000444 ) ;
#12392=ORIENTED_EDGE ( 'NONE', *, *, #28436, .T. ) ;
#12422=DIRECTION ( 'NONE',  ( 1.734723475976806848E-16, -1.000000000000000000, 0.000000000000000000 ) ) ;
#12438=CARTESIAN_POINT ( 'NONE',  ( 6.066782984417857350, 4.584330080086930965E-16, 0.000000000000000000 ) ) ;
#12444=CONICAL_SURFACE ( 'NONE', #102704, 2.500000000000000444, 0.9599310885968830309 ) ;
#12477=VERTEX_POINT ( 'NONE', #131800 ) ;
#12490=FACE_OUTER_BOUND ( 'NONE', #78385, .T. ) ;
#12533=CARTESIAN_POINT ( 'NONE',  ( 8.423184310185783730, -2.500000000000000444, 3.061616997868384127E-16 ) ) ;
#12548=VECTOR ( 'NONE', #140766, 1000.000000000000000 ) ;
#12566=AXIS2_PLACEMENT_3D ( 'NONE', #526, #97718, #131789 ) ;
#12583=DIRECTION ( 'NONE',  ( -1.000000000000000000, -0.000000000000000000, -0.000000000000000000 ) ) ;
#12619=LINE ( 'NONE', #25638, #139849 ) ;
#12623=LINE ( 'NONE', #101055, #88683 ) ;
#12683=EDGE_CURVE ( 'NONE', #110962, #87033, #130214, .T. ) ;
#12697=EDGE_CURVE ( 'NONE', #124724, #88761, #126466, .T. ) ;
#12706=CARTESIAN_POINT ( 'NONE',  ( 11.25346039003969523, -2.055000000000000160, 2.789133085058097101E-16 ) ) ;
#12711=DIRECTION ( 'NONE',  ( -1.000000000000000000, -1.224606353822377258E-16, -0.000000000000000000 ) ) ;
#12719=DIRECTION ( 'NONE',  ( 1.000000000000000000, 1.224606353822377258E-16, 0.000000000000000000 ) ) ;
#12727=CARTESIAN_POINT ( 'NONE',  ( -12.69999999999998153, 0.000000000000000000, 0.000000000000000000 ) ) ;
#12737=DIRECTION ( 'NONE',  ( 0.5735764363510444941, 0.8191520442889929088, 0.000000000000000000 ) ) ;
#12749=ORIENTED_EDGE ( 'NONE', *, *, #45996, .T. ) ;
#12772=CARTESIAN_POINT ( 'NONE',  ( -12.69999999999998153, 0.000000000000000000, 0.000000000000000000 ) ) ;
#12788=CARTESIAN_POINT ( 'NONE',  ( 13.29826936130429260, -2.500000000000001776, 0.000000000000000000 ) ) ;
#12792=DIRECTION ( 'NONE',  ( -1.000000000000000000, -1.224606353822377258E-16, -0.000000000000000000 ) ) ;
#12793=AXIS2_PLACEMENT_3D ( 'NONE', #90253, #37324, #134502 ) ;
#12833=FACE_OUTER_BOUND ( 'NONE', #139729, .T. ) ;
#12863=AXIS2_PLACEMENT_3D ( 'NONE', #108239, #21279, #42339 ) ;
#12884=AXIS2_PLACEMENT_3D ( 'NONE', #42490, #97539, #86694 ) ;
#12905=VERTEX_POINT ( 'NONE', #48735 ) ;
#12995=CIRCLE ( 'NONE', #94032, 2.500000000000000444 ) ;
#13005=LINE ( 'NONE', #36222, #72664 ) ;
#13056=VERTEX_POINT ( 'NONE', #118965 ) ;
#13072=EDGE_CURVE ( 'NONE', #50807, #72701, #103375, .T. ) ;
#13083=ORIENTED_EDGE ( 'NONE', *, *, #863, .F. ) ;
#13111=FACE_OUTER_BOUND ( 'NONE', #70720, .T. ) ;
#13115=ORIENTED_EDGE ( 'NONE', *, *, #134671, .F. ) ;
#13118=ORIENTED_EDGE ( 'NONE', *, *, #126761, .T. ) ;
#13122=DIRECTION ( 'NONE',  ( -1.000000000000000000, -1.224606353822377258E-16, -0.000000000000000000 ) ) ;
#13177=ORIENTED_EDGE ( 'NONE', *, *, #82115, .F. ) ;
#13178=EDGE_LOOP ( 'NONE', ( #125419, #135739, #140264, #137351, #45481, #127619 ) ) ;
#13192=LINE ( 'NONE', #44457, #86592 ) ;
#13226=EDGE_CURVE ( 'NONE', #131513, #130990, #34123, .T. ) ;
#13272=VERTEX_POINT ( 'NONE', #94176 ) ;
#13278=CARTESIAN_POINT ( 'NONE',  ( 1.554198618961949885, 0.3999999999999995226, 2.412907390626680026 ) ) ;
#13329=ORIENTED_EDGE ( 'NONE', *, *, #99021, .T. ) ;
#13381=EDGE_CURVE ( 'NONE', #44009, #102743, #65889, .T. ) ;
#13400=CIRCLE ( 'NONE', #71295, 2.055000000000000604 ) ;
#13476=ORIENTED_EDGE ( 'NONE', *, *, #104229, .F. ) ;
#13477=ADVANCED_FACE ( 'NONE', ( #88331 ), #99902, .T. ) ;
#13492=( LENGTH_UNIT ( ) NAMED_UNIT ( * ) SI_UNIT ( .MILLI., .METRE. ) );
#13500=EDGE_LOOP ( 'NONE', ( #57039, #9518, #101181, #47779, #105390 ) ) ;
#13521=AXIS2_PLACEMENT_3D ( 'NONE', #88271, #22254, #34597 ) ;
#13571=FACE_OUTER_BOUND ( 'NONE', #128853, .T. ) ;
#13585=DIRECTION ( 'NONE',  ( 0.000000000000000000, -1.000000000000000000, 0.000000000000000000 ) ) ;
#13593=AXIS2_PLACEMENT_3D ( 'NONE', #43588, #119685, #10233 ) ;
#13595=ORIENTED_EDGE ( 'NONE', *, *, #9974, .F. ) ;
#13596=AXIS2_PLACEMENT_3D ( 'NONE', #108638, #96333, #18053 ) ;
#13631=DIRECTION ( 'NONE',  ( -1.000000000000000000, -1.224606353822377258E-16, -0.000000000000000000 ) ) ;
#13637=ORIENTED_EDGE ( 'NONE', *, *, #59101, .T. ) ;
#13647=CARTESIAN_POINT ( 'NONE',  ( 3.398789304146613954, 4.202752102959690472E-16, 0.000000000000000000 ) ) ;
#13663=EDGE_CURVE ( 'NONE', #96600, #136985, #46013, .T. ) ;
#13723=CARTESIAN_POINT ( 'NONE',  ( 5.443598275411213550, 0.000000000000000000, 2.500000000000000444 ) ) ;
#13735=DIRECTION ( 'NONE',  ( 1.734723475976806848E-16, -1.000000000000000000, 0.000000000000000000 ) ) ;
#13742=DIRECTION ( 'NONE',  ( 1.000000000000000000, 1.224606353822377258E-16, 0.000000000000000000 ) ) ;
#13745=VERTEX_POINT ( 'NONE', #42530 ) ;
#13749=ADVANCED_FACE ( 'NONE', ( #64987 ), #107028, .T. ) ;
#13773=ORIENTED_EDGE ( 'NONE', *, *, #90997, .F. ) ;
#13803=CONICAL_SURFACE ( 'NONE', #85523, 2.500000000000000444, 0.9599310885968830309 ) ;
#13828=CIRCLE ( 'NONE', #20784, 2.055000000000000604 ) ;
#13851=EDGE_CURVE ( 'NONE', #106463, #76190, #117444, .T. ) ;
#13853=DIRECTION ( 'NONE',  ( 0.000000000000000000, 0.000000000000000000, 1.000000000000000000 ) ) ;
#13875=CARTESIAN_POINT ( 'NONE',  ( 20.36747333860806819, 4.333342374871280669E-31, 2.500000000000000444 ) ) ;
#13881=DIRECTION ( 'NONE',  ( 0.000000000000000000, 0.000000000000000000, 1.000000000000000000 ) ) ;
#13929=CIRCLE ( 'NONE', #57973, 2.055000000000000604 ) ;
#13931=ORIENTED_EDGE ( 'NONE', *, *, #102531, .T. ) ;
#13934=CARTESIAN_POINT ( 'NONE',  ( 1.042387978378689573, 0.3999999999999995781, 2.015694669338588429 ) ) ;
#14076=DIRECTION ( 'NONE',  ( 1.000000000000000000, 1.224606353822377258E-16, 0.000000000000000000 ) ) ;
#14079=CARTESIAN_POINT ( 'NONE',  ( 8.585466709768445170, 3.061616997868383634E-16, -2.500000000000000444 ) ) ;
#14100=ORIENTED_EDGE ( 'NONE', *, *, #6917, .T. ) ;
#14105=AXIS2_PLACEMENT_3D ( 'NONE', #142028, #57885, #23044 ) ;
#14147=VECTOR ( 'NONE', #57923, 999.9999999999998863 ) ;
#14181=FACE_OUTER_BOUND ( 'NONE', #118700, .T. ) ;
#14183=AXIS2_PLACEMENT_3D ( 'NONE', #30849, #119242, #31546 ) ;
#14184=EDGE_CURVE ( 'NONE', #12102, #88761, #8232, .T. ) ;
#14187=DIRECTION ( 'NONE',  ( -1.000000000000000000, -0.000000000000000000, -0.000000000000000000 ) ) ;
#14215=ORIENTED_EDGE ( 'NONE', *, *, #47148, .T. ) ;
#14269=VERTEX_POINT ( 'NONE', #117704 ) ;
#14275=DIRECTION ( 'NONE',  ( -1.000000000000000000, -0.000000000000000000, -0.000000000000000000 ) ) ;
#14320=CIRCLE ( 'NONE', #58363, 2.055000000000000604 ) ;
#14321=FACE_OUTER_BOUND ( 'NONE', #71899, .T. ) ;
#14384=FACE_OUTER_BOUND ( 'NONE', #10183, .T. ) ;
#14387=EDGE_CURVE ( 'NONE', #122233, #13272, #32551, .T. ) ;
#14407=ORIENTED_EDGE ( 'NONE', *, *, #51778, .F. ) ;
#14416=EDGE_CURVE ( 'NONE', #22488, #103049, #77132, .T. ) ;
#14434=ADVANCED_FACE ( 'NONE', ( #204 ), #108879, .T. ) ;
#14470=AXIS2_PLACEMENT_3D ( 'NONE', #75071, #63486, #27964 ) ;
#14484=CARTESIAN_POINT ( 'NONE',  ( -12.69999999999998153, 0.000000000000000000, 0.000000000000000000 ) ) ;
#14625=AXIS2_PLACEMENT_3D ( 'NONE', #128207, #126736, #115131 ) ;
#14650=VERTEX_POINT ( 'NONE', #591 ) ;
#14657=CARTESIAN_POINT ( 'NONE',  ( 2.139447441471317823, -2.500000000000000000, 3.061616997868383634E-16 ) ) ;
#14684=AXIS2_PLACEMENT_3D ( 'NONE', #59206, #92484, #24391 ) ;
#14720=ADVANCED_FACE ( 'NONE', ( #11452 ), #29140, .T. ) ;
#14730=CIRCLE ( 'NONE', #114279, 2.500000000000000444 ) ;
#14737=VERTEX_POINT ( 'NONE', #25941 ) ;
#14740=CARTESIAN_POINT ( 'NONE',  ( 14.86920357848291196, 3.061616997868383634E-16, -2.500000000000000444 ) ) ;
#14747=CARTESIAN_POINT ( 'NONE',  ( 2.924914550060625285, 3.061616997868382648E-16, -2.500000000000000444 ) ) ;
#14759=CARTESIAN_POINT ( 'NONE',  ( 13.92145407031093818, 4.584330080086930965E-16, 0.000000000000000000 ) ) ;
#14799=EDGE_CURVE ( 'NONE', #57263, #68516, #106705, .T. ) ;
#14830=LINE ( 'NONE', #137347, #67531 ) ;
#14835=DIRECTION ( 'NONE',  ( 0.000000000000000000, -1.000000000000000000, 0.000000000000000000 ) ) ;
#14839=DIRECTION ( 'NONE',  ( 0.000000000000000000, -1.000000000000000000, 0.000000000000000000 ) ) ;
#14964=CARTESIAN_POINT ( 'NONE',  ( 18.32266436734346726, -2.055000000000000160, 0.000000000000000000 ) ) ;
#14973=AXIS2_PLACEMENT_3D ( 'NONE', #58395, #102578, #136599 ) ;
#14999=CARTESIAN_POINT ( 'NONE',  ( 0.3605397743886045170, -0.4000000000000003553, 2.166563419957292513 ) ) ;
#15010=DIRECTION ( 'NONE',  ( 0.000000000000000000, 1.000000000000000000, 0.000000000000000000 ) ) ;
#15025=ADVANCED_FACE ( 'NONE', ( #109910 ), #2499, .T. ) ;
#15051=ORIENTED_EDGE ( 'NONE', *, *, #117649, .F. ) ;
#15063=ORIENTED_EDGE ( 'NONE', *, *, #99659, .T. ) ;
#15089=EDGE_LOOP ( 'NONE', ( #142651, #72666, #135057, #3495, #22723 ) ) ;
#15090=CYLINDRICAL_SURFACE ( 'NONE', #116615, 2.500000000000000444 ) ;
#15174=AXIS2_PLACEMENT_3D ( 'NONE', #560, #89042, #44852 ) ;
#15188=CARTESIAN_POINT ( 'NONE',  ( 1.353980332882009252, 4.584330080086930965E-16, 0.000000000000000000 ) ) ;
#15220=CARTESIAN_POINT ( 'NONE',  ( 0.9387689034200080718, -0.4000000000000003553, 2.166563668000045961 ) ) ;
#15234=CARTESIAN_POINT ( 'NONE',  ( 8.423184310185783730, 2.500000000000000444, 0.000000000000000000 ) ) ;
#15254=DIRECTION ( 'NONE',  ( 0.000000000000000000, 0.000000000000000000, 1.000000000000000000 ) ) ;
#15274=ADVANCED_BREP_SHAPE_REPRESENTATION ( '', ( #46161, #127880 ), #97842 ) ;
#15288=ORIENTED_EDGE ( 'NONE', *, *, #24083, .T. ) ;
#15291=EDGE_CURVE ( 'NONE', #40384, #134578, #97609, .T. ) ;
#15374=CONICAL_SURFACE ( 'NONE', #107991, 2.500000000000000444, 0.9599310885968830309 ) ;
#15457=EDGE_CURVE ( 'NONE', #84629, #64882, #64102, .T. ) ;
#15487=EDGE_CURVE ( 'NONE', #130884, #16482, #129342, .T. ) ;
#15504=FACE_OUTER_BOUND ( 'NONE', #72211, .T. ) ;
#15511=AXIS2_PLACEMENT_3D ( 'NONE', #79054, #10864, #55131 ) ;
#15560=CARTESIAN_POINT ( 'NONE',  ( 3.872664058232598183, 3.821174125832445049E-16, 0.000000000000000000 ) ) ;
#15565=VERTEX_POINT ( 'NONE', #124188 ) ;
#15570=DIRECTION ( 'NONE',  ( 0.000000000000000000, -1.000000000000000000, 0.000000000000000000 ) ) ;
#15589=VERTEX_POINT ( 'NONE', #122023 ) ;
#15606=DIRECTION ( 'NONE',  ( -1.000000000000000000, -1.224606353822377258E-16, -0.000000000000000000 ) ) ;
#15618=LINE ( 'NONE', #70794, #136951 ) ;
#15633=CARTESIAN_POINT ( 'NONE',  ( 4.495848767239241539, 2.500000000000000444, 0.000000000000000000 ) ) ;
#15646=EDGE_CURVE ( 'NONE', #38043, #19525, #127762, .T. ) ;
#15657=EDGE_CURVE ( 'NONE', #10245, #104418, #74573, .T. ) ;
#15670=LINE ( 'NONE', #59957, #28207 ) ;
#15687=AXIS2_PLACEMENT_3D ( 'NONE', #97060, #129729, #40606 ) ;
#15749=DIRECTION ( 'NONE',  ( -1.000000000000000000, -0.000000000000000000, -0.000000000000000000 ) ) ;
#15772=CARTESIAN_POINT ( 'NONE',  ( 0.7307956238753654521, 3.821174125832445049E-16, 0.000000000000000000 ) ) ;
#15786=ORIENTED_EDGE ( 'NONE', *, *, #19290, .F. ) ;
#15795=EDGE_CURVE ( 'NONE', #73287, #137211, #141732, .T. ) ;
#15821=EDGE_CURVE ( 'NONE', #103560, #142252, #116150, .T. ) ;
#15888=ORIENTED_EDGE ( 'NONE', *, *, #140873, .F. ) ;
#15892=AXIS2_PLACEMENT_3D ( 'NONE', #126764, #105023, #94138 ) ;
#15897=ORIENTED_EDGE ( 'NONE', *, *, #51537, .T. ) ;
#15929=FACE_OUTER_BOUND ( 'NONE', #70759, .T. ) ;
#15934=EDGE_CURVE ( 'NONE', #24150, #98637, #55201, .T. ) ;
#15953=B_SPLINE_CURVE_WITH_KNOTS ( 'NONE', 3,
 ( #13934, #90833, #48041, #103115 ),
 .UNSPECIFIED., .F., .F.,
 ( 4, 4 ),
 ( 0.008853860144884173958, 0.009403245473020183098 ),
 .UNSPECIFIED. ) ;
#16010=LINE ( 'NONE', #69200, #20930 ) ;
#16013=DIRECTION ( 'NONE',  ( -1.000000000000000000, -1.224606353822377258E-16, -0.000000000000000000 ) ) ;
#16019=VERTEX_POINT ( 'NONE', #102289 ) ;
#16127=LINE ( 'NONE', #93731, #52007 ) ;
#16171=CARTESIAN_POINT ( 'NONE',  ( -12.69999999999998153, 3.061616997868383634E-16, -2.500000000000000444 ) ) ;
#16173=VERTEX_POINT ( 'NONE', #140586 ) ;
#16174=CARTESIAN_POINT ( 'NONE',  ( 2.924914550060625285, 4.584330080086930965E-16, 0.000000000000000000 ) ) ;
#16195=CIRCLE ( 'NONE', #44083, 2.500000000000000444 ) ;
#16208=CIRCLE ( 'NONE', #97233, 2.500000000000000444 ) ;
#16210=DIRECTION ( 'NONE',  ( -1.000000000000000000, -1.224606353822377258E-16, -0.000000000000000000 ) ) ;
#16224=DIRECTION ( 'NONE',  ( -1.000000000000000000, -1.224606353822377258E-16, -0.000000000000000000 ) ) ;
#16239=CARTESIAN_POINT ( 'NONE',  ( 8.585466709768445170, -2.500000000000001776, 0.000000000000000000 ) ) ;
#16243=CLOSED_SHELL ( 'NONE', ( #76042, #99156, #50442, #118200, #139262, #142524, #105420, #56673, #115495, #11111, #83621, #4747, #137523, #96623, #73242, #134531, #121584, #23425, #76383, #96450, #47704, #42737, #142729, #17124, #11168, #56831, #11817, #105467, #27455, #94205, #46810, #120649, #96166, #101250, #13477, #52568, #21289, #107295, #271, #19012, #87371, #23548, #30814, #84662, #107683, #70386, #117176, #87070, #82338, #16784, #69023, #70725, #42009, #111567, #128495, #85358, #66574, #65558, #24677, #21220, #7659, #61379, #45230, #77103, #124193, #138400, #54329, #52034, #39587, #20528, #139788, #78070, #68674, #135521, #141131, #45469, #46128, #77455, #75125, #89296, #134571, #36602, #44142, #135791, #41658, #24164, #14720, #105366, #141910, #60734, #107810, #142042, #94065, #20077, #70903, #131472, #70115, #13749, #28701, #95019, #105755, #66056, #78371, #106173, #90323, #31763, #123855, #34856, #18582, #2454, #142132, #19788, #65897, #134649, #114931, #108246, #70027, #53339, #32614, #8583, #62495, #79933, #54838, #91785, #118272, #103493, #43823, #29496, #97796, #63780, #140402, #134216, #107799, #31294, #51717, #26610, #62561, #50072, #86572, #50063, #139737, #9738, #61716, #120386, #48293, #41505, #111617, #122704, #39927, #92396, #2582, #101415, #112160, #127492, #59200, #89559, #143207, #10886, #46518, #31224, #121182, #49184, #36946, #142031, #79971, #58101, #127385, #30731, #15025, #75002, #60556, #17641, #90820, #115847, #134367, #124856, #120219, #93054, #14434, #46875, #36858, #10602 ) ) ;
#16327=DIRECTION ( 'NONE',  ( 1.055184596092948005E-16, -1.000000000000000000, 0.000000000000000000 ) ) ;
#16358=AXIS2_PLACEMENT_3D ( 'NONE', #27626, #46032, #123602 ) ;
#16361=CIRCLE ( 'NONE', #48802, 2.500000000000000444 ) ;
#16376=CARTESIAN_POINT ( 'NONE',  ( 9.208651418775088970, 0.000000000000000000, 2.500000000000000444 ) ) ;
#16413=CARTESIAN_POINT ( 'NONE',  ( 6.852250093007166143, 4.584330080086930965E-16, 0.000000000000000000 ) ) ;
#16469=DIRECTION ( 'NONE',  ( -1.000000000000000000, -1.224606353822377258E-16, -0.000000000000000000 ) ) ;
#16482=VERTEX_POINT ( 'NONE', #109033 ) ;
#16513=AXIS2_PLACEMENT_3D ( 'NONE', #112798, #72022, #35283 ) ;
#16550=AXIS2_PLACEMENT_3D ( 'NONE', #42806, #130525, #86996 ) ;
#16563=ORIENTED_EDGE ( 'NONE', *, *, #97270, .F. ) ;
#16579=FACE_OUTER_BOUND ( 'NONE', #140655, .T. ) ;
#16591=AXIS2_PLACEMENT_3D ( 'NONE', #19259, #64200, #27995 ) ;
#16593=CONICAL_SURFACE ( 'NONE', #100030, 2.055000000000000604, 0.9599310885968764806 ) ;
#16686=CARTESIAN_POINT ( 'NONE',  ( 12.82439460721831104, 2.055000000000001048, 0.000000000000000000 ) ) ;
#16695=CARTESIAN_POINT ( 'NONE',  ( 9.994118527364397764, -2.500000000000000000, 3.061616997868383634E-16 ) ) ;
#16703=CIRCLE ( 'NONE', #60842, 2.500000000000000444 ) ;
#16715=ORIENTED_EDGE ( 'NONE', *, *, #81037, .F. ) ;
#16732=CARTESIAN_POINT ( 'NONE',  ( 20.20519093902540320, 2.500000000000000444, 0.000000000000000000 ) ) ;
#16759=EDGE_CURVE ( 'NONE', #110962, #28611, #42392, .T. ) ;
#16762=AXIS2_PLACEMENT_3D ( 'NONE', #77139, #52483, #96667 ) ;
#16784=ADVANCED_FACE ( 'NONE', ( #45267 ), #34352, .T. ) ;
#16788=EDGE_CURVE ( 'NONE', #106463, #119988, #101019, .T. ) ;
#16797=FACE_OUTER_BOUND ( 'NONE', #128980, .T. ) ;
#16803=CARTESIAN_POINT ( 'NONE',  ( -12.69999999999998153, 3.061616997868383634E-16, -2.500000000000000444 ) ) ;
#16806=CIRCLE ( 'NONE', #53874, 2.500000000000000444 ) ;
#16809=CARTESIAN_POINT ( 'NONE',  ( 21.15294044719737698, -2.499999999999996447, 0.000000000000000000 ) ) ;
#16886=VECTOR ( 'NONE', #74446, 1000.000000000000000 ) ;
#16960=EDGE_CURVE ( 'NONE', #132555, #74043, #21475, .T. ) ;
#16981=EDGE_LOOP ( 'NONE', ( #135597, #82932, #9443, #29082, #75042, #127690 ) ) ;
#17006=AXIS2_PLACEMENT_3D ( 'NONE', #18632, #72382, #117231 ) ;
#17008=LINE ( 'NONE', #38062, #87259 ) ;
#17042=EDGE_CURVE ( 'NONE', #82553, #27734, #132081, .T. ) ;
#17054=CARTESIAN_POINT ( 'NONE',  ( 13.29826936130429260, 3.821174125832445049E-16, 0.000000000000000000 ) ) ;
#17103=VECTOR ( 'NONE', #4517, 999.9999999999998863 ) ;
#17115=VECTOR ( 'NONE', #98358, 999.9999999999998863 ) ;
#17116=DIRECTION ( 'NONE',  ( -0.000000000000000000, 1.301042606982605074E-16, -1.000000000000000000 ) ) ;
#17124=ADVANCED_FACE ( 'NONE', ( #13111 ), #5396, .T. ) ;
#17156=AXIS2_PLACEMENT_3D ( 'NONE', #109621, #96568, #107480 ) ;
#17191=CARTESIAN_POINT ( 'NONE',  ( 10.46799328145038821, 2.055000000000001048, 2.516649172247811554E-16 ) ) ;
#17261=DIRECTION ( 'NONE',  ( -1.000000000000000000, -1.224606353822377258E-16, -0.000000000000000000 ) ) ;
#17267=ORIENTED_EDGE ( 'NONE', *, *, #21550, .T. ) ;
#17391=EDGE_LOOP ( 'NONE', ( #7499, #141154, #55044, #10523, #2557, #95487 ) ) ;
#17410=EDGE_LOOP ( 'NONE', ( #57733, #38206, #79653, #2870, #40043 ) ) ;
#17419=DIRECTION ( 'NONE',  ( 1.000000000000000000, 0.000000000000000000, 0.000000000000000000 ) ) ;
#17432=CARTESIAN_POINT ( 'NONE',  ( 13.29826936130429260, 0.000000000000000000, 2.500000000000000444 ) ) ;
#17441=EDGE_CURVE ( 'NONE', #67004, #102793, #28626, .T. ) ;
#17449=DIRECTION ( 'NONE',  ( 0.5735764363510444941, 0.8191520442889929088, 0.000000000000000000 ) ) ;
#17455=EDGE_LOOP ( 'NONE', ( #100788, #121878, #89319, #128322, #92643 ) ) ;
#17464=DIRECTION ( 'NONE',  ( -1.000000000000000000, -1.224606353822377258E-16, -0.000000000000000000 ) ) ;
#17534=ORIENTED_EDGE ( 'NONE', *, *, #71106, .T. ) ;
#17540=VERTEX_POINT ( 'NONE', #44186 ) ;
#17542=VERTEX_POINT ( 'NONE', #111561 ) ;
#17554=AXIS2_PLACEMENT_3D ( 'NONE', #7697, #141821, #131651 ) ;
#17574=CARTESIAN_POINT ( 'NONE',  ( 15.18079593298623564, 2.055000000000001048, 0.000000000000000000 ) ) ;
#17606=DIRECTION ( 'NONE',  ( -1.000000000000000000, -1.224606353822377258E-16, -0.000000000000000000 ) ) ;
#17641=ADVANCED_FACE ( 'NONE', ( #79677 ), #12444, .T. ) ;
#17642=DIRECTION ( 'NONE',  ( 0.000000000000000000, 0.000000000000000000, 1.000000000000000000 ) ) ;
#17702=ORIENTED_EDGE ( 'NONE', *, *, #134833, .F. ) ;
#17703=CARTESIAN_POINT ( 'NONE',  ( 13.92145407031093818, 4.584330080086930965E-16, 0.000000000000000000 ) ) ;
#17705=CONICAL_SURFACE ( 'NONE', #73321, 2.500000000000000444, 0.9599310885968830309 ) ;
#17737=VECTOR ( 'NONE', #96837, 1000.000000000000000 ) ;
#17738=ORIENTED_EDGE ( 'NONE', *, *, #19486, .T. ) ;
#17764=EDGE_LOOP ( 'NONE', ( #82983, #90171, #70123, #22895, #49790 ) ) ;
#17801=DIRECTION ( 'NONE',  ( 0.5735764363510448272, -0.8191520442889927978, 1.003171929053526103E-16 ) ) ;
#17851=EDGE_CURVE ( 'NONE', #60360, #61548, #91237, .T. ) ;
#17887=DIRECTION ( 'NONE',  ( 0.000000000000000000, -1.000000000000000000, 0.000000000000000000 ) ) ;
#17914=EDGE_CURVE ( 'NONE', #60360, #98372, #65764, .T. ) ;
#17941=CARTESIAN_POINT ( 'NONE',  ( 11.72733514412567857, 3.821174125832445049E-16, 0.000000000000000000 ) ) ;
#17954=EDGE_CURVE ( 'NONE', #19275, #59344, #14730, .T. ) ;
#17958=ORIENTED_EDGE ( 'NONE', *, *, #16960, .F. ) ;
#17980=FACE_OUTER_BOUND ( 'NONE', #85243, .T. ) ;
#18004=LINE ( 'NONE', #126112, #123977 ) ;
#18053=DIRECTION ( 'NONE',  ( 0.000000000000000000, -1.000000000000000000, 0.000000000000000000 ) ) ;
#18061=CARTESIAN_POINT ( 'NONE',  ( 1.042387978378689573, -0.4000000000000003553, 2.015694669338588429 ) ) ;
#18125=LINE ( 'NONE', #117454, #86225 ) ;
#18131=LINE ( 'NONE', #106575, #67967 ) ;
#18171=DIRECTION ( 'NONE',  ( -1.000000000000000000, -0.000000000000000000, -0.000000000000000000 ) ) ;
#18180=CYLINDRICAL_SURFACE ( 'NONE', #140094, 2.500000000000000444 ) ;
#18214=EDGE_CURVE ( 'NONE', #51507, #121969, #7392, .T. ) ;
#18233=CONICAL_SURFACE ( 'NONE', #8896, 2.055000000000000604, 0.9599310885968764806 ) ;
#18248=EDGE_CURVE ( 'NONE', #69267, #103049, #45004, .T. ) ;
#18286=ORIENTED_EDGE ( 'NONE', *, *, #62092, .T. ) ;
#18288=DIRECTION ( 'NONE',  ( 0.000000000000000000, -1.000000000000000000, 0.000000000000000000 ) ) ;
#18292=DIRECTION ( 'NONE',  ( 0.000000000000000000, -1.000000000000000000, 0.000000000000000000 ) ) ;
#18297=LINE ( 'NONE', #42254, #135016 ) ;
#18412=DIRECTION ( 'NONE',  ( 1.201410254241279878E-16, -1.000000000000000000, 0.000000000000000000 ) ) ;
#18445=VERTEX_POINT ( 'NONE', #15234 ) ;
#18475=CIRCLE ( 'NONE', #87951, 2.500000000000000444 ) ;
#18481=ORIENTED_EDGE ( 'NONE', *, *, #9387, .T. ) ;
#18490=ORIENTED_EDGE ( 'NONE', *, *, #42802, .F. ) ;
#18528=DIRECTION ( 'NONE',  ( -1.000000000000000000, -1.224606353822377258E-16, -0.000000000000000000 ) ) ;
#18582=ADVANCED_FACE ( 'NONE', ( #15929 ), #3426, .T. ) ;
#18626=CONICAL_SURFACE ( 'NONE', #9402, 2.500000000000000444, 0.9599310885968830309 ) ;
#18629=CARTESIAN_POINT ( 'NONE',  ( 5.443598275411213550, 3.821174125832445049E-16, 0.000000000000000000 ) ) ;
#18632=CARTESIAN_POINT ( 'NONE',  ( 12.35051985313232237, 4.584330080086930965E-16, 0.000000000000000000 ) ) ;
#18645=CARTESIAN_POINT ( 'NONE',  ( 0.9387689034200082938, 0.4000000000000001332, -2.166563668000045517 ) ) ;
#18648=ORIENTED_EDGE ( 'NONE', *, *, #28436, .F. ) ;
#18713=VERTEX_POINT ( 'NONE', #140599 ) ;
#18733=CARTESIAN_POINT ( 'NONE',  ( 0.2569208697893813342, -0.4000000000000003553, 2.015694669338588429 ) ) ;
#18747=ORIENTED_EDGE ( 'NONE', *, *, #82507, .F. ) ;
#18822=CIRCLE ( 'NONE', #35112, 2.500000000000000444 ) ;
#18838=CARTESIAN_POINT ( 'NONE',  ( -12.69999999999998153, -0.4000000000000004108, 2.467792535850613866 ) ) ;
#18861=VECTOR ( 'NONE', #89657, 1000.000000000000000 ) ;
#18869=EDGE_CURVE ( 'NONE', #16019, #10551, #82139, .T. ) ;
#18877=VECTOR ( 'NONE', #51256, 1000.000000000000000 ) ;
#18878=DIRECTION ( 'NONE',  ( 0.000000000000000000, -1.000000000000000000, 0.000000000000000000 ) ) ;
#18951=EDGE_CURVE ( 'NONE', #5194, #141895, #63402, .T. ) ;
#18958=CARTESIAN_POINT ( 'NONE',  ( 1.827855086967997922, -2.055000000000000160, 0.000000000000000000 ) ) ;
#18977=AXIS2_PLACEMENT_3D ( 'NONE', #69707, #113891, #3657 ) ;
#18978=ORIENTED_EDGE ( 'NONE', *, *, #65496, .F. ) ;
#19012=ADVANCED_FACE ( 'NONE', ( #105645 ), #114265, .T. ) ;
#19037=DIRECTION ( 'NONE',  ( -1.000000000000000000, -0.000000000000000000, -0.000000000000000000 ) ) ;
#19046=DIRECTION ( 'NONE',  ( -0.5735764363510499342, -0.8191520442889891340, 0.000000000000000000 ) ) ;
#19052=DIRECTION ( 'NONE',  ( -1.000000000000000000, -1.224606353822377258E-16, -0.000000000000000000 ) ) ;
#19133=ORIENTED_EDGE ( 'NONE', *, *, #8639, .T. ) ;
#19141=B_SPLINE_CURVE_WITH_KNOTS ( 'NONE', 3,
 ( #52692, #53417, #84628, #19364 ),
 .UNSPECIFIED., .F., .F.,
 ( 4, 4 ),
 ( 0.003785693138453205195, 0.004021000868919195545 ),
 .UNSPECIFIED. ) ;
#19181=AXIS2_PLACEMENT_3D ( 'NONE', #29212, #85022, #97294 ) ;
#19225=ORIENTED_EDGE ( 'NONE', *, *, #13663, .F. ) ;
#19233=CARTESIAN_POINT ( 'NONE',  ( 4.495848767239241539, 4.584330080086930965E-16, 0.000000000000000000 ) ) ;
#19249=CARTESIAN_POINT ( 'NONE',  ( -12.69999999999998153, 0.000000000000000000, 2.500000000000000444 ) ) ;
#19259=CARTESIAN_POINT ( 'NONE',  ( 7.326124847093153925, 4.202752102959690472E-16, 0.000000000000000000 ) ) ;
#19275=VERTEX_POINT ( 'NONE', #86792 ) ;
#19277=CARTESIAN_POINT ( 'NONE',  ( 10.94186803553636977, 3.821174125832445049E-16, 0.000000000000000000 ) ) ;
#19290=EDGE_CURVE ( 'NONE', #5092, #63283, #30993, .T. ) ;
#19302=CARTESIAN_POINT ( 'NONE',  ( 1.042387978378689573, 0.3999999999999995781, 2.015694669338588429 ) ) ;
#19334=ORIENTED_EDGE ( 'NONE', *, *, #79856, .T. ) ;
#19336=DIRECTION ( 'NONE',  ( -1.000000000000000000, -0.000000000000000000, -0.000000000000000000 ) ) ;
#19351=AXIS2_PLACEMENT_3D ( 'NONE', #82429, #5548, #27304 ) ;
#19361=LINE ( 'NONE', #63613, #58397 ) ;
#19364=CARTESIAN_POINT ( 'NONE',  ( 0.000000000000000000, -0.4000000000000003553, 2.015694669338588429 ) ) ;
#19365=EDGE_LOOP ( 'NONE', ( #113951, #13083, #125780, #48250 ) ) ;
#19369=AXIS2_PLACEMENT_3D ( 'NONE', #33965, #9285, #42707 ) ;
#19432=ORIENTED_EDGE ( 'NONE', *, *, #96006, .T. ) ;
#19461=LINE ( 'NONE', #7114, #122805 ) ;
#19486=EDGE_CURVE ( 'NONE', #96111, #5701, #109718, .T. ) ;
#19509=VERTEX_POINT ( 'NONE', #77878 ) ;
#19525=VERTEX_POINT ( 'NONE', #32975 ) ;
#19554=VERTEX_POINT ( 'NONE', #69155 ) ;
#19592=ORIENTED_EDGE ( 'NONE', *, *, #60935, .F. ) ;
#19600=FACE_OUTER_BOUND ( 'NONE', #47956, .T. ) ;
#19614=EDGE_CURVE ( 'NONE', #82511, #11616, #83608, .T. ) ;
#19619=DIRECTION ( 'NONE',  ( 1.000000000000000000, 1.224606353822377258E-16, 0.000000000000000000 ) ) ;
#19633=ORIENTED_EDGE ( 'NONE', *, *, #58918, .F. ) ;
#19657=CARTESIAN_POINT ( 'NONE',  ( 19.89359858452208130, 4.202752102959690472E-16, 0.000000000000000000 ) ) ;
#19675=LINE ( 'NONE', #53761, #110996 ) ;
#19684=ORIENTED_EDGE ( 'NONE', *, *, #27489, .T. ) ;
#19710=DIRECTION ( 'NONE',  ( 0.000000000000000000, -1.000000000000000000, 0.000000000000000000 ) ) ;
#19760=DIRECTION ( 'NONE',  ( 0.000000000000000000, -1.000000000000000000, 0.000000000000000000 ) ) ;
#19769=VERTEX_POINT ( 'NONE', #40800 ) ;
#19771=CARTESIAN_POINT ( 'NONE',  ( 25.00000000000000000, 1.749999999999999778, 0.000000000000000000 ) ) ;
#19788=ADVANCED_FACE ( 'NONE', ( #136896 ), #91230, .T. ) ;
#19841=AXIS2_PLACEMENT_3D ( 'NONE', #38743, #72128, #132194 ) ;
#19919=ORIENTED_EDGE ( 'NONE', *, *, #137486, .F. ) ;
#19926=DIRECTION ( 'NONE',  ( -1.000000000000000000, -1.224606353822377258E-16, -0.000000000000000000 ) ) ;
#19944=ORIENTED_EDGE ( 'NONE', *, *, #118294, .F. ) ;
#19948=CARTESIAN_POINT ( 'NONE',  ( 1.516262732464673579, -0.3999999999999997446, -2.467792535850613866 ) ) ;
#19963=DIRECTION ( 'NONE',  ( 0.000000000000000000, -1.000000000000000000, 0.000000000000000000 ) ) ;
#19994=DIRECTION ( 'NONE',  ( -1.000000000000000000, -1.224606353822377258E-16, -0.000000000000000000 ) ) ;
#20032=VECTOR ( 'NONE', #104722, 999.9999999999998863 ) ;
#20038=ORIENTED_EDGE ( 'NONE', *, *, #70056, .F. ) ;
#20054=CARTESIAN_POINT ( 'NONE',  ( 0.5685132242927012358, 0.4000000000000001887, -2.467792535850613866 ) ) ;
#20077=ADVANCED_FACE ( 'NONE', ( #83234 ), #49911, .T. ) ;
#20099=CARTESIAN_POINT ( 'NONE',  ( 9.208651418775088970, 2.500000000000000888, 0.000000000000000000 ) ) ;
#20110=CYLINDRICAL_SURFACE ( 'NONE', #129043, 2.500000000000000444 ) ;
#20142=AXIS2_PLACEMENT_3D ( 'NONE', #133208, #78813, #101261 ) ;
#20155=CARTESIAN_POINT ( 'NONE',  ( 3.710381658649934078, -2.500000000000000000, 3.061616997868383634E-16 ) ) ;
#20171=CIRCLE ( 'NONE', #47958, 2.055000000000000604 ) ;
#20200=EDGE_CURVE ( 'NONE', #125896, #64781, #120839, .T. ) ;
#20222=VERTEX_POINT ( 'NONE', #133180 ) ;
#20229=ORIENTED_EDGE ( 'NONE', *, *, #49999, .T. ) ;
#20348=DIRECTION ( 'NONE',  ( -1.000000000000000000, -1.224606353822377258E-16, -0.000000000000000000 ) ) ;
#20364=CARTESIAN_POINT ( 'NONE',  ( 17.53719725875415847, -2.055000000000000160, 0.000000000000000000 ) ) ;
#20419=DIRECTION ( 'NONE',  ( -1.000000000000000000, -1.224606353822377258E-16, -0.000000000000000000 ) ) ;
#20450=LINE ( 'NONE', #9566, #64739 ) ;
#20505=CARTESIAN_POINT ( 'NONE',  ( -12.69999999999998153, 0.000000000000000000, 0.000000000000000000 ) ) ;
#20506=ORIENTED_EDGE ( 'NONE', *, *, #129606, .T. ) ;
#20513=B_SPLINE_CURVE_WITH_KNOTS ( 'NONE', 3,
 ( #108404, #21450, #120003, #131645 ),
 .UNSPECIFIED., .F., .F.,
 ( 4, 4 ),
 ( 0.008519363277820954025, 0.008755597426397561736 ),
 .UNSPECIFIED. ) ;
#20527=LINE ( 'NONE', #51775, #60538 ) ;
#20528=ADVANCED_FACE ( 'NONE', ( #120661 ), #106152, .T. ) ;
#20531=CARTESIAN_POINT ( 'NONE',  ( 6.066782984417857350, 4.584330080086930965E-16, 0.000000000000000000 ) ) ;
#20575=CARTESIAN_POINT ( 'NONE',  ( 16.44013779566152778, 2.499999999999998224, 3.061616997868380183E-16 ) ) ;
#20590=VECTOR ( 'NONE', #92318, 1000.000000000000000 ) ;
#20608=EDGE_LOOP ( 'NONE', ( #140635, #95346, #87197, #25133, #131366 ) ) ;
#20640=AXIS2_PLACEMENT_3D ( 'NONE', #137578, #91242, #79678 ) ;
#20660=CONICAL_SURFACE ( 'NONE', #101702, 2.500000000000000444, 0.9599310885968830309 ) ;
#20683=CARTESIAN_POINT ( 'NONE',  ( 0.2569208697893813897, 0.3999999999999995781, 2.015694669338588429 ) ) ;
#20685=DIRECTION ( 'NONE',  ( -0.5735764363510499342, -0.8191520442889891340, 0.000000000000000000 ) ) ;
#20690=DIRECTION ( 'NONE',  ( -1.000000000000000000, -1.224606353822377258E-16, -0.000000000000000000 ) ) ;
#20714=CARTESIAN_POINT ( 'NONE',  ( 0.1161069444170879233, -2.256103126841972450, 0.000000000000000000 ) ) ;
#20727=EDGE_LOOP ( 'NONE', ( #61146, #115564, #60193, #46760, #60390, #55987 ) ) ;
#20784=AXIS2_PLACEMENT_3D ( 'NONE', #76998, #102309, #2955 ) ;
#20794=EDGE_CURVE ( 'NONE', #78146, #98048, #59739, .T. ) ;
#20795=CARTESIAN_POINT ( 'NONE',  ( 0.07735795229993543132, 0.4000000000000001332, -2.152165010376131171 ) ) ;
#20836=CARTESIAN_POINT ( 'NONE',  ( 11.72733514412567857, 3.821174125832445049E-16, 0.000000000000000000 ) ) ;
#20849=VERTEX_POINT ( 'NONE', #3854 ) ;
#20902=CARTESIAN_POINT ( 'NONE',  ( 4.495848767239241539, 4.584330080086930965E-16, 0.000000000000000000 ) ) ;
#20921=CARTESIAN_POINT ( 'NONE',  ( 16.27785539607886633, 3.061616997868383634E-16, -2.500000000000000444 ) ) ;
#20930=VECTOR ( 'NONE', #101811, 1000.000000000000000 ) ;
#20935=DIRECTION ( 'NONE',  ( 1.000000000000000000, 1.224606353822377258E-16, 0.000000000000000000 ) ) ;
#21000=( NAMED_UNIT ( * ) SI_UNIT ( $, .STERADIAN. ) SOLID_ANGLE_UNIT ( ) );
#21006=ORIENTED_EDGE ( 'NONE', *, *, #10496, .F. ) ;
#21030=CARTESIAN_POINT ( 'NONE',  ( 13.13598696172163116, 4.584330080086930965E-16, 0.000000000000000000 ) ) ;
#21043=AXIS2_PLACEMENT_3D ( 'NONE', #120777, #54840, #110598 ) ;
#21054=CIRCLE ( 'NONE', #111286, 2.500000000000000444 ) ;
#21056=DIRECTION ( 'NONE',  ( 0.000000000000000000, -1.000000000000000000, 0.000000000000000000 ) ) ;
#21074=DIRECTION ( 'NONE',  ( 0.000000000000000000, -1.000000000000000000, 0.000000000000000000 ) ) ;
#21082=CARTESIAN_POINT ( 'NONE',  ( 11.25346039003969523, 4.202752102959690472E-16, 0.000000000000000000 ) ) ;
#21116=DIRECTION ( 'NONE',  ( -1.000000000000000000, -1.224606353822377258E-16, -0.000000000000000000 ) ) ;
#21144=CARTESIAN_POINT ( 'NONE',  ( 15.65467068707222076, 3.821174125832445049E-16, 0.000000000000000000 ) ) ;
#21174=EDGE_LOOP ( 'NONE', ( #23272, #118060, #1542, #89281, #19592 ) ) ;
#21182=DIRECTION ( 'NONE',  ( -0.5735764363510501562, 0.8191520442889890230, 1.003171929053521419E-16 ) ) ;
#21220=ADVANCED_FACE ( 'NONE', ( #121215 ), #2148, .T. ) ;
#21237=CARTESIAN_POINT ( 'NONE',  ( -12.69999999999998153, 0.000000000000000000, 0.000000000000000000 ) ) ;
#21261=AXIS2_PLACEMENT_3D ( 'NONE', #75223, #119385, #141908 ) ;
#21279=DIRECTION ( 'NONE',  ( 1.000000000000000000, 1.224606353822377258E-16, 0.000000000000000000 ) ) ;
#21283=DIRECTION ( 'NONE',  ( 0.000000000000000000, -1.000000000000000000, 0.000000000000000000 ) ) ;
#21289=ADVANCED_FACE ( 'NONE', ( #42733 ), #74011, .T. ) ;
#21320=ORIENTED_EDGE ( 'NONE', *, *, #94026, .F. ) ;
#21437=CONICAL_SURFACE ( 'NONE', #127933, 2.055000000000000604, 0.9599310885968764806 ) ;
#21450=CARTESIAN_POINT ( 'NONE',  ( 0.03865117921958875769, -0.3999999999999998002, -2.083945894980139268 ) ) ;
#21468=ORIENTED_EDGE ( 'NONE', *, *, #80186, .T. ) ;
#21475=CIRCLE ( 'NONE', #91130, 2.500000000000000444 ) ;
#21491=DIRECTION ( 'NONE',  ( 1.301042606982605074E-16, -1.000000000000000000, 0.000000000000000000 ) ) ;
#21530=CONICAL_SURFACE ( 'NONE', #28480, 2.500000000000000444, 0.9599310885968830309 ) ;
#21532=DIRECTION ( 'NONE',  ( 0.000000000000000000, 1.000000000000000000, 0.000000000000000000 ) ) ;
#21549=ORIENTED_EDGE ( 'NONE', *, *, #129668, .T. ) ;
#21550=EDGE_CURVE ( 'NONE', #54699, #103560, #47352, .T. ) ;
#21568=AXIS2_PLACEMENT_3D ( 'NONE', #130482, #84814, #118864 ) ;
#21573=CARTESIAN_POINT ( 'NONE',  ( 14.70692117890024697, 2.500000000000000888, 0.000000000000000000 ) ) ;
#21591=EDGE_CURVE ( 'NONE', #79754, #51035, #64211, .T. ) ;
#21639=CARTESIAN_POINT ( 'NONE',  ( 13.29826936130429260, 3.821174125832445049E-16, 0.000000000000000000 ) ) ;
#21677=ORIENTED_EDGE ( 'NONE', *, *, #51529, .F. ) ;
#21678=DIRECTION ( 'NONE',  ( 0.000000000000000000, -1.000000000000000000, 0.000000000000000000 ) ) ;
#21704=EDGE_CURVE ( 'NONE', #137282, #130467, #85265, .T. ) ;
#21717=CIRCLE ( 'NONE', #70411, 2.055000000000000604 ) ;
#21761=DIRECTION ( 'NONE',  ( -1.000000000000000000, -0.000000000000000000, -0.000000000000000000 ) ) ;
#21807=FACE_OUTER_BOUND ( 'NONE', #82486, .T. ) ;
#21813=ORIENTED_EDGE ( 'NONE', *, *, #2202, .F. ) ;
#21831=VERTEX_POINT ( 'NONE', #14079 ) ;
#21862=DIRECTION ( 'NONE',  ( 0.000000000000000000, -1.000000000000000000, 0.000000000000000000 ) ) ;
#21881=AXIS2_PLACEMENT_3D ( 'NONE', #26778, #47863, #13735 ) ;
#21908=DIRECTION ( 'NONE',  ( 0.000000000000000000, -1.000000000000000000, 0.000000000000000000 ) ) ;
#21909=DIRECTION ( 'NONE',  ( 0.000000000000000000, 1.000000000000000000, 0.000000000000000000 ) ) ;
#21932=ORIENTED_EDGE ( 'NONE', *, *, #15821, .T. ) ;
#21941=CARTESIAN_POINT ( 'NONE',  ( 17.84878961325748037, 4.584330080086930965E-16, 0.000000000000000000 ) ) ;
#21962=ORIENTED_EDGE ( 'NONE', *, *, #28723, .T. ) ;
#22010=DIRECTION ( 'NONE',  ( -1.000000000000000000, -0.000000000000000000, -0.000000000000000000 ) ) ;
#22037=ORIENTED_EDGE ( 'NONE', *, *, #52077, .T. ) ;
#22101=DIRECTION ( 'NONE',  ( -1.000000000000000000, -1.224606353822377258E-16, -0.000000000000000000 ) ) ;
#22126=DIRECTION ( 'NONE',  ( -1.000000000000000000, -1.224606353822377258E-16, -0.000000000000000000 ) ) ;
#22242=EDGE_CURVE ( 'NONE', #29201, #121119, #36401, .T. ) ;
#22254=DIRECTION ( 'NONE',  ( 1.000000000000000000, 1.224606353822377258E-16, 0.000000000000000000 ) ) ;
#22267=DIRECTION ( 'NONE',  ( 0.000000000000000000, 1.000000000000000000, 0.000000000000000000 ) ) ;
#22291=CARTESIAN_POINT ( 'NONE',  ( 6.540657738503846907, 4.202752102959690472E-16, 0.000000000000000000 ) ) ;
#22305=DIRECTION ( 'NONE',  ( 0.000000000000000000, 0.000000000000000000, 1.000000000000000000 ) ) ;
#22418=ORIENTED_EDGE ( 'NONE', *, *, #102075, .T. ) ;
#22440=EDGE_CURVE ( 'NONE', #87797, #71583, #27947, .T. ) ;
#22460=CIRCLE ( 'NONE', #15511, 2.500000000000000444 ) ;
#22488=VERTEX_POINT ( 'NONE', #10868 ) ;
#22491=EDGE_LOOP ( 'NONE', ( #62485, #96850, #66413, #19944, #93711 ) ) ;
#22512=ORIENTED_EDGE ( 'NONE', *, *, #65951, .T. ) ;
#22517=CARTESIAN_POINT ( 'NONE',  ( 6.066782984417857350, 4.584330080086930965E-16, 0.000000000000000000 ) ) ;
#22524=ORIENTED_EDGE ( 'NONE', *, *, #40272, .T. ) ;
#22530=AXIS2_PLACEMENT_3D ( 'NONE', #141715, #130855, #31520 ) ;
#22584=DIRECTION ( 'NONE',  ( 0.000000000000000000, -1.000000000000000000, 0.000000000000000000 ) ) ;
#22588=DIRECTION ( 'NONE',  ( -1.000000000000000000, -1.224606353822377258E-16, -0.000000000000000000 ) ) ;
#22594=APPLICATION_CONTEXT ( 'automotive_design' ) ;
#22652=ORIENTED_EDGE ( 'NONE', *, *, #30985, .F. ) ;
#22696=AXIS2_PLACEMENT_3D ( 'NONE', #9149, #30235, #63619 ) ;
#22723=ORIENTED_EDGE ( 'NONE', *, *, #86269, .F. ) ;
#22757=VERTEX_POINT ( 'NONE', #60885 ) ;
#22770=UNCERTAINTY_MEASURE_WITH_UNIT (LENGTH_MEASURE( 1.000000000000000082E-05 ), #123847, 'distance_accuracy_value', 'NONE');
#22783=AXIS2_PLACEMENT_3D ( 'NONE', #118663, #107769, #75196 ) ;
#22815=EDGE_CURVE ( 'NONE', #117989, #120212, #32500, .T. ) ;
#22872=VERTEX_POINT ( 'NONE', #54971 ) ;
#22895=ORIENTED_EDGE ( 'NONE', *, *, #135225, .F. ) ;
#22906=EDGE_CURVE ( 'NONE', #52143, #46122, #33246, .T. ) ;
#22932=AXIS2_PLACEMENT_3D ( 'NONE', #28024, #128069, #84562 ) ;
#22956=B_SPLINE_CURVE_WITH_KNOTS ( 'NONE', 3,
 ( #133668, #13278, #45961, #101016 ),
 .UNSPECIFIED., .F., .F.,
 ( 4, 4 ),
 ( 0.003609336753060590763, 0.003809496093231039965 ),
 .UNSPECIFIED. ) ;
#22962=EDGE_CURVE ( 'NONE', #127065, #104418, #31350, .T. ) ;
#22978=CARTESIAN_POINT ( 'NONE',  ( 7.637717201596474048, 4.584330080086930965E-16, 0.000000000000000000 ) ) ;
#22991=CARTESIAN_POINT ( 'NONE',  ( 7.326124847093153925, 4.202752102959690472E-16, 0.000000000000000000 ) ) ;
#23017=AXIS2_PLACEMENT_3D ( 'NONE', #39402, #17606, #140143 ) ;
#23044=DIRECTION ( 'NONE',  ( -0.000000000000000000, 0.000000000000000000, 1.000000000000000000 ) ) ;
#23052=CARTESIAN_POINT ( 'NONE',  ( 10.77958563595370833, 3.061616997868383634E-16, -2.500000000000000444 ) ) ;
#23059=DIRECTION ( 'NONE',  ( 0.000000000000000000, 1.000000000000000000, 0.000000000000000000 ) ) ;
#23071=ORIENTED_EDGE ( 'NONE', *, *, #98556, .T. ) ;
#23090=ORIENTED_EDGE ( 'NONE', *, *, #141689, .F. ) ;
#23171=ORIENTED_EDGE ( 'NONE', *, *, #63981, .F. ) ;
#23187=DIRECTION ( 'NONE',  ( 0.000000000000000000, 1.301042606982605074E-16, -1.000000000000000000 ) ) ;
#23212=VECTOR ( 'NONE', #82120, 1000.000000000000000 ) ;
#23239=CARTESIAN_POINT ( 'NONE',  ( 6.066782984417857350, 3.061616997868382648E-16, -2.500000000000000444 ) ) ;
#23268=DIRECTION ( 'NONE',  ( -1.000000000000000000, -1.224606353822377258E-16, -0.000000000000000000 ) ) ;
#23269=DIRECTION ( 'NONE',  ( 2.110369192185896011E-16, -1.000000000000000000, 0.000000000000000000 ) ) ;
#23272=ORIENTED_EDGE ( 'NONE', *, *, #14416, .F. ) ;
#23310=CARTESIAN_POINT ( 'NONE',  ( 15.65467068707222076, 3.061616997868383634E-16, -2.500000000000000444 ) ) ;
#23321=CARTESIAN_POINT ( 'NONE',  ( 15.49238828748955576, 4.584330080086930965E-16, 0.000000000000000000 ) ) ;
#23326=CONICAL_SURFACE ( 'NONE', #127561, 2.055000000000000604, 0.9599310885968764806 ) ;
#23345=LINE ( 'NONE', #67618, #46614 ) ;
#23362=EDGE_CURVE ( 'NONE', #122791, #31140, #18822, .T. ) ;
#23392=LINE ( 'NONE', #109699, #140506 ) ;
#23411=ORIENTED_EDGE ( 'NONE', *, *, #134833, .T. ) ;
#23425=ADVANCED_FACE ( 'NONE', ( #92944 ), #125328, .T. ) ;
#23449=EDGE_LOOP ( 'NONE', ( #79154, #66222, #64491, #68703, #25856 ) ) ;
#23453=VERTEX_POINT ( 'NONE', #95067 ) ;
#23456=CIRCLE ( 'NONE', #104482, 2.500000000000000444 ) ;
#23465=DIRECTION ( 'NONE',  ( 0.000000000000000000, 0.000000000000000000, 1.000000000000000000 ) ) ;
#23507=EDGE_CURVE ( 'NONE', #67994, #123638, #117522, .T. ) ;
#23518=CARTESIAN_POINT ( 'NONE',  ( 22.25000000000000000, 0.000000000000000000, 0.000000000000000000 ) ) ;
#23523=CARTESIAN_POINT ( 'NONE',  ( 12.51280225271498736, -2.499999999999999112, 0.000000000000000000 ) ) ;
#23548=ADVANCED_FACE ( 'NONE', ( #21807 ), #129985, .T. ) ;
#23563=LINE ( 'NONE', #67831, #93237 ) ;
#23586=AXIS2_PLACEMENT_3D ( 'NONE', #32205, #130829, #63438 ) ;
#23630=DIRECTION ( 'NONE',  ( -1.000000000000000000, -1.224606353822377258E-16, -0.000000000000000000 ) ) ;
#23662=DIRECTION ( 'NONE',  ( -1.000000000000000000, -1.224606353822377258E-16, -0.000000000000000000 ) ) ;
#23668=DIRECTION ( 'NONE',  ( 0.000000000000000000, 0.000000000000000000, 1.000000000000000000 ) ) ;
#23741=CARTESIAN_POINT ( 'NONE',  ( 0.1161069444170876042, 0.3999999999999995781, 2.220360628129161906 ) ) ;
#23744=VERTEX_POINT ( 'NONE', #92754 ) ;
#23747=ORIENTED_EDGE ( 'NONE', *, *, #25486, .F. ) ;
#23775=ORIENTED_EDGE ( 'NONE', *, *, #31725, .T. ) ;
#23831=VERTEX_POINT ( 'NONE', #58780 ) ;
#23865=CARTESIAN_POINT ( 'NONE',  ( 0.2569208697893817228, -2.055000000000000160, 0.000000000000000000 ) ) ;
#23890=DIRECTION ( 'NONE',  ( -1.000000000000000000, -1.224606353822377258E-16, -0.000000000000000000 ) ) ;
#23892=DIRECTION ( 'NONE',  ( -1.000000000000000000, -0.000000000000000000, -0.000000000000000000 ) ) ;
#23948=DIRECTION ( 'NONE',  ( -1.000000000000000000, -0.000000000000000000, -0.000000000000000000 ) ) ;
#23966=ORIENTED_EDGE ( 'NONE', *, *, #42956, .F. ) ;
#23971=AXIS2_PLACEMENT_3D ( 'NONE', #91918, #53795, #65395 ) ;
#24083=EDGE_CURVE ( 'NONE', #45596, #97154, #30551, .T. ) ;
#24107=DIRECTION ( 'NONE',  ( -1.000000000000000000, -0.000000000000000000, -0.000000000000000000 ) ) ;
#24121=DIRECTION ( 'NONE',  ( -1.734723475976806848E-16, 1.000000000000000000, 0.000000000000000000 ) ) ;
#24150=VERTEX_POINT ( 'NONE', #125957 ) ;
#24164=ADVANCED_FACE ( 'NONE', ( #14321 ), #25983, .T. ) ;
#24231=CARTESIAN_POINT ( 'NONE',  ( 1.146006882977912644, -0.4000000000000003553, 2.166563419957292513 ) ) ;
#24236=EDGE_CURVE ( 'NONE', #21831, #42023, #128790, .T. ) ;
#24265=CARTESIAN_POINT ( 'NONE',  ( 1.249915061292911078, 0.4000000000000001887, -2.317232259782045833 ) ) ;
#24289=EDGE_CURVE ( 'NONE', #31140, #109534, #83157, .T. ) ;
#24329=DIRECTION ( 'NONE',  ( 0.000000000000000000, -1.000000000000000000, 0.000000000000000000 ) ) ;
#24391=DIRECTION ( 'NONE',  ( 0.000000000000000000, -1.000000000000000000, 0.000000000000000000 ) ) ;
#24395=SURFACE_STYLE_USAGE ( .BOTH. , #46192 ) ;
#24406=EDGE_CURVE ( 'NONE', #103560, #74147, #121481, .T. ) ;
#24454=CARTESIAN_POINT ( 'NONE',  ( 17.84878961325748037, 2.500000000000000444, 0.000000000000000000 ) ) ;
#24475=VERTEX_POINT ( 'NONE', #78004 ) ;
#24498=AXIS2_PLACEMENT_3D ( 'NONE', #37512, #81747, #50515 ) ;
#24501=( NAMED_UNIT ( * ) PLANE_ANGLE_UNIT ( ) SI_UNIT ( $, .RADIAN. ) );
#24535=LINE ( 'NONE', #90523, #14147 ) ;
#24560=EDGE_CURVE ( 'NONE', #109980, #131513, #125648, .T. ) ;
#24601=VECTOR ( 'NONE', #98835, 1000.000000000000000 ) ;
#24616=CARTESIAN_POINT ( 'NONE',  ( 6.229065384000522343, 3.821174125832445049E-16, 0.000000000000000000 ) ) ;
#24638=DIRECTION ( 'NONE',  ( 0.000000000000000000, 0.000000000000000000, 1.000000000000000000 ) ) ;
#24657=DIRECTION ( 'NONE',  ( 0.000000000000000000, 0.000000000000000000, -1.000000000000000000 ) ) ;
#24677=ADVANCED_FACE ( 'NONE', ( #72150 ), #95276, .T. ) ;
#24684=CIRCLE ( 'NONE', #105686, 2.500000000000000444 ) ;
#24734=CARTESIAN_POINT ( 'NONE',  ( 14.39532882439692862, 4.202752102959690472E-16, 0.000000000000000000 ) ) ;
#24751=ORIENTED_EDGE ( 'NONE', *, *, #99589, .T. ) ;
#24756=CARTESIAN_POINT ( 'NONE',  ( -12.69999999999998153, 0.000000000000000000, 0.000000000000000000 ) ) ;
#24774=ORIENTED_EDGE ( 'NONE', *, *, #35547, .T. ) ;
#24785=EDGE_CURVE ( 'NONE', #23453, #93248, #118590, .T. ) ;
#24789=ORIENTED_EDGE ( 'NONE', *, *, #24560, .F. ) ;
#24810=DIRECTION ( 'NONE',  ( 0.5735764363510448272, -0.8191520442889927978, 1.003171929053526103E-16 ) ) ;
#24845=CIRCLE ( 'NONE', #96521, 2.500000000000000444 ) ;
#24883=CARTESIAN_POINT ( 'NONE',  ( 1.516262732464673135, 2.500000000000000888, 3.061616997868384127E-16 ) ) ;
#24887=DIRECTION ( 'NONE',  ( -1.000000000000000000, -0.000000000000000000, -0.000000000000000000 ) ) ;
#24931=AXIS2_PLACEMENT_3D ( 'NONE', #79508, #48246, #15570 ) ;
#24962=CARTESIAN_POINT ( 'NONE',  ( 15.49238828748955576, 4.584330080086930965E-16, 0.000000000000000000 ) ) ;
#24972=FACE_OUTER_BOUND ( 'NONE', #35502, .T. ) ;
#24975=CYLINDRICAL_SURFACE ( 'NONE', #14973, 2.500000000000000444 ) ;
#24976=EDGE_CURVE ( 'NONE', #101876, #109461, #83358, .T. ) ;
#25011=DIRECTION ( 'NONE',  ( 0.000000000000000000, -1.000000000000000000, 0.000000000000000000 ) ) ;
#25028=CARTESIAN_POINT ( 'NONE',  ( 0.2569208697893814453, 4.202752102959690472E-16, 0.000000000000000000 ) ) ;
#25082=EDGE_LOOP ( 'NONE', ( #82192, #118040, #4137, #6144, #70178, #59676 ) ) ;
#25098=LINE ( 'NONE', #57066, #36987 ) ;
#25103=VERTEX_POINT ( 'NONE', #127757 ) ;
#25133=ORIENTED_EDGE ( 'NONE', *, *, #47590, .F. ) ;
#25164=EDGE_CURVE ( 'NONE', #13056, #14650, #35965, .T. ) ;
#25183=DIRECTION ( 'NONE',  ( -8.673617379884034239E-17, 1.000000000000000000, 0.000000000000000000 ) ) ;
#25241=CARTESIAN_POINT ( 'NONE',  ( 2.139447441471317379, 4.584330080086930965E-16, 0.000000000000000000 ) ) ;
#25249=DIRECTION ( 'NONE',  ( 1.318980745116185161E-16, -1.000000000000000000, 0.000000000000000000 ) ) ;
#25322=DIRECTION ( 'NONE',  ( 0.000000000000000000, -1.000000000000000000, 0.000000000000000000 ) ) ;
#25330=ORIENTED_EDGE ( 'NONE', *, *, #102791, .T. ) ;
#25433=DIRECTION ( 'NONE',  ( 1.000000000000000000, 1.224606353822377258E-16, 0.000000000000000000 ) ) ;
#25438=FACE_OUTER_BOUND ( 'NONE', #76679, .T. ) ;
#25486=EDGE_CURVE ( 'NONE', #34286, #95435, #74523, .T. ) ;
#25493=VERTEX_POINT ( 'NONE', #85143 ) ;
#25520=ORIENTED_EDGE ( 'NONE', *, *, #48723, .T. ) ;
#25530=EDGE_CURVE ( 'NONE', #84085, #139503, #86096, .T. ) ;
#25533=DIRECTION ( 'NONE',  ( -1.000000000000000000, -1.224606353822377258E-16, -0.000000000000000000 ) ) ;
#25549=AXIS2_PLACEMENT_3D ( 'NONE', #5487, #133038, #32276 ) ;
#25581=ORIENTED_EDGE ( 'NONE', *, *, #17914, .T. ) ;
#25638=CARTESIAN_POINT ( 'NONE',  ( 3.710381658649933190, 2.500000000000000888, 0.000000000000000000 ) ) ;
#25671=ORIENTED_EDGE ( 'NONE', *, *, #137252, .F. ) ;
#25700=ORIENTED_EDGE ( 'NONE', *, *, #86457, .F. ) ;
#25719=DIRECTION ( 'NONE',  ( -1.000000000000000000, -1.224606353822377258E-16, -0.000000000000000000 ) ) ;
#25743=VECTOR ( 'NONE', #84599, 1000.000000000000000 ) ;
#25767=CARTESIAN_POINT ( 'NONE',  ( 12.35051985313232237, 4.584330080086930965E-16, 0.000000000000000000 ) ) ;
#25774=VECTOR ( 'NONE', #40653, 1000.000000000000000 ) ;
#25809=VERTEX_POINT ( 'NONE', #24883 ) ;
#25856=ORIENTED_EDGE ( 'NONE', *, *, #117775, .F. ) ;
#25874=DIRECTION ( 'NONE',  ( 0.000000000000000000, -1.000000000000000000, 0.000000000000000000 ) ) ;
#25893=CARTESIAN_POINT ( 'NONE',  ( 0.2569208697893813342, -0.4000000000000003553, 2.015694669338588429 ) ) ;
#25905=CARTESIAN_POINT ( 'NONE',  ( 3.087196949643289834, 3.061616997868383141E-16, -2.500000000000000444 ) ) ;
#25941=CARTESIAN_POINT ( 'NONE',  ( 16.75173015016484968, 2.055000000000001048, 0.000000000000000000 ) ) ;
#25955=AXIS2_PLACEMENT_3D ( 'NONE', #15772, #36169, #68810 ) ;
#25983=CONICAL_SURFACE ( 'NONE', #49083, 2.055000000000000604, 0.9599310885968764806 ) ;
#25995=AXIS2_PLACEMENT_3D ( 'NONE', #57256, #1381, #45668 ) ;
#26038=ORIENTED_EDGE ( 'NONE', *, *, #50281, .T. ) ;
#26105=CARTESIAN_POINT ( 'NONE',  ( 14.70692117890024697, -2.500000000000000000, 3.061616997868383634E-16 ) ) ;
#26151=DIRECTION ( 'NONE',  ( -1.000000000000000000, -0.000000000000000000, -0.000000000000000000 ) ) ;
#26198=ORIENTED_EDGE ( 'NONE', *, *, #73012, .T. ) ;
#26234=ORIENTED_EDGE ( 'NONE', *, *, #94022, .F. ) ;
#26257=CARTESIAN_POINT ( 'NONE',  ( 11.56505274454301357, 4.584330080086930965E-16, 0.000000000000000000 ) ) ;
#26270=CARTESIAN_POINT ( 'NONE',  ( 0.000000000000000000, 0.3999999999999995781, 2.015694669338588429 ) ) ;
#26275=ORIENTED_EDGE ( 'NONE', *, *, #131390, .T. ) ;
#26307=AXIS2_PLACEMENT_3D ( 'NONE', #65634, #109801, #55432 ) ;
#26321=ORIENTED_EDGE ( 'NONE', *, *, #14387, .F. ) ;
#26434=LINE ( 'NONE', #127905, #141606 ) ;
#26549=DIRECTION ( 'NONE',  ( 0.000000000000000000, -1.000000000000000000, 0.000000000000000000 ) ) ;
#26578=DIRECTION ( 'NONE',  ( 0.000000000000000000, -1.000000000000000000, 0.000000000000000000 ) ) ;
#26610=ADVANCED_FACE ( 'NONE', ( #14384 ), #55187, .T. ) ;
#26649=( NAMED_UNIT ( * ) SI_UNIT ( $, .STERADIAN. ) SOLID_ANGLE_UNIT ( ) );
#26651=EDGE_LOOP ( 'NONE', ( #125863, #47279, #36656, #65357, #127384, #138879 ) ) ;
#26684=CYLINDRICAL_SURFACE ( 'NONE', #72698, 2.500000000000000444 ) ;
#26689=DIRECTION ( 'NONE',  ( 1.000000000000000000, 1.224606353822377258E-16, 0.000000000000000000 ) ) ;
#26691=CARTESIAN_POINT ( 'NONE',  ( 17.22560490425083657, 2.499999999999998224, 3.061616997868380183E-16 ) ) ;
#26707=DIRECTION ( 'NONE',  ( 1.301042606982605074E-16, -1.000000000000000000, 0.000000000000000000 ) ) ;
#26761=ORIENTED_EDGE ( 'NONE', *, *, #65974, .T. ) ;
#26778=CARTESIAN_POINT ( 'NONE',  ( 2.924914550060625285, 4.584330080086930965E-16, 0.000000000000000000 ) ) ;
#26780=DIRECTION ( 'NONE',  ( -1.000000000000000000, -0.000000000000000000, -0.000000000000000000 ) ) ;
#26853=CARTESIAN_POINT ( 'NONE',  ( 0.7307956238753654521, 3.821174125832445049E-16, 0.000000000000000000 ) ) ;
#26863=EDGE_LOOP ( 'NONE', ( #111763, #100415, #110102, #87794, #33703, #39684 ) ) ;
#26864=ORIENTED_EDGE ( 'NONE', *, *, #69656, .F. ) ;
#26873=DIRECTION ( 'NONE',  ( -1.000000000000000000, -0.000000000000000000, -0.000000000000000000 ) ) ;
#26888=VERTEX_POINT ( 'NONE', #14747 ) ;
#26911=ORIENTED_EDGE ( 'NONE', *, *, #83712, .T. ) ;
#26928=ORIENTED_EDGE ( 'NONE', *, *, #52021, .T. ) ;
#26930=EDGE_LOOP ( 'NONE', ( #134686, #138763, #19684, #13476, #34313, #25700 ) ) ;
#26944=EDGE_CURVE ( 'NONE', #84629, #115093, #62544, .T. ) ;
#27106=CARTESIAN_POINT ( 'NONE',  ( 0.1161069444170889225, -0.4000000000000003553, 2.220360628129160130 ) ) ;
#27115=CARTESIAN_POINT ( 'NONE',  ( 7.637717201596474048, 3.061616997868383634E-16, -2.500000000000000444 ) ) ;
#27133=DIRECTION ( 'NONE',  ( -0.5735764363510501562, 0.8191520442889890230, 1.003171929053521419E-16 ) ) ;
#27160=ORIENTED_EDGE ( 'NONE', *, *, #114345, .F. ) ;
#27175=LINE ( 'NONE', #71420, #73740 ) ;
#27180=EDGE_LOOP ( 'NONE', ( #15051, #4526, #47385, #61463, #107086 ) ) ;
#27230=DIRECTION ( 'NONE',  ( 0.000000000000000000, -1.000000000000000000, 0.000000000000000000 ) ) ;
#27276=ORIENTED_EDGE ( 'NONE', *, *, #14799, .F. ) ;
#27291=EDGE_CURVE ( 'NONE', #40629, #34286, #115673, .T. ) ;
#27304=DIRECTION ( 'NONE',  ( 0.000000000000000000, -1.000000000000000000, 0.000000000000000000 ) ) ;
#27331=CARTESIAN_POINT ( 'NONE',  ( 12.35051985313232237, -2.500000000000000444, 3.061616997868384127E-16 ) ) ;
#27374=EDGE_CURVE ( 'NONE', #42523, #15565, #37172, .T. ) ;
#27378=FACE_OUTER_BOUND ( 'NONE', #11783, .T. ) ;
#27404=DIRECTION ( 'NONE',  ( 0.000000000000000000, -1.000000000000000000, 0.000000000000000000 ) ) ;
#27408=ORIENTED_EDGE ( 'NONE', *, *, #69462, .T. ) ;
#27446=DIRECTION ( 'NONE',  ( -1.000000000000000000, -1.224606353822377258E-16, -0.000000000000000000 ) ) ;
#27455=ADVANCED_FACE ( 'NONE', ( #137077 ), #70440, .T. ) ;
#27489=EDGE_CURVE ( 'NONE', #78997, #26888, #42061, .T. ) ;
#27546=DIRECTION ( 'NONE',  ( 1.000000000000000000, 1.224606353822377258E-16, 0.000000000000000000 ) ) ;
#27581=CARTESIAN_POINT ( 'NONE',  ( 10.77958563595370833, 0.000000000000000000, 2.500000000000000444 ) ) ;
#27624=CARTESIAN_POINT ( 'NONE',  ( 18.32266436734346726, 4.202752102959690472E-16, 0.000000000000000000 ) ) ;
#27626=CARTESIAN_POINT ( 'NONE',  ( 18.32266436734346726, 4.202752102959690472E-16, 0.000000000000000000 ) ) ;
#27651=ORIENTED_EDGE ( 'NONE', *, *, #74258, .T. ) ;
#27658=CARTESIAN_POINT ( 'NONE',  ( 18.32266436734346726, 4.202752102959690472E-16, 0.000000000000000000 ) ) ;
#27688=EDGE_CURVE ( 'NONE', #10245, #52878, #111574, .T. ) ;
#27701=EDGE_LOOP ( 'NONE', ( #140740, #57063, #30762, #92783, #107120 ) ) ;
#27711=EDGE_CURVE ( 'NONE', #43404, #116730, #88421, .T. ) ;
#27731=ORIENTED_EDGE ( 'NONE', *, *, #69478, .T. ) ;
#27734=VERTEX_POINT ( 'NONE', #33351 ) ;
#27750=CARTESIAN_POINT ( 'NONE',  ( 11.56505274454301357, 4.584330080086930965E-16, 0.000000000000000000 ) ) ;
#27759=DIRECTION ( 'NONE',  ( 0.000000000000000000, -1.000000000000000000, 0.000000000000000000 ) ) ;
#27797=EDGE_LOOP ( 'NONE', ( #72271, #53401, #40955, #82930, #18978 ) ) ;
#27854=ORIENTED_EDGE ( 'NONE', *, *, #47148, .F. ) ;
#27877=ORIENTED_EDGE ( 'NONE', *, *, #141182, .F. ) ;
#27885=VECTOR ( 'NONE', #11087, 999.9999999999998863 ) ;
#27894=CONICAL_SURFACE ( 'NONE', #11950, 2.055000000000000604, 0.9599310885968764806 ) ;
#27947=CIRCLE ( 'NONE', #6996, 2.500000000000000444 ) ;
#27964=DIRECTION ( 'NONE',  ( 0.000000000000000000, -1.000000000000000000, 0.000000000000000000 ) ) ;
#27978=DIRECTION ( 'NONE',  ( 0.000000000000000000, -1.000000000000000000, 0.000000000000000000 ) ) ;
#27995=DIRECTION ( 'NONE',  ( 0.000000000000000000, -1.000000000000000000, 0.000000000000000000 ) ) ;
#28007=ORIENTED_EDGE ( 'NONE', *, *, #63553, .T. ) ;
#28011=ORIENTED_EDGE ( 'NONE', *, *, #35662, .F. ) ;
#28024=CARTESIAN_POINT ( 'NONE',  ( 21.46453280170069888, 4.202752102959690472E-16, 0.000000000000000000 ) ) ;
#28032=CIRCLE ( 'NONE', #85862, 2.500000000000000444 ) ;
#28055=AXIS2_PLACEMENT_3D ( 'NONE', #117898, #96159, #120781 ) ;
#28063=DIRECTION ( 'NONE',  ( 0.000000000000000000, 1.000000000000000000, 0.000000000000000000 ) ) ;
#28069=VECTOR ( 'NONE', #23892, 1000.000000000000000 ) ;
#28088=VECTOR ( 'NONE', #122054, 999.9999999999998863 ) ;
#28116=DIRECTION ( 'NONE',  ( -1.000000000000000000, -0.000000000000000000, -0.000000000000000000 ) ) ;
#28135=ORIENTED_EDGE ( 'NONE', *, *, #135299, .T. ) ;
#28141=DIRECTION ( 'NONE',  ( -1.000000000000000000, 0.000000000000000000, -0.000000000000000000 ) ) ;
#28174=ORIENTED_EDGE ( 'NONE', *, *, #143347, .T. ) ;
#28196=AXIS2_PLACEMENT_3D ( 'NONE', #109603, #98031, #131368 ) ;
#28207=VECTOR ( 'NONE', #102742, 999.9999999999998863 ) ;
#28242=DIRECTION ( 'NONE',  ( 1.000000000000000000, 1.224606353822377258E-16, 0.000000000000000000 ) ) ;
#28281=DIRECTION ( 'NONE',  ( -0.5735764363510499342, -0.8191520442889891340, 0.000000000000000000 ) ) ;
#28320=DIRECTION ( 'NONE',  ( -1.000000000000000000, -0.000000000000000000, -0.000000000000000000 ) ) ;
#28328=CARTESIAN_POINT ( 'NONE',  ( 20.67906569311139009, 2.055000000000001048, 2.516649172247811554E-16 ) ) ;
#28359=CARTESIAN_POINT ( 'NONE',  ( 16.27785539607886633, 4.584330080086930965E-16, 0.000000000000000000 ) ) ;
#28365=CARTESIAN_POINT ( 'NONE',  ( 1.353980332882009252, 4.584330080086930965E-16, 0.000000000000000000 ) ) ;
#28375=FACE_OUTER_BOUND ( 'NONE', #101865, .T. ) ;
#28387=DIRECTION ( 'NONE',  ( -1.000000000000000000, -1.224606353822377258E-16, -0.000000000000000000 ) ) ;
#28398=DIRECTION ( 'NONE',  ( -1.000000000000000000, -1.224606353822377258E-16, -0.000000000000000000 ) ) ;
#28426=FACE_OUTER_BOUND ( 'NONE', #141867, .T. ) ;
#28435=DIRECTION ( 'NONE',  ( -1.000000000000000000, -1.224606353822377258E-16, -0.000000000000000000 ) ) ;
#28436=EDGE_CURVE ( 'NONE', #61275, #10245, #72195, .T. ) ;
#28451=FACE_OUTER_BOUND ( 'NONE', #59411, .T. ) ;
#28480=AXIS2_PLACEMENT_3D ( 'NONE', #47513, #3222, #114821 ) ;
#28484=DIRECTION ( 'NONE',  ( -1.000000000000000000, -0.000000000000000000, -0.000000000000000000 ) ) ;
#28519=VECTOR ( 'NONE', #118308, 1000.000000000000000 ) ;
#28528=CARTESIAN_POINT ( 'NONE',  ( 19.10813147593277250, 4.202752102959690472E-16, 0.000000000000000000 ) ) ;
#28608=EDGE_CURVE ( 'NONE', #73287, #86117, #107313, .T. ) ;
#28611=VERTEX_POINT ( 'NONE', #29738 ) ;
#28626=CIRCLE ( 'NONE', #21568, 2.500000000000000444 ) ;
#28631=CARTESIAN_POINT ( 'NONE',  ( 0.000000000000000000, 0.000000000000000000, 0.000000000000000000 ) ) ;
#28667=DIRECTION ( 'NONE',  ( -1.000000000000000000, -1.224606353822377258E-16, -0.000000000000000000 ) ) ;
#28701=ADVANCED_FACE ( 'NONE', ( #42090 ), #95212, .T. ) ;
#28723=EDGE_CURVE ( 'NONE', #47408, #117065, #75421, .T. ) ;
#28782=EDGE_CURVE ( 'NONE', #117931, #102793, #44976, .T. ) ;
#28788=EDGE_CURVE ( 'NONE', #60360, #10019, #34065, .T. ) ;
#28790=FACE_OUTER_BOUND ( 'NONE', #27180, .T. ) ;
#28821=ORIENTED_EDGE ( 'NONE', *, *, #80867, .T. ) ;
#28828=EDGE_LOOP ( 'NONE', ( #108767, #111100, #128280, #45826, #6606, #109454 ) ) ;
#28893=DIRECTION ( 'NONE',  ( 0.000000000000000000, -1.000000000000000000, 0.000000000000000000 ) ) ;
#28923=DIRECTION ( 'NONE',  ( -1.000000000000000000, -1.224606353822377258E-16, -0.000000000000000000 ) ) ;
#28984=DIRECTION ( 'NONE',  ( -1.000000000000000000, -1.224606353822377258E-16, -0.000000000000000000 ) ) ;
#29055=CARTESIAN_POINT ( 'NONE',  ( 4.969723521325230209, -2.055000000000000160, 0.000000000000000000 ) ) ;
#29082=ORIENTED_EDGE ( 'NONE', *, *, #82507, .T. ) ;
#29109=EDGE_LOOP ( 'NONE', ( #124401, #25581, #27731, #135144, #122577 ) ) ;
#29111=EDGE_CURVE ( 'NONE', #11920, #72701, #42258, .T. ) ;
#29131=DIRECTION ( 'NONE',  ( -1.000000000000000000, -1.224606353822377258E-16, -0.000000000000000000 ) ) ;
#29133=DIRECTION ( 'NONE',  ( 1.055184596092948005E-16, -1.000000000000000000, 0.000000000000000000 ) ) ;
#29140=PLANE ( 'NONE',  #14105 ) ;
#29155=ORIENTED_EDGE ( 'NONE', *, *, #78013, .F. ) ;
#29156=EDGE_CURVE ( 'NONE', #78146, #68546, #37499, .T. ) ;
#29159=AXIS2_PLACEMENT_3D ( 'NONE', #43219, #142532, #65718 ) ;
#29201=VERTEX_POINT ( 'NONE', #23310 ) ;
#29212=CARTESIAN_POINT ( 'NONE',  ( 10.94186803553636977, 3.821174125832445049E-16, 0.000000000000000000 ) ) ;
#29219=DIRECTION ( 'NONE',  ( 0.000000000000000000, -1.000000000000000000, 0.000000000000000000 ) ) ;
#29231=CARTESIAN_POINT ( 'NONE',  ( 9.994118527364397764, 4.584330080086930965E-16, 0.000000000000000000 ) ) ;
#29304=AXIS2_PLACEMENT_3D ( 'NONE', #130587, #142178, #120355 ) ;
#29319=ORIENTED_EDGE ( 'NONE', *, *, #84093, .F. ) ;
#29339=EDGE_LOOP ( 'NONE', ( #90565, #23411, #67983, #100894, #80237 ) ) ;
#29345=VERTEX_POINT ( 'NONE', #61702 ) ;
#29354=VECTOR ( 'NONE', #73171, 999.9999999999998863 ) ;
#29409=DIRECTION ( 'NONE',  ( -1.000000000000000000, -1.224606353822377258E-16, -0.000000000000000000 ) ) ;
#29415=CARTESIAN_POINT ( 'NONE',  ( 12.82439460721831104, -2.055000000000000160, 0.000000000000000000 ) ) ;
#29424=EDGE_CURVE ( 'NONE', #17542, #37203, #18125, .T. ) ;
#29448=AXIS2_PLACEMENT_3D ( 'NONE', #105086, #128285, #73201 ) ;
#29453=DIRECTION ( 'NONE',  ( -1.000000000000000000, -1.224606353822377258E-16, -0.000000000000000000 ) ) ;
#29496=ADVANCED_FACE ( 'NONE', ( #46392 ), #123295, .T. ) ;
#29499=DIRECTION ( 'NONE',  ( -1.000000000000000000, -1.224606353822377258E-16, -0.000000000000000000 ) ) ;
#29512=DIRECTION ( 'NONE',  ( -1.000000000000000000, -1.224606353822377258E-16, -0.000000000000000000 ) ) ;
#29532=ORIENTED_EDGE ( 'NONE', *, *, #4445, .T. ) ;
#29556=VERTEX_POINT ( 'NONE', #111605 ) ;
#29576=EDGE_CURVE ( 'NONE', #123638, #120212, #141811, .T. ) ;
#29587=EDGE_CURVE ( 'NONE', #94208, #83589, #49193, .T. ) ;
#29613=CARTESIAN_POINT ( 'NONE',  ( 7.637717201596474048, 4.584330080086930965E-16, 0.000000000000000000 ) ) ;
#29635=ORIENTED_EDGE ( 'NONE', *, *, #121073, .T. ) ;
#29672=ORIENTED_EDGE ( 'NONE', *, *, #99791, .T. ) ;
#29683=ORIENTED_EDGE ( 'NONE', *, *, #66553, .F. ) ;
#29705=ORIENTED_EDGE ( 'NONE', *, *, #53335, .T. ) ;
#29729=CARTESIAN_POINT ( 'NONE',  ( 12.03892749862900402, 4.202752102959690472E-16, 0.000000000000000000 ) ) ;
#29738=CARTESIAN_POINT ( 'NONE',  ( 9.682526172861077640, 2.055000000000001048, 0.000000000000000000 ) ) ;
#29766=LINE ( 'NONE', #63866, #83635 ) ;
#29793=DIRECTION ( 'NONE',  ( 0.000000000000000000, -1.000000000000000000, 0.000000000000000000 ) ) ;
#29808=EDGE_CURVE ( 'NONE', #52143, #47310, #67512, .T. ) ;
#29830=CARTESIAN_POINT ( 'NONE',  ( 1.042387978378689573, 4.202752102959690472E-16, 0.000000000000000000 ) ) ;
#29845=AXIS2_PLACEMENT_3D ( 'NONE', #49033, #136722, #37436 ) ;
#29873=CYLINDRICAL_SURFACE ( 'NONE', #117592, 2.500000000000000444 ) ;
#29916=ORIENTED_EDGE ( 'NONE', *, *, #14799, .T. ) ;
#29920=EDGE_CURVE ( 'NONE', #124115, #118128, #76691, .T. ) ;
#30074=FACE_OUTER_BOUND ( 'NONE', #52212, .T. ) ;
#30079=EDGE_CURVE ( 'NONE', #52416, #122791, #122953, .T. ) ;
#30085=ORIENTED_EDGE ( 'NONE', *, *, #47495, .F. ) ;
#30094=EDGE_CURVE ( 'NONE', #14737, #29556, #7210, .T. ) ;
#30106=EDGE_CURVE ( 'NONE', #130990, #70483, #125333, .T. ) ;
#30124=ORIENTED_EDGE ( 'NONE', *, *, #30767, .F. ) ;
#30126=CARTESIAN_POINT ( 'NONE',  ( 15.96626304157554266, 4.202752102959690472E-16, 0.000000000000000000 ) ) ;
#30130=FACE_OUTER_BOUND ( 'NONE', #103171, .T. ) ;
#30181=ORIENTED_EDGE ( 'NONE', *, *, #79482, .F. ) ;
#30217=ORIENTED_EDGE ( 'NONE', *, *, #29156, .T. ) ;
#30235=DIRECTION ( 'NONE',  ( -1.000000000000000000, -1.224606353822377258E-16, -0.000000000000000000 ) ) ;
#30252=CONICAL_SURFACE ( 'NONE', #16358, 2.055000000000000604, 0.9599310885968764806 ) ;
#30263=EDGE_LOOP ( 'NONE', ( #24774, #26928, #36095, #648, #93530 ) ) ;
#30267=CIRCLE ( 'NONE', #32560, 2.500000000000000444 ) ;
#30284=ORIENTED_EDGE ( 'NONE', *, *, #97366, .T. ) ;
#30368=ORIENTED_EDGE ( 'NONE', *, *, #126407, .F. ) ;
#30393=AXIS2_PLACEMENT_3D ( 'NONE', #15560, #4667, #48970 ) ;
#30457=CONICAL_SURFACE ( 'NONE', #116134, 2.500000000000000444, 0.9599310885968830309 ) ;
#30472=DIRECTION ( 'NONE',  ( 0.000000000000000000, 1.000000000000000000, 0.000000000000000000 ) ) ;
#30488=AXIS2_PLACEMENT_3D ( 'NONE', #122312, #133242, #12139 ) ;
#30551=CIRCLE ( 'NONE', #141685, 2.500000000000000444 ) ;
#30553=B_SPLINE_CURVE_WITH_KNOTS ( 'NONE', 3,
 ( #45932, #134364, #77150, #35067 ),
 .UNSPECIFIED., .F., .F.,
 ( 4, 4 ),
 ( 0.003615568590623272072, 0.004164643302645765210 ),
 .UNSPECIFIED. ) ;
#30597=CIRCLE ( 'NONE', #56078, 2.500000000000000444 ) ;
#30664=CARTESIAN_POINT ( 'NONE',  ( 10.15640092694706453, 3.061616997868383634E-16, -2.500000000000000444 ) ) ;
#30685=CARTESIAN_POINT ( 'NONE',  ( -12.69999999999998153, 0.000000000000000000, 2.500000000000000444 ) ) ;
#30731=ADVANCED_FACE ( 'NONE', ( #74741 ), #64550, .T. ) ;
#30762=ORIENTED_EDGE ( 'NONE', *, *, #58617, .T. ) ;
#30767=EDGE_CURVE ( 'NONE', #52339, #15589, #108019, .T. ) ;
#30814=ADVANCED_FACE ( 'NONE', ( #121766 ), #49183, .T. ) ;
#30849=CARTESIAN_POINT ( 'NONE',  ( 0.2569208697893814453, 4.202752102959690472E-16, 0.000000000000000000 ) ) ;
#30852=CONICAL_SURFACE ( 'NONE', #12293, 1.749999999999999778, 0.7853981633974480570 ) ;
#30853=DIRECTION ( 'NONE',  ( 0.000000000000000000, -1.000000000000000000, 0.000000000000000000 ) ) ;
#30858=EDGE_LOOP ( 'NONE', ( #12749, #26761, #112447, #73702, #41499, #32142 ) ) ;
#30919=CIRCLE ( 'NONE', #23971, 2.055000000000000604 ) ;
#30940=CARTESIAN_POINT ( 'NONE',  ( 1.042387978378689573, -0.3999999999999998002, -2.015694669338588429 ) ) ;
#30981=ORIENTED_EDGE ( 'NONE', *, *, #29424, .F. ) ;
#30985=EDGE_CURVE ( 'NONE', #51277, #27734, #9716, .T. ) ;
#30993=LINE ( 'NONE', #9919, #58772 ) ;
#31031=CONICAL_SURFACE ( 'NONE', #17156, 2.055000000000000604, 0.9599310885968764806 ) ;
#31046=DIRECTION ( 'NONE',  ( -1.000000000000000000, -1.224606353822377258E-16, -0.000000000000000000 ) ) ;
#31083=VERTEX_POINT ( 'NONE', #51375 ) ;
#31088=CARTESIAN_POINT ( 'NONE',  ( 14.08373646989360317, 3.821174125832445049E-16, 0.000000000000000000 ) ) ;
#31140=VERTEX_POINT ( 'NONE', #75974 ) ;
#31142=VECTOR ( 'NONE', #31191, 999.9999999999998863 ) ;
#31191=DIRECTION ( 'NONE',  ( 0.5735764363510448272, -0.8191520442889927978, 1.003171929053526103E-16 ) ) ;
#31224=ADVANCED_FACE ( 'NONE', ( #111444 ), #53742, .T. ) ;
#31254=DIRECTION ( 'NONE',  ( -1.000000000000000000, -1.224606353822377258E-16, -0.000000000000000000 ) ) ;
#31263=ORIENTED_EDGE ( 'NONE', *, *, #83477, .F. ) ;
#31264=AXIS2_PLACEMENT_3D ( 'NONE', #32692, #140026, #52274 ) ;
#31267=DIRECTION ( 'NONE',  ( -1.000000000000000000, -1.224606353822377258E-16, -0.000000000000000000 ) ) ;
#31275=ORIENTED_EDGE ( 'NONE', *, *, #60532, .T. ) ;
#31281=CARTESIAN_POINT ( 'NONE',  ( 13.29826936130429260, 3.061616997868383634E-16, -2.500000000000000444 ) ) ;
#31294=ADVANCED_FACE ( 'NONE', ( #71537 ), #21437, .T. ) ;
#31350=B_SPLINE_CURVE_WITH_KNOTS ( 'NONE', 3,
 ( #89717, #136791, #14999, #25893 ),
 .UNSPECIFIED., .F., .F.,
 ( 4, 4 ),
 ( 0.003615568590623256459, 0.004164643302645746996 ),
 .UNSPECIFIED. ) ;
#31359=VERTEX_POINT ( 'NONE', #92532 ) ;
#31422=CYLINDRICAL_SURFACE ( 'NONE', #103955, 2.500000000000000444 ) ;
#31426=DIRECTION ( 'NONE',  ( -1.000000000000000000, -1.224606353822377258E-16, -0.000000000000000000 ) ) ;
#31520=DIRECTION ( 'NONE',  ( 0.000000000000000000, -1.000000000000000000, 0.000000000000000000 ) ) ;
#31546=DIRECTION ( 'NONE',  ( 1.318980745116185161E-16, -1.000000000000000000, 0.000000000000000000 ) ) ;
#31662=AXIS2_PLACEMENT_3D ( 'NONE', #73519, #39469, #85797 ) ;
#31670=EDGE_CURVE ( 'NONE', #136234, #44903, #130309, .T. ) ;
#31725=EDGE_CURVE ( 'NONE', #5194, #45596, #23563, .T. ) ;
#31763=ADVANCED_FACE ( 'NONE', ( #24972 ), #21530, .T. ) ;
#31765=FACE_OUTER_BOUND ( 'NONE', #85100, .T. ) ;
#31784=VECTOR ( 'NONE', #28320, 1000.000000000000000 ) ;
#31794=VECTOR ( 'NONE', #112747, 999.9999999999998863 ) ;
#31860=CIRCLE ( 'NONE', #36514, 2.500000000000000444 ) ;
#31911=DIRECTION ( 'NONE',  ( 1.055184596092948005E-16, -1.000000000000000000, 0.000000000000000000 ) ) ;
#31943=DIRECTION ( 'NONE',  ( 1.000000000000000000, 1.224606353822377258E-16, 0.000000000000000000 ) ) ;
#31973=ORIENTED_EDGE ( 'NONE', *, *, #73206, .T. ) ;
#31983=CARTESIAN_POINT ( 'NONE',  ( 9.994118527364397764, 3.061616997868383634E-16, -2.500000000000000444 ) ) ;
#32027=CARTESIAN_POINT ( 'NONE',  ( -12.69999999999998153, 3.061616997868383634E-16, -2.500000000000000444 ) ) ;
#32051=EDGE_CURVE ( 'NONE', #97154, #94686, #704, .T. ) ;
#32123=DIRECTION ( 'NONE',  ( 1.734723475976806848E-16, -1.000000000000000000, 0.000000000000000000 ) ) ;
#32137=CIRCLE ( 'NONE', #4318, 2.500000000000000444 ) ;
#32139=ORIENTED_EDGE ( 'NONE', *, *, #10062, .F. ) ;
#32142=ORIENTED_EDGE ( 'NONE', *, *, #96731, .F. ) ;
#32153=DIRECTION ( 'NONE',  ( -1.000000000000000000, -1.224606353822377258E-16, -0.000000000000000000 ) ) ;
#32156=DIRECTION ( 'NONE',  ( -1.000000000000000000, -1.224606353822377258E-16, -0.000000000000000000 ) ) ;
#32196=EDGE_CURVE ( 'NONE', #73650, #23831, #4982, .T. ) ;
#32205=CARTESIAN_POINT ( 'NONE',  ( 25.00000000000000000, 0.000000000000000000, 0.000000000000000000 ) ) ;
#32248=DIRECTION ( 'NONE',  ( 0.000000000000000000, -1.000000000000000000, 0.000000000000000000 ) ) ;
#32276=DIRECTION ( 'NONE',  ( 0.000000000000000000, -1.000000000000000000, 0.000000000000000000 ) ) ;
#32356=VECTOR ( 'NONE', #77742, 1000.000000000000000 ) ;
#32401=CIRCLE ( 'NONE', #46298, 2.055000000000000604 ) ;
#32410=CARTESIAN_POINT ( 'NONE',  ( 0.000000000000000000, 0.4000000000000001332, -2.015694669338588429 ) ) ;
#32483=DIRECTION ( 'NONE',  ( 0.000000000000000000, -1.000000000000000000, 0.000000000000000000 ) ) ;
#32489=ORIENTED_EDGE ( 'NONE', *, *, #75395, .T. ) ;
#32500=LINE ( 'NONE', #20155, #97356 ) ;
#32546=ORIENTED_EDGE ( 'NONE', *, *, #21591, .F. ) ;
#32547=CIRCLE ( 'NONE', #41857, 2.500000000000000444 ) ;
#32551=CIRCLE ( 'NONE', #141287, 2.337593264352433753 ) ;
#32560=AXIS2_PLACEMENT_3D ( 'NONE', #104254, #125331, #136911 ) ;
#32590=AXIS2_PLACEMENT_3D ( 'NONE', #90842, #35763, #90085 ) ;
#32614=ADVANCED_FACE ( 'NONE', ( #38214 ), #102672, .T. ) ;
#32692=CARTESIAN_POINT ( 'NONE',  ( 10.46799328145038821, 4.202752102959690472E-16, 0.000000000000000000 ) ) ;
#32697=VERTEX_POINT ( 'NONE', #45300 ) ;
#32715=DIRECTION ( 'NONE',  ( -0.5735764363510499342, -0.8191520442889891340, 0.000000000000000000 ) ) ;
#32769=DIRECTION ( 'NONE',  ( 2.110369192185896011E-16, -1.000000000000000000, 0.000000000000000000 ) ) ;
#32804=ORIENTED_EDGE ( 'NONE', *, *, #71617, .T. ) ;
#32818=ORIENTED_EDGE ( 'NONE', *, *, #49999, .F. ) ;
#32864=CARTESIAN_POINT ( 'NONE',  ( 0.5685132242927012358, -0.3999999999999997446, -2.467792535850613866 ) ) ;
#32870=CYLINDRICAL_SURFACE ( 'NONE', #124892, 2.500000000000000444 ) ;
#32943=ORIENTED_EDGE ( 'NONE', *, *, #141001, .T. ) ;
#32960=AXIS2_PLACEMENT_3D ( 'NONE', #100025, #143511, #33375 ) ;
#32975=CARTESIAN_POINT ( 'NONE',  ( 8.585466709768445170, 2.500000000000003109, 3.061616997868386592E-16 ) ) ;
#32978=ORIENTED_EDGE ( 'NONE', *, *, #97452, .T. ) ;
#33039=CARTESIAN_POINT ( 'NONE',  ( 5.281315875828549444, 2.500000000000000444, 0.000000000000000000 ) ) ;
#33145=CARTESIAN_POINT ( 'NONE',  ( 9.370933818357753964, 0.000000000000000000, 2.500000000000000444 ) ) ;
#33154=EDGE_CURVE ( 'NONE', #111848, #31083, #75808, .T. ) ;
#33215=ORIENTED_EDGE ( 'NONE', *, *, #21704, .T. ) ;
#33232=DIRECTION ( 'NONE',  ( 0.000000000000000000, 1.000000000000000000, 0.000000000000000000 ) ) ;
#33246=LINE ( 'NONE', #99884, #92820 ) ;
#33272=ORIENTED_EDGE ( 'NONE', *, *, #66553, .T. ) ;
#33351=CARTESIAN_POINT ( 'NONE',  ( 20.20519093902540320, 0.000000000000000000, 2.500000000000000444 ) ) ;
#33375=DIRECTION ( 'NONE',  ( 0.000000000000000000, -1.000000000000000000, 0.000000000000000000 ) ) ;
#33386=VERTEX_POINT ( 'NONE', #57636 ) ;
#33411=VERTEX_POINT ( 'NONE', #104671 ) ;
#33422=CARTESIAN_POINT ( 'NONE',  ( 18.32266436734346726, 2.055000000000001048, 2.516649172247811554E-16 ) ) ;
#33434=EDGE_LOOP ( 'NONE', ( #67853, #54013, #95098, #94020, #116764 ) ) ;
#33439=DIRECTION ( 'NONE',  ( -1.000000000000000000, -1.224606353822377258E-16, -0.000000000000000000 ) ) ;
#33455=CIRCLE ( 'NONE', #116818, 2.055000000000000604 ) ;
#33535=ORIENTED_EDGE ( 'NONE', *, *, #35203, .F. ) ;
#33651=CIRCLE ( 'NONE', #114630, 2.500000000000000444 ) ;
#33674=ORIENTED_EDGE ( 'NONE', *, *, #22815, .T. ) ;
#33701=DIRECTION ( 'NONE',  ( -1.000000000000000000, -1.224606353822377258E-16, -0.000000000000000000 ) ) ;
#33703=ORIENTED_EDGE ( 'NONE', *, *, #104552, .F. ) ;
#33709=DIRECTION ( 'NONE',  ( 0.000000000000000000, 0.000000000000000000, 1.000000000000000000 ) ) ;
#33761=FACE_OUTER_BOUND ( 'NONE', #131403, .T. ) ;
#33766=ORIENTED_EDGE ( 'NONE', *, *, #104713, .F. ) ;
#33767=FACE_OUTER_BOUND ( 'NONE', #89762, .T. ) ;
#33778=DIRECTION ( 'NONE',  ( -1.000000000000000000, -0.000000000000000000, -0.000000000000000000 ) ) ;
#33815=CARTESIAN_POINT ( 'NONE',  ( 6.066782984417857350, 2.500000000000000888, 0.000000000000000000 ) ) ;
#33868=DIRECTION ( 'NONE',  ( -0.5735764363510501562, 0.8191520442889890230, 1.003171929053521419E-16 ) ) ;
#33907=FACE_OUTER_BOUND ( 'NONE', #13178, .T. ) ;
#33922=AXIS2_PLACEMENT_3D ( 'NONE', #57716, #134562, #91737 ) ;
#33928=ORIENTED_EDGE ( 'NONE', *, *, #6137, .T. ) ;
#33952=FACE_OUTER_BOUND ( 'NONE', #19365, .T. ) ;
#33965=CARTESIAN_POINT ( 'NONE',  ( 9.994118527364397764, 4.584330080086930965E-16, 0.000000000000000000 ) ) ;
#33996=ORIENTED_EDGE ( 'NONE', *, *, #30079, .T. ) ;
#34004=EDGE_CURVE ( 'NONE', #95435, #82553, #38571, .T. ) ;
#34013=EDGE_CURVE ( 'NONE', #133133, #80135, #68698, .T. ) ;
#34020=EDGE_CURVE ( 'NONE', #112772, #67004, #24684, .T. ) ;
#34065=LINE ( 'NONE', #78278, #62861 ) ;
#34101=AXIS2_PLACEMENT_3D ( 'NONE', #99308, #121782, #135554 ) ;
#34113=DIRECTION ( 'NONE',  ( 0.000000000000000000, -1.000000000000000000, -1.301042606982605074E-16 ) ) ;
#34123=LINE ( 'NONE', #45034, #140442 ) ;
#34230=VERTEX_POINT ( 'NONE', #139974 ) ;
#34235=ORIENTED_EDGE ( 'NONE', *, *, #87199, .T. ) ;
#34255=CARTESIAN_POINT ( 'NONE',  ( 21.66240673564756491, 2.862726108897619232E-16, -2.337593264352432421 ) ) ;
#34265=CARTESIAN_POINT ( 'NONE',  ( 1.042387978378689573, 4.202752102959690472E-16, 0.000000000000000000 ) ) ;
#34275=VERTEX_POINT ( 'NONE', #105860 ) ;
#34286=VERTEX_POINT ( 'NONE', #95724 ) ;
#34313=ORIENTED_EDGE ( 'NONE', *, *, #10089, .F. ) ;
#34323=AXIS2_PLACEMENT_3D ( 'NONE', #66966, #2371, #34329 ) ;
#34329=DIRECTION ( 'NONE',  ( 0.000000000000000000, -1.000000000000000000, 0.000000000000000000 ) ) ;
#34347=CARTESIAN_POINT ( 'NONE',  ( -12.69999999999998153, 0.000000000000000000, 0.000000000000000000 ) ) ;
#34352=CYLINDRICAL_SURFACE ( 'NONE', #77064, 2.500000000000000444 ) ;
#34373=EDGE_LOOP ( 'NONE', ( #21006, #78120, #88383, #14407, #63686 ) ) ;
#34374=DIRECTION ( 'NONE',  ( 0.000000000000000000, -1.000000000000000000, 0.000000000000000000 ) ) ;
#34376=EDGE_CURVE ( 'NONE', #1859, #99111, #32137, .T. ) ;
#34378=CARTESIAN_POINT ( 'NONE',  ( 17.84878961325748037, 4.584330080086930965E-16, 0.000000000000000000 ) ) ;
#34424=CONICAL_SURFACE ( 'NONE', #8899, 2.500000000000000444, 0.9599310885968830309 ) ;
#34478=ORIENTED_EDGE ( 'NONE', *, *, #99126, .T. ) ;
#34487=CARTESIAN_POINT ( 'NONE',  ( 21.15294044719737698, 3.821174125832445049E-16, 0.000000000000000000 ) ) ;
#34500=FACE_OUTER_BOUND ( 'NONE', #58897, .T. ) ;
#34510=CARTESIAN_POINT ( 'NONE',  ( 14.86920357848291196, 3.821174125832445049E-16, 0.000000000000000000 ) ) ;
#34552=ORIENTED_EDGE ( 'NONE', *, *, #4445, .F. ) ;
#34589=DIRECTION ( 'NONE',  ( 0.000000000000000000, -1.000000000000000000, 0.000000000000000000 ) ) ;
#34597=DIRECTION ( 'NONE',  ( 0.000000000000000000, 1.000000000000000000, 0.000000000000000000 ) ) ;
#34618=DIRECTION ( 'NONE',  ( -1.000000000000000000, -1.224606353822377258E-16, -0.000000000000000000 ) ) ;
#34632=VECTOR ( 'NONE', #81673, 1000.000000000000000 ) ;
#34644=DIRECTION ( 'NONE',  ( -1.000000000000000000, -1.224606353822377258E-16, -0.000000000000000000 ) ) ;
#34658=CARTESIAN_POINT ( 'NONE',  ( 1.353980332882009252, 4.584330080086930965E-16, 0.000000000000000000 ) ) ;
#34672=AXIS2_PLACEMENT_3D ( 'NONE', #77124, #32156, #21283 ) ;
#34687=( NAMED_UNIT ( * ) PLANE_ANGLE_UNIT ( ) SI_UNIT ( $, .RADIAN. ) );
#34716=DIRECTION ( 'NONE',  ( 0.000000000000000000, 0.000000000000000000, 1.000000000000000000 ) ) ;
#34719=CARTESIAN_POINT ( 'NONE',  ( 0.2569208697893814453, 4.202752102959690472E-16, 0.000000000000000000 ) ) ;
#34723=CARTESIAN_POINT ( 'NONE',  ( 18.79653912142945060, 3.061616997868387579E-16, -2.500000000000000444 ) ) ;
#34728=CARTESIAN_POINT ( 'NONE',  ( 20.67906569311139009, 4.202752102959690472E-16, 0.000000000000000000 ) ) ;
#34758=ORIENTED_EDGE ( 'NONE', *, *, #6532, .T. ) ;
#34761=DIRECTION ( 'NONE',  ( 0.000000000000000000, -1.000000000000000000, 0.000000000000000000 ) ) ;
#34786=CARTESIAN_POINT ( 'NONE',  ( 9.682526172861077640, 2.055000000000001048, 2.516649172247811554E-16 ) ) ;
#34794=DIRECTION ( 'NONE',  ( 0.000000000000000000, -1.000000000000000000, 0.000000000000000000 ) ) ;
#34813=ORIENTED_EDGE ( 'NONE', *, *, #90812, .F. ) ;
#34829=CARTESIAN_POINT ( 'NONE',  ( -12.69999999999998153, 0.000000000000000000, 0.000000000000000000 ) ) ;
#34833=ORIENTED_EDGE ( 'NONE', *, *, #67568, .F. ) ;
#34855=AXIS2_PLACEMENT_3D ( 'NONE', #47770, #49897, #38993 ) ;
#34856=ADVANCED_FACE ( 'NONE', ( #52057 ), #20110, .T. ) ;
#34910=ORIENTED_EDGE ( 'NONE', *, *, #65785, .T. ) ;
#34928=ORIENTED_EDGE ( 'NONE', *, *, #19614, .T. ) ;
#35005=CARTESIAN_POINT ( 'NONE',  ( 16.44013779566152778, 3.061616997868387579E-16, -2.500000000000000444 ) ) ;
#35006=DIRECTION ( 'NONE',  ( -1.000000000000000000, -1.224606353822377258E-16, -0.000000000000000000 ) ) ;
#35036=DIRECTION ( 'NONE',  ( 0.5735764363510444941, 0.8191520442889929088, 0.000000000000000000 ) ) ;
#35055=VECTOR ( 'NONE', #90325, 1000.000000000000000 ) ;
#35067=CARTESIAN_POINT ( 'NONE',  ( 1.042387978378689573, 0.3999999999999995781, 2.015694669338588429 ) ) ;
#35112=AXIS2_PLACEMENT_3D ( 'NONE', #56261, #25533, #133774 ) ;
#35114=FACE_OUTER_BOUND ( 'NONE', #127228, .T. ) ;
#35119=CARTESIAN_POINT ( 'NONE',  ( 16.27785539607886633, 4.584330080086930965E-16, 0.000000000000000000 ) ) ;
#35130=CARTESIAN_POINT ( 'NONE',  ( -12.69999999999998153, 0.000000000000000000, 0.000000000000000000 ) ) ;
#35203=EDGE_CURVE ( 'NONE', #131513, #71093, #110298, .T. ) ;
#35273=DIRECTION ( 'NONE',  ( 0.000000000000000000, -1.000000000000000000, 0.000000000000000000 ) ) ;
#35279=EDGE_CURVE ( 'NONE', #111457, #46699, #5635, .T. ) ;
#35282=ORIENTED_EDGE ( 'NONE', *, *, #132588, .F. ) ;
#35283=DIRECTION ( 'NONE',  ( 0.000000000000000000, 0.000000000000000000, 1.000000000000000000 ) ) ;
#35381=DIRECTION ( 'NONE',  ( 0.5735764363510448272, -0.8191520442889927978, 1.003171929053526103E-16 ) ) ;
#35392=CARTESIAN_POINT ( 'NONE',  ( 6.852250093007166143, 4.584330080086930965E-16, 0.000000000000000000 ) ) ;
#35425=CARTESIAN_POINT ( 'NONE',  ( 19.89359858452208130, -2.055000000000000160, 2.789133085058097101E-16 ) ) ;
#35429=SURFACE_SIDE_STYLE ('',( #46306 ) ) ;
#35502=EDGE_LOOP ( 'NONE', ( #97350, #2196, #38409, #102602, #82874 ) ) ;
#35547=EDGE_CURVE ( 'NONE', #141465, #73316, #20171, .T. ) ;
#35569=DIRECTION ( 'NONE',  ( 0.000000000000000000, -1.000000000000000000, 0.000000000000000000 ) ) ;
#35571=CARTESIAN_POINT ( 'NONE',  ( 9.994118527364397764, 4.584330080086930965E-16, 0.000000000000000000 ) ) ;
#35578=EDGE_CURVE ( 'NONE', #133129, #63294, #3256, .T. ) ;
#35600=CIRCLE ( 'NONE', #107371, 2.500000000000000444 ) ;
#35603=ORIENTED_EDGE ( 'NONE', *, *, #46548, .F. ) ;
#35615=AXIS2_PLACEMENT_3D ( 'NONE', #71323, #95187, #126390 ) ;
#35629=EDGE_LOOP ( 'NONE', ( #105836, #57895, #53331, #133060, #81630, #36500 ) ) ;
#35662=EDGE_CURVE ( 'NONE', #119988, #109534, #61822, .T. ) ;
#35668=DIRECTION ( 'NONE',  ( -1.000000000000000000, -1.224606353822377258E-16, -0.000000000000000000 ) ) ;
#35669=EDGE_CURVE ( 'NONE', #141895, #140903, #17008, .T. ) ;
#35721=ORIENTED_EDGE ( 'NONE', *, *, #90997, .T. ) ;
#35739=CARTESIAN_POINT ( 'NONE',  ( 4.184256412735922304, 4.202752102959690472E-16, 0.000000000000000000 ) ) ;
#35763=DIRECTION ( 'NONE',  ( -1.000000000000000000, -1.224606353822377258E-16, -0.000000000000000000 ) ) ;
#35818=DIRECTION ( 'NONE',  ( 0.5735764363510444941, 0.8191520442889929088, 0.000000000000000000 ) ) ;
#35858=CARTESIAN_POINT ( 'NONE',  ( -12.69999999999998153, 0.000000000000000000, 1.749999999999999778 ) ) ;
#35860=CARTESIAN_POINT ( 'NONE',  ( 0.2569208697893815008, -0.3999999999999998002, -2.015694669338588429 ) ) ;
#35869=EDGE_CURVE ( 'NONE', #73316, #141465, #94844, .T. ) ;
#35873=ORIENTED_EDGE ( 'NONE', *, *, #21550, .F. ) ;
#35875=DIRECTION ( 'NONE',  ( -1.000000000000000000, -1.224606353822377258E-16, -0.000000000000000000 ) ) ;
#35956=DIRECTION ( 'NONE',  ( 0.000000000000000000, 0.000000000000000000, 1.000000000000000000 ) ) ;
#35965=LINE ( 'NONE', #33815, #49296 ) ;
#35967=CARTESIAN_POINT ( 'NONE',  ( 6.852250093007166143, 4.584330080086930965E-16, 0.000000000000000000 ) ) ;
#35978=ORIENTED_EDGE ( 'NONE', *, *, #52666, .T. ) ;
#36014=VERTEX_POINT ( 'NONE', #56672 ) ;
#36038=CARTESIAN_POINT ( 'NONE',  ( 18.01107201284014536, 3.821174125832445049E-16, 0.000000000000000000 ) ) ;
#36091=CONICAL_SURFACE ( 'NONE', #89361, 2.500000000000000444, 0.9599310885968830309 ) ;
#36095=ORIENTED_EDGE ( 'NONE', *, *, #45996, .F. ) ;
#36096=CIRCLE ( 'NONE', #135628, 2.500000000000000444 ) ;
#36100=CARTESIAN_POINT ( 'NONE',  ( 14.08373646989360317, 3.821174125832445049E-16, 0.000000000000000000 ) ) ;
#36119=CIRCLE ( 'NONE', #117101, 2.500000000000000444 ) ;
#36146=ORIENTED_EDGE ( 'NONE', *, *, #15457, .T. ) ;
#36147=DIRECTION ( 'NONE',  ( 1.734723475976806848E-16, -1.000000000000000000, 0.000000000000000000 ) ) ;
#36169=DIRECTION ( 'NONE',  ( -1.000000000000000000, -1.224606353822377258E-16, -0.000000000000000000 ) ) ;
#36222=CARTESIAN_POINT ( 'NONE',  ( 8.897059064271770623, -2.055000000000000160, 0.000000000000000000 ) ) ;
#36251=DIRECTION ( 'NONE',  ( -1.000000000000000000, -1.224606353822377258E-16, -0.000000000000000000 ) ) ;
#36292=ORIENTED_EDGE ( 'NONE', *, *, #5719, .T. ) ;
#36301=LINE ( 'NONE', #90695, #9004 ) ;
#36340=VECTOR ( 'NONE', #76278, 1000.000000000000000 ) ;
#36341=DIRECTION ( 'NONE',  ( 0.000000000000000000, -1.000000000000000000, 0.000000000000000000 ) ) ;
#36390=ORIENTED_EDGE ( 'NONE', *, *, #316, .T. ) ;
#36401=LINE ( 'NONE', #37105, #48656 ) ;
#36417=AXIS2_PLACEMENT_3D ( 'NONE', #11602, #131281, #121806 ) ;
#36434=CARTESIAN_POINT ( 'NONE',  ( 13.92145407031093818, 0.000000000000000000, 2.500000000000000444 ) ) ;
#36446=VECTOR ( 'NONE', #87330, 1000.000000000000000 ) ;
#36477=ORIENTED_EDGE ( 'NONE', *, *, #84093, .T. ) ;
#36495=DIRECTION ( 'NONE',  ( 0.000000000000000000, -1.000000000000000000, 0.000000000000000000 ) ) ;
#36500=ORIENTED_EDGE ( 'NONE', *, *, #141495, .F. ) ;
#36502=VERTEX_POINT ( 'NONE', #99504 ) ;
#36505=DIRECTION ( 'NONE',  ( -1.000000000000000000, -1.224606353822377258E-16, -0.000000000000000000 ) ) ;
#36514=AXIS2_PLACEMENT_3D ( 'NONE', #97185, #47016, #44869 ) ;
#36529=FACE_OUTER_BOUND ( 'NONE', #133430, .T. ) ;
#36593=DIRECTION ( 'NONE',  ( -0.5735764363510501562, 0.8191520442889890230, 1.003171929053521419E-16 ) ) ;
#36602=ADVANCED_FACE ( 'NONE', ( #4426 ), #20660, .T. ) ;
#36620=ORIENTED_EDGE ( 'NONE', *, *, #64119, .T. ) ;
#36624=DIRECTION ( 'NONE',  ( 1.318980745116185161E-16, -1.000000000000000000, 0.000000000000000000 ) ) ;
#36656=ORIENTED_EDGE ( 'NONE', *, *, #142604, .T. ) ;
#36711=AXIS2_PLACEMENT_3D ( 'NONE', #67828, #357, #66372 ) ;
#36747=FACE_OUTER_BOUND ( 'NONE', #109112, .T. ) ;
#36813=CONICAL_SURFACE ( 'NONE', #36711, 2.055000000000000604, 0.9599310885968764806 ) ;
#36833=CARTESIAN_POINT ( 'NONE',  ( 4.969723521325230209, 2.055000000000001048, 0.000000000000000000 ) ) ;
#36836=EDGE_CURVE ( 'NONE', #139503, #12106, #114772, .T. ) ;
#36858=ADVANCED_FACE ( 'NONE', ( #100370 ), #134431, .T. ) ;
#36870=CARTESIAN_POINT ( 'NONE',  ( 5.755190629914537226, 4.202752102959690472E-16, 0.000000000000000000 ) ) ;
#36871=DIRECTION ( 'NONE',  ( 0.000000000000000000, -1.000000000000000000, 0.000000000000000000 ) ) ;
#36930=CIRCLE ( 'NONE', #60143, 2.500000000000000444 ) ;
#36946=ADVANCED_FACE ( 'NONE', ( #36529 ), #13803, .T. ) ;
#36954=EDGE_CURVE ( 'NONE', #80135, #116730, #41562, .T. ) ;
#36972=VERTEX_POINT ( 'NONE', #117617 ) ;
#36987=VECTOR ( 'NONE', #33868, 999.9999999999998863 ) ;
#36995=DIRECTION ( 'NONE',  ( 1.000000000000000000, 1.224606353822377258E-16, 0.000000000000000000 ) ) ;
#37028=ORIENTED_EDGE ( 'NONE', *, *, #5719, .F. ) ;
#37036=DIRECTION ( 'NONE',  ( 0.000000000000000000, 1.000000000000000000, 0.000000000000000000 ) ) ;
#37049=ORIENTED_EDGE ( 'NONE', *, *, #115714, .F. ) ;
#37050=EDGE_LOOP ( 'NONE', ( #61141, #95158, #115236, #137456, #91381 ) ) ;
#37103=VERTEX_POINT ( 'NONE', #65452 ) ;
#37105=CARTESIAN_POINT ( 'NONE',  ( -12.69999999999998153, 3.061616997868383634E-16, -2.500000000000000444 ) ) ;
#37127=CIRCLE ( 'NONE', #127358, 2.500000000000000444 ) ;
#37172=CIRCLE ( 'NONE', #4717, 2.500000000000000444 ) ;
#37203=VERTEX_POINT ( 'NONE', #87169 ) ;
#37229=DIRECTION ( 'NONE',  ( 0.000000000000000000, 1.000000000000000000, 0.000000000000000000 ) ) ;
#37239=CONICAL_SURFACE ( 'NONE', #118240, 2.500000000000000444, 0.9599310885968830309 ) ;
#37324=DIRECTION ( 'NONE',  ( -1.000000000000000000, -1.224606353822377258E-16, -0.000000000000000000 ) ) ;
#37356=CIRCLE ( 'NONE', #132381, 2.500000000000000444 ) ;
#37376=ORIENTED_EDGE ( 'NONE', *, *, #89962, .F. ) ;
#37407=VECTOR ( 'NONE', #35818, 1000.000000000000000 ) ;
#37430=FILL_AREA_STYLE_COLOUR ( '', #40185 ) ;
#37434=DIRECTION ( 'NONE',  ( 0.000000000000000000, -1.000000000000000000, 0.000000000000000000 ) ) ;
#37436=DIRECTION ( 'NONE',  ( 0.000000000000000000, -1.000000000000000000, 0.000000000000000000 ) ) ;
#37499=CIRCLE ( 'NONE', #95316, 2.500000000000000444 ) ;
#37501=ORIENTED_EDGE ( 'NONE', *, *, #121273, .F. ) ;
#37512=CARTESIAN_POINT ( 'NONE',  ( 16.75173015016484968, 4.202752102959690472E-16, 0.000000000000000000 ) ) ;
#37527=DIRECTION ( 'NONE',  ( -1.000000000000000000, -1.224606353822377258E-16, -0.000000000000000000 ) ) ;
#37542=DIRECTION ( 'NONE',  ( -1.000000000000000000, -1.224606353822377258E-16, -0.000000000000000000 ) ) ;
#37599=CARTESIAN_POINT ( 'NONE',  ( 0.7307956238753654521, 3.821174125832445049E-16, 0.000000000000000000 ) ) ;
#37664=ORIENTED_EDGE ( 'NONE', *, *, #38478, .T. ) ;
#37680=DIRECTION ( 'NONE',  ( 0.000000000000000000, -1.000000000000000000, 0.000000000000000000 ) ) ;
#37687=DIRECTION ( 'NONE',  ( 0.000000000000000000, 1.000000000000000000, 0.000000000000000000 ) ) ;
#37729=ORIENTED_EDGE ( 'NONE', *, *, #13072, .F. ) ;
#37746=AXIS2_PLACEMENT_3D ( 'NONE', #88494, #31254, #29793 ) ;
#37884=CARTESIAN_POINT ( 'NONE',  ( 19.58200623001875940, 3.821174125832445049E-16, 0.000000000000000000 ) ) ;
#37928=ORIENTED_EDGE ( 'NONE', *, *, #38142, .T. ) ;
#37981=CONICAL_SURFACE ( 'NONE', #7818, 2.500000000000000444, 0.9599310885968830309 ) ;
#37989=CARTESIAN_POINT ( 'NONE',  ( 10.15640092694706453, -2.499999999999999112, 0.000000000000000000 ) ) ;
#38008=VERTEX_POINT ( 'NONE', #9030 ) ;
#38043=VERTEX_POINT ( 'NONE', #59754 ) ;
#38052=DIRECTION ( 'NONE',  ( 0.000000000000000000, 0.000000000000000000, 1.000000000000000000 ) ) ;
#38062=CARTESIAN_POINT ( 'NONE',  ( 4.184256412735922304, 2.055000000000001048, 2.516649172247811554E-16 ) ) ;
#38064=DIRECTION ( 'NONE',  ( 0.000000000000000000, 0.000000000000000000, 1.000000000000000000 ) ) ;
#38105=DIRECTION ( 'NONE',  ( 0.000000000000000000, -1.000000000000000000, 0.000000000000000000 ) ) ;
#38142=EDGE_CURVE ( 'NONE', #51507, #90821, #48239, .T. ) ;
#38169=CARTESIAN_POINT ( 'NONE',  ( 1.629999999999999893, -0.3999999999999997446, -2.500000000000000000 ) ) ;
#38206=ORIENTED_EDGE ( 'NONE', *, *, #39435, .T. ) ;
#38214=FACE_OUTER_BOUND ( 'NONE', #70577, .T. ) ;
#38221=ORIENTED_EDGE ( 'NONE', *, *, #108828, .T. ) ;
#38230=EDGE_LOOP ( 'NONE', ( #107317, #28821, #67118, #61637, #75451, #53870 ) ) ;
#38282=AXIS2_PLACEMENT_3D ( 'NONE', #35571, #13742, #730 ) ;
#38290=DIRECTION ( 'NONE',  ( -1.000000000000000000, -1.224606353822377258E-16, -0.000000000000000000 ) ) ;
#38297=CARTESIAN_POINT ( 'NONE',  ( 1.042387978378689350, 0.4000000000000001332, -2.015694669338588429 ) ) ;
#38328=FACE_OUTER_BOUND ( 'NONE', #17764, .T. ) ;
#38347=CARTESIAN_POINT ( 'NONE',  ( 0.5685132242927012358, 0.3999999999999995226, 2.467792535850613866 ) ) ;
#38368=AXIS2_PLACEMENT_3D ( 'NONE', #105547, #81711, #125910 ) ;
#38391=ORIENTED_EDGE ( 'NONE', *, *, #16960, .T. ) ;
#38409=ORIENTED_EDGE ( 'NONE', *, *, #111033, .T. ) ;
#38444=VERTEX_POINT ( 'NONE', #103746 ) ;
#38478=EDGE_CURVE ( 'NONE', #14737, #96111, #105198, .T. ) ;
#38513=LINE ( 'NONE', #6534, #93333 ) ;
#38571=CIRCLE ( 'NONE', #33922, 2.500000000000000444 ) ;
#38577=CARTESIAN_POINT ( 'NONE',  ( -12.69999999999998153, 0.000000000000000000, 2.500000000000000444 ) ) ;
#38624=VECTOR ( 'NONE', #49199, 1000.000000000000000 ) ;
#38676=LINE ( 'NONE', #95899, #107172 ) ;
#38686=CARTESIAN_POINT ( 'NONE',  ( 5.281315875828549444, 4.584330080086930965E-16, 0.000000000000000000 ) ) ;
#38698=AXIS2_PLACEMENT_3D ( 'NONE', #96639, #140197, #83700 ) ;
#38724=AXIS2_PLACEMENT_3D ( 'NONE', #59813, #82985, #71397 ) ;
#38743=CARTESIAN_POINT ( 'NONE',  ( 19.41972383043609440, 4.584330080086930965E-16, 0.000000000000000000 ) ) ;
#38778=AXIS2_PLACEMENT_3D ( 'NONE', #12727, #122940, #35956 ) ;
#38792=ORIENTED_EDGE ( 'NONE', *, *, #36954, .T. ) ;
#38801=ORIENTED_EDGE ( 'NONE', *, *, #93418, .T. ) ;
#38805=DIRECTION ( 'NONE',  ( -1.000000000000000000, -1.224606353822377258E-16, -0.000000000000000000 ) ) ;
#38836=ORIENTED_EDGE ( 'NONE', *, *, #6318, .F. ) ;
#38904=LINE ( 'NONE', #72297, #127767 ) ;
#38993=DIRECTION ( 'NONE',  ( 0.000000000000000000, 1.000000000000000000, 0.000000000000000000 ) ) ;
#38995=AXIS2_PLACEMENT_3D ( 'NONE', #109639, #108176, #8159 ) ;
#39001=EDGE_LOOP ( 'NONE', ( #130031, #108586, #103360, #37049, #63800 ) ) ;
#39025=DIRECTION ( 'NONE',  ( 0.000000000000000000, -1.000000000000000000, 0.000000000000000000 ) ) ;
#39033=CARTESIAN_POINT ( 'NONE',  ( 14.39532882439692862, 4.202752102959690472E-16, 0.000000000000000000 ) ) ;
#39114=DIRECTION ( 'NONE',  ( 0.5735764363510448272, -0.8191520442889927978, 1.003171929053526103E-16 ) ) ;
#39184=VERTEX_POINT ( 'NONE', #27115 ) ;
#39204=ORIENTED_EDGE ( 'NONE', *, *, #98383, .T. ) ;
#39236=CIRCLE ( 'NONE', #120207, 2.500000000000000444 ) ;
#39251=DIRECTION ( 'NONE',  ( 0.5735764363510444941, 0.8191520442889929088, 0.000000000000000000 ) ) ;
#39253=DIRECTION ( 'NONE',  ( 0.000000000000000000, -1.301042606982605074E-16, 1.000000000000000000 ) ) ;
#39276=FACE_OUTER_BOUND ( 'NONE', #127576, .T. ) ;
#39277=EDGE_CURVE ( 'NONE', #117931, #59073, #98974, .T. ) ;
#39301=AXIS2_PLACEMENT_3D ( 'NONE', #104401, #115979, #85494 ) ;
#39305=DIRECTION ( 'NONE',  ( -1.000000000000000000, -1.224606353822377258E-16, -0.000000000000000000 ) ) ;
#39334=AXIS2_PLACEMENT_3D ( 'NONE', #3241, #25719, #14839 ) ;
#39345=DIRECTION ( 'NONE',  ( 0.000000000000000000, -1.000000000000000000, 0.000000000000000000 ) ) ;
#39359=AXIS2_PLACEMENT_3D ( 'NONE', #131145, #20935, #52151 ) ;
#39373=EDGE_LOOP ( 'NONE', ( #84443, #39434, #104605, #140066, #6969 ) ) ;
#39401=AXIS2_PLACEMENT_3D ( 'NONE', #1373, #66675, #34761 ) ;
#39402=CARTESIAN_POINT ( 'NONE',  ( 12.35051985313232237, 4.584330080086930965E-16, 0.000000000000000000 ) ) ;
#39410=DIRECTION ( 'NONE',  ( -1.000000000000000000, -1.224606353822377258E-16, -0.000000000000000000 ) ) ;
#39427=EDGE_CURVE ( 'NONE', #9541, #123638, #99060, .T. ) ;
#39434=ORIENTED_EDGE ( 'NONE', *, *, #131201, .F. ) ;
#39435=EDGE_CURVE ( 'NONE', #22872, #36502, #87222, .T. ) ;
#39454=CARTESIAN_POINT ( 'NONE',  ( 15.18079593298623564, 4.202752102959690472E-16, 0.000000000000000000 ) ) ;
#39469=DIRECTION ( 'NONE',  ( -1.000000000000000000, -0.000000000000000000, -0.000000000000000000 ) ) ;
#39544=CARTESIAN_POINT ( 'NONE',  ( 3.710381658649933634, 4.584330080086930965E-16, 0.000000000000000000 ) ) ;
#39556=ORIENTED_EDGE ( 'NONE', *, *, #119091, .F. ) ;
#39571=ORIENTED_EDGE ( 'NONE', *, *, #53589, .T. ) ;
#39587=ADVANCED_FACE ( 'NONE', ( #57473 ), #126808, .T. ) ;
#39614=CONICAL_SURFACE ( 'NONE', #141418, 2.055000000000000604, 0.9599310885968764806 ) ;
#39621=EDGE_CURVE ( 'NONE', #106357, #59504, #135728, .T. ) ;
#39655=AXIS2_PLACEMENT_3D ( 'NONE', #58183, #105199, #13881 ) ;
#39680=AXIS2_PLACEMENT_3D ( 'NONE', #22291, #34644, #14835 ) ;
#39684=ORIENTED_EDGE ( 'NONE', *, *, #28723, .F. ) ;
#39701=VECTOR ( 'NONE', #63425, 1000.000000000000000 ) ;
#39711=CIRCLE ( 'NONE', #221, 2.500000000000000444 ) ;
#39727=ORIENTED_EDGE ( 'NONE', *, *, #74348, .F. ) ;
#39869=CARTESIAN_POINT ( 'NONE',  ( 8.111591955682463606, 4.202752102959690472E-16, 0.000000000000000000 ) ) ;
#39927=ADVANCED_FACE ( 'NONE', ( #70346 ), #5952, .T. ) ;
#39968=LINE ( 'NONE', #29055, #71790 ) ;
#39977=EDGE_CURVE ( 'NONE', #36972, #140889, #102232, .T. ) ;
#40043=ORIENTED_EDGE ( 'NONE', *, *, #29111, .F. ) ;
#40050=AXIS2_PLACEMENT_3D ( 'NONE', #1037, #35875, #135184 ) ;
#40056=EDGE_LOOP ( 'NONE', ( #41120, #72898, #110243, #13329, #29155 ) ) ;
#40098=EDGE_CURVE ( 'NONE', #13272, #11616, #8133, .T. ) ;
#40120=CARTESIAN_POINT ( 'NONE',  ( 15.49238828748955576, 4.584330080086930965E-16, 0.000000000000000000 ) ) ;
#40139=DIRECTION ( 'NONE',  ( -1.000000000000000000, -1.224606353822377258E-16, -0.000000000000000000 ) ) ;
#40147=EDGE_CURVE ( 'NONE', #111848, #51277, #115901, .T. ) ;
#40185=COLOUR_RGB ( '', 0.40784314, 0.44705882, 0.49803922) ;
#40223=EDGE_LOOP ( 'NONE', ( #75058, #20506, #74758, #84885, #1184 ) ) ;
#40260=AXIS2_PLACEMENT_3D ( 'NONE', #7433, #51696, #102 ) ;
#40272=EDGE_CURVE ( 'NONE', #79754, #25103, #94246, .T. ) ;
#40348=VECTOR ( 'NONE', #87217, 999.9999999999998863 ) ;
#40353=FACE_OUTER_BOUND ( 'NONE', #5670, .T. ) ;
#40384=VERTEX_POINT ( 'NONE', #112215 ) ;
#40390=LINE ( 'NONE', #104157, #18877 ) ;
#40394=LINE ( 'NONE', #17191, #110367 ) ;
#40419=CARTESIAN_POINT ( 'NONE',  ( 14.08373646989360317, 0.000000000000000000, 2.500000000000000444 ) ) ;
#40527=EDGE_CURVE ( 'NONE', #131428, #19769, #126629, .T. ) ;
#40573=EDGE_CURVE ( 'NONE', #124115, #140149, #21717, .T. ) ;
#40574=AXIS2_PLACEMENT_3D ( 'NONE', #106445, #94873, #37687 ) ;
#40606=DIRECTION ( 'NONE',  ( 0.000000000000000000, -1.000000000000000000, 0.000000000000000000 ) ) ;
#40620=ORIENTED_EDGE ( 'NONE', *, *, #12683, .F. ) ;
#40629=VERTEX_POINT ( 'NONE', #60670 ) ;
#40630=CARTESIAN_POINT ( 'NONE',  ( 21.15294044719737698, 0.000000000000000000, 2.500000000000000444 ) ) ;
#40653=DIRECTION ( 'NONE',  ( -1.000000000000000000, -0.000000000000000000, -0.000000000000000000 ) ) ;
#40655=ORIENTED_EDGE ( 'NONE', *, *, #93875, .T. ) ;
#40671=CARTESIAN_POINT ( 'NONE',  ( 14.86920357848291196, 2.500000000000000444, 3.061616997868383634E-16 ) ) ;
#40764=LINE ( 'NONE', #84966, #64342 ) ;
#40800=CARTESIAN_POINT ( 'NONE',  ( 0.000000000000000000, 0.4000000000000001332, -2.015694669338588429 ) ) ;
#40851=VECTOR ( 'NONE', #44112, 1000.000000000000000 ) ;
#40876=AXIS2_PLACEMENT_3D ( 'NONE', #10685, #75285, #120897 ) ;
#40878=ORIENTED_EDGE ( 'NONE', *, *, #35279, .F. ) ;
#40892=DIRECTION ( 'NONE',  ( 1.000000000000000000, 1.224606353822377258E-16, 0.000000000000000000 ) ) ;
#40897=CARTESIAN_POINT ( 'NONE',  ( 1.554198602559970332, -0.4000000000000004108, 2.412907414356850744 ) ) ;
#40935=ORIENTED_EDGE ( 'NONE', *, *, #80975, .F. ) ;
#40941=DIRECTION ( 'NONE',  ( -1.000000000000000000, -1.224606353822377258E-16, -0.000000000000000000 ) ) ;
#40955=ORIENTED_EDGE ( 'NONE', *, *, #122748, .F. ) ;
#41013=CIRCLE ( 'NONE', #34101, 2.500000000000000444 ) ;
#41028=DIRECTION ( 'NONE',  ( -1.000000000000000000, -1.224606353822377258E-16, -0.000000000000000000 ) ) ;
#41068=DIRECTION ( 'NONE',  ( -1.000000000000000000, -0.000000000000000000, -0.000000000000000000 ) ) ;
#41083=ORIENTED_EDGE ( 'NONE', *, *, #50672, .T. ) ;
#41120=ORIENTED_EDGE ( 'NONE', *, *, #35547, .F. ) ;
#41149=VERTEX_POINT ( 'NONE', #85756 ) ;
#41168=DIRECTION ( 'NONE',  ( 0.000000000000000000, -1.000000000000000000, 0.000000000000000000 ) ) ;
#41200=ORIENTED_EDGE ( 'NONE', *, *, #76972, .T. ) ;
#41278=ORIENTED_EDGE ( 'NONE', *, *, #73378, .F. ) ;
#41311=ORIENTED_EDGE ( 'NONE', *, *, #25164, .T. ) ;
#41360=FACE_OUTER_BOUND ( 'NONE', #52598, .T. ) ;
#41372=AXIS2_PLACEMENT_3D ( 'NONE', #108384, #88115, #132364 ) ;
#41419=DIRECTION ( 'NONE',  ( -1.000000000000000000, -1.224606353822377258E-16, -0.000000000000000000 ) ) ;
#41447=DIRECTION ( 'NONE',  ( 1.301042606982605074E-16, -1.000000000000000000, 0.000000000000000000 ) ) ;
#41469=CARTESIAN_POINT ( 'NONE',  ( 6.852250093007166143, 4.584330080086930965E-16, 0.000000000000000000 ) ) ;
#41493=ORIENTED_EDGE ( 'NONE', *, *, #92965, .F. ) ;
#41499=ORIENTED_EDGE ( 'NONE', *, *, #32051, .F. ) ;
#41505=ADVANCED_FACE ( 'NONE', ( #129510 ), #4811, .T. ) ;
#41510=EDGE_CURVE ( 'NONE', #142252, #42684, #109049, .T. ) ;
#41562=CIRCLE ( 'NONE', #23017, 2.500000000000000444 ) ;
#41595=DIRECTION ( 'NONE',  ( -0.5735764363510501562, 0.8191520442889890230, 1.003171929053521419E-16 ) ) ;
#41602=ORIENTED_EDGE ( 'NONE', *, *, #114354, .F. ) ;
#41603=B_SPLINE_CURVE_WITH_KNOTS ( 'NONE', 3,
 ( #109733, #110422, #11096, #98845 ),
 .UNSPECIFIED., .F., .F.,
 ( 4, 4 ),
 ( 0.003615568590623272072, 0.004164643302645765210 ),
 .UNSPECIFIED. ) ;
#41638=DIRECTION ( 'NONE',  ( 0.000000000000000000, -1.000000000000000000, 0.000000000000000000 ) ) ;
#41650=CONICAL_SURFACE ( 'NONE', #141189, 2.500000000000000444, 0.9599310885968830309 ) ;
#41651=CIRCLE ( 'NONE', #46251, 2.055000000000000604 ) ;
#41658=ADVANCED_FACE ( 'NONE', ( #56301 ), #115977, .T. ) ;
#41792=CARTESIAN_POINT ( 'NONE',  ( -12.69999999999998153, 0.000000000000000000, 0.000000000000000000 ) ) ;
#41822=ORIENTED_EDGE ( 'NONE', *, *, #142604, .F. ) ;
#41823=CARTESIAN_POINT ( 'NONE',  ( 18.63425672184678916, 4.584330080086930965E-16, 0.000000000000000000 ) ) ;
#41857=AXIS2_PLACEMENT_3D ( 'NONE', #51185, #29409, #88091 ) ;
#41872=VERTEX_POINT ( 'NONE', #7558 ) ;
#41899=VECTOR ( 'NONE', #35036, 1000.000000000000000 ) ;
#41966=ORIENTED_EDGE ( 'NONE', *, *, #64639, .T. ) ;
#42002=CIRCLE ( 'NONE', #123025, 2.055000000000000604 ) ;
#42009=ADVANCED_FACE ( 'NONE', ( #76426 ), #44535, .T. ) ;
#42023=VERTEX_POINT ( 'NONE', #79315 ) ;
#42061=LINE ( 'NONE', #73260, #92727 ) ;
#42077=DIRECTION ( 'NONE',  ( -1.000000000000000000, -1.224606353822377258E-16, -0.000000000000000000 ) ) ;
#42079=CONICAL_SURFACE ( 'NONE', #18977, 2.055000000000000604, 0.9599310885968764806 ) ;
#42087=DIRECTION ( 'NONE',  ( -0.5735764363510499342, -0.8191520442889891340, 0.000000000000000000 ) ) ;
#42090=FACE_OUTER_BOUND ( 'NONE', #53604, .T. ) ;
#42093=AXIS2_PLACEMENT_3D ( 'NONE', #9104, #132414, #118626 ) ;
#42130=CONICAL_SURFACE ( 'NONE', #127804, 2.055000000000000604, 0.9599310885968764806 ) ;
#42163=ORIENTED_EDGE ( 'NONE', *, *, #46748, .F. ) ;
#42254=CARTESIAN_POINT ( 'NONE',  ( 20.67906569311139009, -2.055000000000000160, 0.000000000000000000 ) ) ;
#42258=LINE ( 'NONE', #117615, #120772 ) ;
#42261=VECTOR ( 'NONE', #41595, 999.9999999999998863 ) ;
#42299=ORIENTED_EDGE ( 'NONE', *, *, #104713, .T. ) ;
#42331=AXIS2_PLACEMENT_3D ( 'NONE', #85994, #107021, #127351 ) ;
#42339=DIRECTION ( 'NONE',  ( 0.000000000000000000, 1.000000000000000000, 0.000000000000000000 ) ) ;
#42392=CIRCLE ( 'NONE', #53985, 2.055000000000000604 ) ;
#42410=EDGE_CURVE ( 'NONE', #111848, #110816, #30919, .T. ) ;
#42490=CARTESIAN_POINT ( 'NONE',  ( -12.69999999999998153, 0.000000000000000000, 0.000000000000000000 ) ) ;
#42523=VERTEX_POINT ( 'NONE', #138294 ) ;
#42530=CARTESIAN_POINT ( 'NONE',  ( 3.087196949643289390, 2.500000000000000444, 3.061616997868383634E-16 ) ) ;
#42532=LINE ( 'NONE', #107737, #17737 ) ;
#42533=EDGE_LOOP ( 'NONE', ( #59024, #86274, #2837, #81601, #65724 ) ) ;
#42605=ORIENTED_EDGE ( 'NONE', *, *, #49930, .F. ) ;
#42639=DIRECTION ( 'NONE',  ( 0.000000000000000000, -1.000000000000000000, 0.000000000000000000 ) ) ;
#42664=DIRECTION ( 'NONE',  ( -1.000000000000000000, -1.224606353822377258E-16, -0.000000000000000000 ) ) ;
#42684=VERTEX_POINT ( 'NONE', #20054 ) ;
#42693=EDGE_LOOP ( 'NONE', ( #70474, #105397, #119018, #66647, #69385 ) ) ;
#42707=DIRECTION ( 'NONE',  ( 0.000000000000000000, -1.000000000000000000, 0.000000000000000000 ) ) ;
#42733=FACE_OUTER_BOUND ( 'NONE', #53017, .T. ) ;
#42737=ADVANCED_FACE ( 'NONE', ( #99772 ), #95870, .T. ) ;
#42741=DIRECTION ( 'NONE',  ( 0.000000000000000000, -1.000000000000000000, 0.000000000000000000 ) ) ;
#42792=CARTESIAN_POINT ( 'NONE',  ( 13.92145407031093818, -2.500000000000000000, 3.061616997868383634E-16 ) ) ;
#42802=EDGE_CURVE ( 'NONE', #23744, #29345, #112103, .T. ) ;
#42806=CARTESIAN_POINT ( 'NONE',  ( 1.042387978378689573, 4.202752102959690472E-16, 0.000000000000000000 ) ) ;
#42812=EDGE_CURVE ( 'NONE', #129512, #34230, #90324, .T. ) ;
#42818=AXIS2_PLACEMENT_3D ( 'NONE', #115716, #82430, #48364 ) ;
#42854=CARTESIAN_POINT ( 'NONE',  ( 1.629999999999999893, 0.4000000000000001887, -2.500000000000000000 ) ) ;
#42901=PRODUCT_DEFINITION_CONTEXT ( 'detailed design', #22594, 'design' ) ;
#42956=EDGE_CURVE ( 'NONE', #62751, #2459, #118952, .T. ) ;
#42971=CARTESIAN_POINT ( 'NONE',  ( 2.924914550060625285, 4.584330080086930965E-16, 0.000000000000000000 ) ) ;
#43047=DIRECTION ( 'NONE',  ( 1.000000000000000000, 0.000000000000000000, 0.000000000000000000 ) ) ;
#43064=LINE ( 'NONE', #100290, #24601 ) ;
#43084=ORIENTED_EDGE ( 'NONE', *, *, #13851, .T. ) ;
#43095=B_SPLINE_CURVE_WITH_KNOTS ( 'NONE', 3,
 ( #38297, #18645, #62925, #7777 ),
 .UNSPECIFIED., .F., .F.,
 ( 4, 4 ),
 ( 0.008853860144884201713, 0.009403245473020210854 ),
 .UNSPECIFIED. ) ;
#43140=CARTESIAN_POINT ( 'NONE',  ( 13.60986171580761805, 4.202752102959690472E-16, 0.000000000000000000 ) ) ;
#43141=CARTESIAN_POINT ( 'NONE',  ( 0.000000000000000000, 0.4000000000000001887, -2.500000000000000000 ) ) ;
#43204=CARTESIAN_POINT ( 'NONE',  ( 10.77958563595370833, 4.584330080086930965E-16, 0.000000000000000000 ) ) ;
#43208=AXIS2_PLACEMENT_3D ( 'NONE', #54765, #14076, #101816 ) ;
#43219=CARTESIAN_POINT ( 'NONE',  ( 7.799999601179139042, 3.821174125832445049E-16, 0.000000000000000000 ) ) ;
#43230=DIRECTION ( 'NONE',  ( 0.000000000000000000, 0.000000000000000000, 1.000000000000000000 ) ) ;
#43244=ORIENTED_EDGE ( 'NONE', *, *, #89446, .T. ) ;
#43262=ORIENTED_EDGE ( 'NONE', *, *, #134427, .T. ) ;
#43279=VERTEX_POINT ( 'NONE', #14740 ) ;
#43290=DIRECTION ( 'NONE',  ( -1.000000000000000000, -1.224606353822377258E-16, -0.000000000000000000 ) ) ;
#43292=CARTESIAN_POINT ( 'NONE',  ( 21.77612515620402078, 4.584330080086930965E-16, 0.000000000000000000 ) ) ;
#43304=EDGE_CURVE ( 'NONE', #22488, #93303, #16127, .T. ) ;
#43307=EDGE_CURVE ( 'NONE', #32697, #117017, #89069, .T. ) ;
#43404=VERTEX_POINT ( 'NONE', #63284 ) ;
#43415=AXIS2_PLACEMENT_3D ( 'NONE', #114022, #138646, #125633 ) ;
#43428=AXIS2_PLACEMENT_3D ( 'NONE', #34728, #91945, #102132 ) ;
#43440=CIRCLE ( 'NONE', #75845, 2.055000000000000604 ) ;
#43442=AXIS2_PLACEMENT_3D ( 'NONE', #126326, #113295, #69853 ) ;
#43509=CYLINDRICAL_SURFACE ( 'NONE', #117796, 2.500000000000000444 ) ;
#43574=AXIS2_PLACEMENT_3D ( 'NONE', #21144, #38805, #82321 ) ;
#43588=CARTESIAN_POINT ( 'NONE',  ( 1.353980332882009252, 4.584330080086930965E-16, 0.000000000000000000 ) ) ;
#43596=DIRECTION ( 'NONE',  ( -1.000000000000000000, -1.224606353822377258E-16, -0.000000000000000000 ) ) ;
#43679=DIRECTION ( 'NONE',  ( -1.000000000000000000, -1.224606353822377258E-16, -0.000000000000000000 ) ) ;
#43682=ORIENTED_EDGE ( 'NONE', *, *, #5464, .F. ) ;
#43739=EDGE_CURVE ( 'NONE', #8017, #7243, #81278, .T. ) ;
#43740=DIRECTION ( 'NONE',  ( 0.000000000000000000, -1.000000000000000000, 0.000000000000000000 ) ) ;
#43772=CIRCLE ( 'NONE', #127161, 2.500000000000000444 ) ;
#43785=CARTESIAN_POINT ( 'NONE',  ( -12.69999999999998153, 0.000000000000000000, 0.000000000000000000 ) ) ;
#43822=CARTESIAN_POINT ( 'NONE',  ( 14.39532882439692862, -2.055000000000000160, 0.000000000000000000 ) ) ;
#43823=ADVANCED_FACE ( 'NONE', ( #141336 ), #65753, .T. ) ;
#43825=FACE_OUTER_BOUND ( 'NONE', #140763, .T. ) ;
#43861=ORIENTED_EDGE ( 'NONE', *, *, #19614, .F. ) ;
#43980=VECTOR ( 'NONE', #141817, 1000.000000000000000 ) ;
#43983=CIRCLE ( 'NONE', #108817, 2.500000000000000444 ) ;
#43985=DIRECTION ( 'NONE',  ( 0.000000000000000000, 0.000000000000000000, 1.000000000000000000 ) ) ;
#44009=VERTEX_POINT ( 'NONE', #53635 ) ;
#44014=AXIS2_PLACEMENT_3D ( 'NONE', #93739, #36505, #27759 ) ;
#44065=CARTESIAN_POINT ( 'NONE',  ( -12.69999999999998153, 0.000000000000000000, 0.000000000000000000 ) ) ;
#44083=AXIS2_PLACEMENT_3D ( 'NONE', #100416, #75811, #53317 ) ;
#44112=DIRECTION ( 'NONE',  ( -0.5735764363510499342, -0.8191520442889891340, 0.000000000000000000 ) ) ;
#44120=FACE_OUTER_BOUND ( 'NONE', #21174, .T. ) ;
#44142=ADVANCED_FACE ( 'NONE', ( #71648 ), #15090, .T. ) ;
#44186=CARTESIAN_POINT ( 'NONE',  ( 2.613322195557306049, -2.055000000000000160, 2.789133085058097101E-16 ) ) ;
#44259=ORIENTED_EDGE ( 'NONE', *, *, #63457, .T. ) ;
#44263=AXIS2_PLACEMENT_3D ( 'NONE', #67311, #37542, #3438 ) ;
#44288=CARTESIAN_POINT ( 'NONE',  ( 20.20519093902540320, 4.584330080086930965E-16, 0.000000000000000000 ) ) ;
#44330=CARTESIAN_POINT ( 'NONE',  ( 0.2569208697893812232, 0.4000000000000001332, -2.015694669338588429 ) ) ;
#44400=ORIENTED_EDGE ( 'NONE', *, *, #5130, .F. ) ;
#44429=CARTESIAN_POINT ( 'NONE',  ( 1.353980332882009252, 4.584330080086930965E-16, 0.000000000000000000 ) ) ;
#44457=CARTESIAN_POINT ( 'NONE',  ( -12.69999999999998153, 3.061616997868383634E-16, -2.500000000000000444 ) ) ;
#44493=LINE ( 'NONE', #122723, #41899 ) ;
#44507=CARTESIAN_POINT ( 'NONE',  ( 21.46453280170069888, 4.202752102959690472E-16, 0.000000000000000000 ) ) ;
#44516=VECTOR ( 'NONE', #70057, 1000.000000000000000 ) ;
#44535=CYLINDRICAL_SURFACE ( 'NONE', #57, 2.500000000000000444 ) ;
#44568=EDGE_LOOP ( 'NONE', ( #96405, #98014, #41200, #78570, #93717 ) ) ;
#44695=CIRCLE ( 'NONE', #114069, 2.500000000000000444 ) ;
#44712=CARTESIAN_POINT ( 'NONE',  ( 14.70692117890024697, 4.584330080086930965E-16, 0.000000000000000000 ) ) ;
#44748=AXIS2_PLACEMENT_3D ( 'NONE', #30126, #115138, #85215 ) ;
#44758=VECTOR ( 'NONE', #50674, 1000.000000000000000 ) ;
#44761=DIRECTION ( 'NONE',  ( 0.000000000000000000, -1.000000000000000000, 0.000000000000000000 ) ) ;
#44824=DIRECTION ( 'NONE',  ( 1.000000000000000000, 1.224606353822377258E-16, 0.000000000000000000 ) ) ;
#44831=ORIENTED_EDGE ( 'NONE', *, *, #15657, .F. ) ;
#44852=DIRECTION ( 'NONE',  ( 8.673617379884034239E-17, -1.000000000000000000, 0.000000000000000000 ) ) ;
#44869=DIRECTION ( 'NONE',  ( 0.000000000000000000, -1.000000000000000000, 0.000000000000000000 ) ) ;
#44873=DIRECTION ( 'NONE',  ( -1.000000000000000000, -1.224606353822377258E-16, -0.000000000000000000 ) ) ;
#44881=ORIENTED_EDGE ( 'NONE', *, *, #106769, .F. ) ;
#44903=VERTEX_POINT ( 'NONE', #55729 ) ;
#44967=VECTOR ( 'NONE', #10512, 1000.000000000000000 ) ;
#44976=LINE ( 'NONE', #121746, #106792 ) ;
#45004=CIRCLE ( 'NONE', #123723, 2.500000000000000444 ) ;
#45014=DIRECTION ( 'NONE',  ( -1.000000000000000000, -1.224606353822377258E-16, -0.000000000000000000 ) ) ;
#45034=CARTESIAN_POINT ( 'NONE',  ( -12.69999999999998153, 0.000000000000000000, 2.500000000000000444 ) ) ;
#45062=VERTEX_POINT ( 'NONE', #49000 ) ;
#45096=CARTESIAN_POINT ( 'NONE',  ( 3.398789304146613954, 4.202752102959690472E-16, 0.000000000000000000 ) ) ;
#45109=CARTESIAN_POINT ( 'NONE',  ( 3.710381658649933634, 4.584330080086930965E-16, 0.000000000000000000 ) ) ;
#45183=CARTESIAN_POINT ( 'NONE',  ( 3.710381658649933634, 4.584330080086930965E-16, 0.000000000000000000 ) ) ;
#45185=CARTESIAN_POINT ( 'NONE',  ( 10.46799328145038821, 2.055000000000001048, 0.000000000000000000 ) ) ;
#45208=ORIENTED_EDGE ( 'NONE', *, *, #114345, .T. ) ;
#45225=DIRECTION ( 'NONE',  ( -1.000000000000000000, -1.224606353822377258E-16, -0.000000000000000000 ) ) ;
#45230=ADVANCED_FACE ( 'NONE', ( #30074 ), #96107, .T. ) ;
#45267=FACE_OUTER_BOUND ( 'NONE', #143342, .T. ) ;
#45270=ORIENTED_EDGE ( 'NONE', *, *, #134671, .T. ) ;
#45281=DIRECTION ( 'NONE',  ( 0.000000000000000000, -1.000000000000000000, 0.000000000000000000 ) ) ;
#45300=CARTESIAN_POINT ( 'NONE',  ( 11.56505274454301357, -2.500000000000000444, 3.061616997868384127E-16 ) ) ;
#45305=DIRECTION ( 'NONE',  ( 0.000000000000000000, -1.000000000000000000, 0.000000000000000000 ) ) ;
#45369=ORIENTED_EDGE ( 'NONE', *, *, #141059, .F. ) ;
#45379=DIRECTION ( 'NONE',  ( -1.000000000000000000, -1.224606353822377258E-16, -0.000000000000000000 ) ) ;
#45434=DIRECTION ( 'NONE',  ( 0.5735764363510444941, 0.8191520442889929088, 0.000000000000000000 ) ) ;
#45439=ORIENTED_EDGE ( 'NONE', *, *, #67785, .T. ) ;
#45469=ADVANCED_FACE ( 'NONE', ( #114067 ), #123877, .T. ) ;
#45481=ORIENTED_EDGE ( 'NONE', *, *, #43307, .F. ) ;
#45543=DIRECTION ( 'NONE',  ( 0.000000000000000000, -1.000000000000000000, 0.000000000000000000 ) ) ;
#45596=VERTEX_POINT ( 'NONE', #109612 ) ;
#45659=DIRECTION ( 'NONE',  ( 0.000000000000000000, -1.000000000000000000, 0.000000000000000000 ) ) ;
#45668=DIRECTION ( 'NONE',  ( 1.734723475976806848E-16, -1.000000000000000000, 0.000000000000000000 ) ) ;
#45719=CYLINDRICAL_SURFACE ( 'NONE', #73075, 2.500000000000000444 ) ;
#45826=ORIENTED_EDGE ( 'NONE', *, *, #69367, .F. ) ;
#45869=CARTESIAN_POINT ( 'NONE',  ( 15.18079593298623564, -2.055000000000000160, 2.789133085058097101E-16 ) ) ;
#45924=CARTESIAN_POINT ( 'NONE',  ( 1.554198618961949441, -0.3999999999999997446, -2.412907390626681359 ) ) ;
#45932=CARTESIAN_POINT ( 'NONE',  ( 0.7307956238753654521, 0.3999999999999995226, 2.467792535850613866 ) ) ;
#45961=CARTESIAN_POINT ( 'NONE',  ( 1.592112687295236917, 0.3999999999999995226, 2.358007167714498475 ) ) ;
#45996=EDGE_CURVE ( 'NONE', #126491, #59163, #112171, .T. ) ;
#46001=CARTESIAN_POINT ( 'NONE',  ( 1.249915061292911078, -0.4000000000000004108, 2.317232259782045389 ) ) ;
#46004=EDGE_CURVE ( 'NONE', #52143, #95691, #7245, .T. ) ;
#46013=LINE ( 'NONE', #124968, #73409 ) ;
#46032=DIRECTION ( 'NONE',  ( -1.000000000000000000, -1.224606353822377258E-16, -0.000000000000000000 ) ) ;
#46034=DIRECTION ( 'NONE',  ( -1.000000000000000000, -1.224606353822377258E-16, -0.000000000000000000 ) ) ;
#46038=CIRCLE ( 'NONE', #101472, 2.337566348077130929 ) ;
#46050=CARTESIAN_POINT ( 'NONE',  ( 4.184256412735922304, 4.202752102959690472E-16, 0.000000000000000000 ) ) ;
#46078=FACE_OUTER_BOUND ( 'NONE', #49066, .T. ) ;
#46104=FACE_OUTER_BOUND ( 'NONE', #40056, .T. ) ;
#46122=VERTEX_POINT ( 'NONE', #12788 ) ;
#46128=ADVANCED_FACE ( 'NONE', ( #58517 ), #70508, .T. ) ;
#46141=AXIS2_PLACEMENT_3D ( 'NONE', #23518, #135177, #90203 ) ;
#46161=MANIFOLD_SOLID_BREP ( 'ThdSchPat', #16243 ) ;
#46190=CIRCLE ( 'NONE', #11453, 2.500000000000000444 ) ;
#46192=SURFACE_SIDE_STYLE ('',( #133881 ) ) ;
#46229=CYLINDRICAL_SURFACE ( 'NONE', #62490, 2.500000000000000444 ) ;
#46251=AXIS2_PLACEMENT_3D ( 'NONE', #82372, #70790, #37434 ) ;
#46298=AXIS2_PLACEMENT_3D ( 'NONE', #45096, #91420, #23269 ) ;
#46306=SURFACE_STYLE_FILL_AREA ( #102077 ) ;
#46343=CARTESIAN_POINT ( 'NONE',  ( 17.06332250466817158, -2.500000000000000000, 3.061616997868383634E-16 ) ) ;
#46357=CIRCLE ( 'NONE', #87910, 2.500000000000000444 ) ;
#46358=CIRCLE ( 'NONE', #129703, 2.055000000000000604 ) ;
#46363=AXIS2_PLACEMENT_3D ( 'NONE', #119894, #98186, #121345 ) ;
#46392=FACE_OUTER_BOUND ( 'NONE', #39001, .T. ) ;
#46518=ADVANCED_FACE ( 'NONE', ( #59058 ), #1721, .T. ) ;
#46548=EDGE_CURVE ( 'NONE', #141894, #36014, #142004, .T. ) ;
#46614=VECTOR ( 'NONE', #82068, 1000.000000000000000 ) ;
#46661=CARTESIAN_POINT ( 'NONE',  ( 1.353980332882009252, 4.584330080086930965E-16, 0.000000000000000000 ) ) ;
#46672=ORIENTED_EDGE ( 'NONE', *, *, #91892, .F. ) ;
#46699=VERTEX_POINT ( 'NONE', #83645 ) ;
#46720=AXIS2_PLACEMENT_3D ( 'NONE', #131793, #42664, #32483 ) ;
#46733=VERTEX_POINT ( 'NONE', #6007 ) ;
#46748=EDGE_CURVE ( 'NONE', #58598, #142779, #48305, .T. ) ;
#46760=ORIENTED_EDGE ( 'NONE', *, *, #103276, .F. ) ;
#46803=FACE_OUTER_BOUND ( 'NONE', #112788, .T. ) ;
#46810=ADVANCED_FACE ( 'NONE', ( #141573 ), #55252, .T. ) ;
#46819=ORIENTED_EDGE ( 'NONE', *, *, #53335, .F. ) ;
#46826=CYLINDRICAL_SURFACE ( 'NONE', #2122, 2.500000000000000444 ) ;
#46831=ORIENTED_EDGE ( 'NONE', *, *, #123998, .T. ) ;
#46864=DIRECTION ( 'NONE',  ( -1.734723475976806848E-16, 1.000000000000000000, 0.000000000000000000 ) ) ;
#46875=ADVANCED_FACE ( 'NONE', ( #54573 ), #119081, .T. ) ;
#46877=VECTOR ( 'NONE', #85634, 1000.000000000000000 ) ;
#46972=DIRECTION ( 'NONE',  ( -1.000000000000000000, -0.000000000000000000, -0.000000000000000000 ) ) ;
#47001=ORIENTED_EDGE ( 'NONE', *, *, #42956, .T. ) ;
#47002=DIRECTION ( 'NONE',  ( 0.000000000000000000, 0.000000000000000000, 1.000000000000000000 ) ) ;
#47016=DIRECTION ( 'NONE',  ( -1.000000000000000000, -1.224606353822377258E-16, -0.000000000000000000 ) ) ;
#47045=SHAPE_REPRESENTATION_RELATIONSHIP ( 'NONE' , 'NONE' ,  #64389, #15274 ) ;
#47084=DIRECTION ( 'NONE',  ( 1.000000000000000000, 1.224606353822377258E-16, 0.000000000000000000 ) ) ;
#47085=CIRCLE ( 'NONE', #14625, 2.500000000000000444 ) ;
#47148=EDGE_CURVE ( 'NONE', #139503, #84085, #50692, .T. ) ;
#47161=ORIENTED_EDGE ( 'NONE', *, *, #83173, .T. ) ;
#47162=ORIENTED_EDGE ( 'NONE', *, *, #103725, .F. ) ;
#47253=CARTESIAN_POINT ( 'NONE',  ( 1.042387978378689795, -2.055000000000000160, 0.000000000000000000 ) ) ;
#47264=DIRECTION ( 'NONE',  ( -1.000000000000000000, -1.224606353822377258E-16, -0.000000000000000000 ) ) ;
#47272=AXIS2_PLACEMENT_3D ( 'NONE', #112304, #47786, #125313 ) ;
#47279=ORIENTED_EDGE ( 'NONE', *, *, #84488, .T. ) ;
#47300=ORIENTED_EDGE ( 'NONE', *, *, #67462, .T. ) ;
#47310=VERTEX_POINT ( 'NONE', #1390 ) ;
#47332=CARTESIAN_POINT ( 'NONE',  ( 11.56505274454301357, 4.584330080086930965E-16, 0.000000000000000000 ) ) ;
#47352=B_SPLINE_CURVE_WITH_KNOTS ( 'NONE', 3,
 ( #20683, #137675, #52602, #38347 ),
 .UNSPECIFIED., .F., .F.,
 ( 4, 4 ),
 ( 0.008853860144884173958, 0.009403245473020183098 ),
 .UNSPECIFIED. ) ;
#47371=DIRECTION ( 'NONE',  ( 1.318980745116185161E-16, -1.000000000000000000, 0.000000000000000000 ) ) ;
#47385=ORIENTED_EDGE ( 'NONE', *, *, #77224, .T. ) ;
#47408=VERTEX_POINT ( 'NONE', #114455 ) ;
#47463=DIRECTION ( 'NONE',  ( -1.000000000000000000, -1.224606353822377258E-16, -0.000000000000000000 ) ) ;
#47495=EDGE_CURVE ( 'NONE', #36972, #45062, #1999, .T. ) ;
#47513=CARTESIAN_POINT ( 'NONE',  ( 2.924914550060625285, 4.584330080086930965E-16, 0.000000000000000000 ) ) ;
#47534=FACE_OUTER_BOUND ( 'NONE', #30858, .T. ) ;
#47535=CARTESIAN_POINT ( 'NONE',  ( -12.69999999999998153, 0.000000000000000000, 0.000000000000000000 ) ) ;
#47553=ORIENTED_EDGE ( 'NONE', *, *, #134919, .F. ) ;
#47556=ORIENTED_EDGE ( 'NONE', *, *, #4926, .F. ) ;
#47590=EDGE_CURVE ( 'NONE', #59910, #135742, #97101, .T. ) ;
#47600=VECTOR ( 'NONE', #11258, 1000.000000000000000 ) ;
#47605=ORIENTED_EDGE ( 'NONE', *, *, #58443, .T. ) ;
#47654=CARTESIAN_POINT ( 'NONE',  ( 3.710381658649933634, -9.629649721936179265E-32, 2.500000000000000444 ) ) ;
#47687=DIRECTION ( 'NONE',  ( -1.000000000000000000, -1.224606353822377258E-16, -0.000000000000000000 ) ) ;
#47704=ADVANCED_FACE ( 'NONE', ( #70133 ), #141108, .T. ) ;
#47720=ORIENTED_EDGE ( 'NONE', *, *, #94022, .T. ) ;
#47765=CARTESIAN_POINT ( 'NONE',  ( 4.184256412735922304, 4.202752102959690472E-16, 0.000000000000000000 ) ) ;
#47770=CARTESIAN_POINT ( 'NONE',  ( 5.281315875828549444, 4.584330080086930965E-16, 0.000000000000000000 ) ) ;
#47779=ORIENTED_EDGE ( 'NONE', *, *, #10089, .T. ) ;
#47786=DIRECTION ( 'NONE',  ( 1.000000000000000000, 1.224606353822377258E-16, 0.000000000000000000 ) ) ;
#47787=CARTESIAN_POINT ( 'NONE',  ( 21.15294044719737698, 2.499999999999998224, 3.061616997868380183E-16 ) ) ;
#47799=ORIENTED_EDGE ( 'NONE', *, *, #65974, .F. ) ;
#47818=ORIENTED_EDGE ( 'NONE', *, *, #20794, .T. ) ;
#47831=DIRECTION ( 'NONE',  ( 0.5735764363510444941, 0.8191520442889929088, 0.000000000000000000 ) ) ;
#47845=CONICAL_SURFACE ( 'NONE', #124273, 2.055000000000000604, 0.9599310885968764806 ) ;
#47863=DIRECTION ( 'NONE',  ( -1.000000000000000000, -1.224606353822377258E-16, -0.000000000000000000 ) ) ;
#47897=EDGE_LOOP ( 'NONE', ( #27854, #87508 ) ) ;
#47916=CARTESIAN_POINT ( 'NONE',  ( 0.5685132242927012358, -0.4000000000000004108, 2.467792535850613866 ) ) ;
#47940=DIRECTION ( 'NONE',  ( 0.5735764363510448272, -0.8191520442889927978, 1.003171929053526103E-16 ) ) ;
#47956=EDGE_LOOP ( 'NONE', ( #43861, #13118, #51294, #111569, #101127 ) ) ;
#47958=AXIS2_PLACEMENT_3D ( 'NONE', #89566, #122178, #110581 ) ;
#47970=AXIS2_PLACEMENT_3D ( 'NONE', #86734, #7707, #43230 ) ;
#48017=DIRECTION ( 'NONE',  ( -1.000000000000000000, -1.224606353822377258E-16, -0.000000000000000000 ) ) ;
#48041=CARTESIAN_POINT ( 'NONE',  ( 1.249915201643648333, 0.3999999999999995226, 2.317232462839659668 ) ) ;
#48136=CARTESIAN_POINT ( 'NONE',  ( 3.710381658649933190, 2.500000000000000888, 0.000000000000000000 ) ) ;
#48165=FACE_OUTER_BOUND ( 'NONE', #125787, .T. ) ;
#48169=DIRECTION ( 'NONE',  ( 0.000000000000000000, -1.000000000000000000, 0.000000000000000000 ) ) ;
#48215=VERTEX_POINT ( 'NONE', #60313 ) ;
#48224=DIRECTION ( 'NONE',  ( 1.000000000000000000, 1.224606353822377258E-16, 0.000000000000000000 ) ) ;
#48239=CIRCLE ( 'NONE', #52777, 2.055000000000000604 ) ;
#48246=DIRECTION ( 'NONE',  ( -1.000000000000000000, -1.224606353822377258E-16, -0.000000000000000000 ) ) ;
#48249=CARTESIAN_POINT ( 'NONE',  ( 6.852250093007166143, 4.584330080086930965E-16, 0.000000000000000000 ) ) ;
#48250=ORIENTED_EDGE ( 'NONE', *, *, #63158, .T. ) ;
#48273=ORIENTED_EDGE ( 'NONE', *, *, #137601, .T. ) ;
#48293=ADVANCED_FACE ( 'NONE', ( #87751 ), #138866, .T. ) ;
#48305=CIRCLE ( 'NONE', #57547, 2.500000000000000444 ) ;
#48359=DIRECTION ( 'NONE',  ( 0.000000000000000000, -1.000000000000000000, 0.000000000000000000 ) ) ;
#48364=DIRECTION ( 'NONE',  ( 0.000000000000000000, -1.000000000000000000, 0.000000000000000000 ) ) ;
#48398=( NAMED_UNIT ( * ) SI_UNIT ( $, .STERADIAN. ) SOLID_ANGLE_UNIT ( ) );
#48423=EDGE_LOOP ( 'NONE', ( #112054, #114393, #53768, #82450 ) ) ;
#48425=ORIENTED_EDGE ( 'NONE', *, *, #23362, .T. ) ;
#48442=FACE_OUTER_BOUND ( 'NONE', #54509, .T. ) ;
#48493=ORIENTED_EDGE ( 'NONE', *, *, #142124, .T. ) ;
#48498=ORIENTED_EDGE ( 'NONE', *, *, #3250, .F. ) ;
#48512=DIRECTION ( 'NONE',  ( 0.000000000000000000, -1.000000000000000000, 0.000000000000000000 ) ) ;
#48536=EDGE_CURVE ( 'NONE', #99466, #70483, #99309, .T. ) ;
#48600=CARTESIAN_POINT ( 'NONE',  ( 0.7307956238753654521, -0.4000000000000004108, 2.467792535850613866 ) ) ;
#48651=LINE ( 'NONE', #95708, #125390 ) ;
#48656=VECTOR ( 'NONE', #18171, 1000.000000000000000 ) ;
#48684=LINE ( 'NONE', #104471, #124898 ) ;
#48723=EDGE_CURVE ( 'NONE', #123895, #13745, #19461, .T. ) ;
#48730=ORIENTED_EDGE ( 'NONE', *, *, #78222, .T. ) ;
#48734=VECTOR ( 'NONE', #55132, 1000.000000000000000 ) ;
#48735=CARTESIAN_POINT ( 'NONE',  ( 2.924914550060625729, -2.500000000000000000, 3.061616997868383634E-16 ) ) ;
#48745=CIRCLE ( 'NONE', #120496, 2.500000000000000444 ) ;
#48802=AXIS2_PLACEMENT_3D ( 'NONE', #131872, #87644, #21678 ) ;
#48811=AXIS2_PLACEMENT_3D ( 'NONE', #59934, #96096, #128052 ) ;
#48813=ORIENTED_EDGE ( 'NONE', *, *, #74258, .F. ) ;
#48819=ORIENTED_EDGE ( 'NONE', *, *, #126081, .T. ) ;
#48939=FACE_OUTER_BOUND ( 'NONE', #120152, .T. ) ;
#48969=EDGE_CURVE ( 'NONE', #104746, #103339, #37127, .T. ) ;
#48970=DIRECTION ( 'NONE',  ( 1.734723475976806848E-16, -1.000000000000000000, 0.000000000000000000 ) ) ;
#48977=DIRECTION ( 'NONE',  ( -1.000000000000000000, -0.000000000000000000, -0.000000000000000000 ) ) ;
#49000=CARTESIAN_POINT ( 'NONE',  ( 18.79653912142945060, 2.499999999999998224, 3.061616997868380183E-16 ) ) ;
#49005=ORIENTED_EDGE ( 'NONE', *, *, #79583, .F. ) ;
#49033=CARTESIAN_POINT ( 'NONE',  ( 19.58200623001875940, 3.821174125832445049E-16, 0.000000000000000000 ) ) ;
#49035=ORIENTED_EDGE ( 'NONE', *, *, #83712, .F. ) ;
#49066=EDGE_LOOP ( 'NONE', ( #119730, #77229, #50069, #13595, #47799 ) ) ;
#49083=AXIS2_PLACEMENT_3D ( 'NONE', #115029, #37527, #90466 ) ;
#49120=AXIS2_PLACEMENT_3D ( 'NONE', #24734, #114587, #134965 ) ;
#49131=LINE ( 'NONE', #139715, #16886 ) ;
#49183=CONICAL_SURFACE ( 'NONE', #130209, 2.500000000000000444, 0.9599310885968830309 ) ;
#49184=ADVANCED_FACE ( 'NONE', ( #110678 ), #56388, .T. ) ;
#49193=CIRCLE ( 'NONE', #118599, 2.500000000000000444 ) ;
#49199=DIRECTION ( 'NONE',  ( 0.5735764363510444941, 0.8191520442889929088, 0.000000000000000000 ) ) ;
#49296=VECTOR ( 'NONE', #12737, 1000.000000000000000 ) ;
#49380=CARTESIAN_POINT ( 'NONE',  ( 17.06332250466817158, 3.061616997868383634E-16, -2.500000000000000444 ) ) ;
#49385=DIRECTION ( 'NONE',  ( -1.000000000000000000, -1.224606353822377258E-16, -0.000000000000000000 ) ) ;
#49504=AXIS2_PLACEMENT_3D ( 'NONE', #35967, #88922, #57011 ) ;
#49558=VECTOR ( 'NONE', #14187, 1000.000000000000000 ) ;
#49564=EDGE_CURVE ( 'NONE', #70483, #94208, #4781, .T. ) ;
#49676=EDGE_LOOP ( 'NONE', ( #107165, #48813, #137232, #108029, #137858, #135447, #11527, #121776, #30124, #116217, #68086, #64312, #37028, #120114, #53655, #118650, #30181, #65479 ) ) ;
#49682=AXIS2_PLACEMENT_3D ( 'NONE', #106560, #130512, #107300 ) ;
#49689=VECTOR ( 'NONE', #28116, 1000.000000000000000 ) ;
#49692=ORIENTED_EDGE ( 'NONE', *, *, #63158, .F. ) ;
#49769=DIRECTION ( 'NONE',  ( 1.000000000000000000, 0.000000000000000000, -0.000000000000000000 ) ) ;
#49790=ORIENTED_EDGE ( 'NONE', *, *, #4391, .F. ) ;
#49811=DIRECTION ( 'NONE',  ( -0.5735764363510499342, -0.8191520442889891340, 0.000000000000000000 ) ) ;
#49840=CARTESIAN_POINT ( 'NONE',  ( -12.69999999999998153, 3.061616997868383634E-16, -2.500000000000000444 ) ) ;
#49856=CIRCLE ( 'NONE', #130883, 2.500000000000000444 ) ;
#49897=DIRECTION ( 'NONE',  ( 1.000000000000000000, 1.224606353822377258E-16, 0.000000000000000000 ) ) ;
#49909=CARTESIAN_POINT ( 'NONE',  ( 12.35051985313232237, 2.500000000000000888, 0.000000000000000000 ) ) ;
#49911=PLANE ( 'NONE',  #129693 ) ;
#49930=EDGE_CURVE ( 'NONE', #123895, #117989, #57679, .T. ) ;
#49949=DIRECTION ( 'NONE',  ( -1.000000000000000000, -0.000000000000000000, -0.000000000000000000 ) ) ;
#49967=EDGE_LOOP ( 'NONE', ( #139094, #130505, #64702, #35282, #1917, #114667 ) ) ;
#49983=CARTESIAN_POINT ( 'NONE',  ( 18.79653912142945060, 3.821174125832445049E-16, 0.000000000000000000 ) ) ;
#49999=EDGE_CURVE ( 'NONE', #7107, #9950, #69151, .T. ) ;
#50041=CARTESIAN_POINT ( 'NONE',  ( 1.629999999999999893, 0.4000000000000001887, -2.303088455023527104 ) ) ;
#50063=ADVANCED_FACE ( 'NONE', ( #115153 ), #136283, .T. ) ;
#50069=ORIENTED_EDGE ( 'NONE', *, *, #127874, .T. ) ;
#50072=ADVANCED_FACE ( 'NONE', ( #17980 ), #107160, .T. ) ;
#50156=DIRECTION ( 'NONE',  ( -1.000000000000000000, -0.000000000000000000, -0.000000000000000000 ) ) ;
#50157=ORIENTED_EDGE ( 'NONE', *, *, #132798, .T. ) ;
#50178=CARTESIAN_POINT ( 'NONE',  ( 4.184256412735922304, 2.055000000000001048, 0.000000000000000000 ) ) ;
#50256=CIRCLE ( 'NONE', #66406, 2.500000000000000444 ) ;
#50281=EDGE_CURVE ( 'NONE', #39184, #56350, #141041, .T. ) ;
#50286=EDGE_CURVE ( 'NONE', #51035, #95691, #138796, .T. ) ;
#50361=ORIENTED_EDGE ( 'NONE', *, *, #52987, .F. ) ;
#50384=ORIENTED_EDGE ( 'NONE', *, *, #4841, .F. ) ;
#50414=ORIENTED_EDGE ( 'NONE', *, *, #110596, .F. ) ;
#50442=ADVANCED_FACE ( 'NONE', ( #40353 ), #108619, .T. ) ;
#50515=DIRECTION ( 'NONE',  ( 0.000000000000000000, -1.000000000000000000, 0.000000000000000000 ) ) ;
#50672=EDGE_CURVE ( 'NONE', #42023, #79690, #46190, .T. ) ;
#50674=DIRECTION ( 'NONE',  ( -1.000000000000000000, -0.000000000000000000, -0.000000000000000000 ) ) ;
#50692=CIRCLE ( 'NONE', #89994, 1.749999999999999778 ) ;
#50716=LINE ( 'NONE', #117364, #133357 ) ;
#50721=ORIENTED_EDGE ( 'NONE', *, *, #13226, .T. ) ;
#50736=CARTESIAN_POINT ( 'NONE',  ( 6.540657738503846907, 4.202752102959690472E-16, 0.000000000000000000 ) ) ;
#50779=DIRECTION ( 'NONE',  ( -1.000000000000000000, -0.000000000000000000, -0.000000000000000000 ) ) ;
#50807=VERTEX_POINT ( 'NONE', #110548 ) ;
#50809=CIRCLE ( 'NONE', #6770, 2.500000000000000444 ) ;
#50819=DIRECTION ( 'NONE',  ( -0.5735764363510501562, 0.8191520442889890230, 1.003171929053521419E-16 ) ) ;
#50831=VECTOR ( 'NONE', #49949, 1000.000000000000000 ) ;
#50840=ORIENTED_EDGE ( 'NONE', *, *, #17954, .T. ) ;
#50864=EDGE_LOOP ( 'NONE', ( #93942, #54612, #106597, #129719, #41083 ) ) ;
#50921=VECTOR ( 'NONE', #58603, 1000.000000000000000 ) ;
#51001=ORIENTED_EDGE ( 'NONE', *, *, #123643, .F. ) ;
#51031=EDGE_CURVE ( 'NONE', #117931, #80430, #140868, .T. ) ;
#51035=VERTEX_POINT ( 'NONE', #142340 ) ;
#51056=DIRECTION ( 'NONE',  ( 0.000000000000000000, -1.000000000000000000, 0.000000000000000000 ) ) ;
#51066=AXIS2_PLACEMENT_3D ( 'NONE', #63827, #42077, #108699 ) ;
#51088=DIRECTION ( 'NONE',  ( 0.000000000000000000, 0.000000000000000000, 1.000000000000000000 ) ) ;
#51162=ORIENTED_EDGE ( 'NONE', *, *, #85604, .T. ) ;
#51175=DIRECTION ( 'NONE',  ( 0.000000000000000000, -1.000000000000000000, 0.000000000000000000 ) ) ;
#51181=AXIS2_PLACEMENT_3D ( 'NONE', #39544, #28667, #130111 ) ;
#51185=CARTESIAN_POINT ( 'NONE',  ( 9.208651418775088970, 4.584330080086930965E-16, 0.000000000000000000 ) ) ;
#51194=AXIS2_PLACEMENT_3D ( 'NONE', #107471, #8134, #52373 ) ;
#51256=DIRECTION ( 'NONE',  ( 0.5735764363510444941, 0.8191520442889929088, 0.000000000000000000 ) ) ;
#51277=VERTEX_POINT ( 'NONE', #122698 ) ;
#51294=ORIENTED_EDGE ( 'NONE', *, *, #67568, .T. ) ;
#51350=DIRECTION ( 'NONE',  ( -1.000000000000000000, -0.000000000000000000, -0.000000000000000000 ) ) ;
#51375=CARTESIAN_POINT ( 'NONE',  ( 19.58200623001875940, -2.499999999999996447, 0.000000000000000000 ) ) ;
#51443=EDGE_CURVE ( 'NONE', #93248, #33386, #71212, .T. ) ;
#51463=ORIENTED_EDGE ( 'NONE', *, *, #34020, .F. ) ;
#51507=VERTEX_POINT ( 'NONE', #63205 ) ;
#51529=EDGE_CURVE ( 'NONE', #15565, #23831, #16208, .T. ) ;
#51537=EDGE_CURVE ( 'NONE', #93024, #66606, #118033, .T. ) ;
#51564=EDGE_CURVE ( 'NONE', #110816, #111848, #103855, .T. ) ;
#51595=CIRCLE ( 'NONE', #95534, 2.055000000000000604 ) ;
#51610=DIRECTION ( 'NONE',  ( -1.000000000000000000, -1.224606353822377258E-16, -0.000000000000000000 ) ) ;
#51642=ORIENTED_EDGE ( 'NONE', *, *, #81155, .F. ) ;
#51689=DIRECTION ( 'NONE',  ( 0.000000000000000000, -1.000000000000000000, 0.000000000000000000 ) ) ;
#51696=DIRECTION ( 'NONE',  ( 1.000000000000000000, 1.224606353822377258E-16, 0.000000000000000000 ) ) ;
#51717=ADVANCED_FACE ( 'NONE', ( #76929 ), #91190, .T. ) ;
#51775=CARTESIAN_POINT ( 'NONE',  ( -12.69999999999998153, 0.000000000000000000, 2.500000000000000444 ) ) ;
#51778=EDGE_CURVE ( 'NONE', #90362, #121849, #74100, .T. ) ;
#51804=AXIS2_PLACEMENT_3D ( 'NONE', #83191, #16469, #17887 ) ;
#51812=DIRECTION ( 'NONE',  ( -1.000000000000000000, -1.224606353822377258E-16, -0.000000000000000000 ) ) ;
#51833=CIRCLE ( 'NONE', #40260, 2.256103126841972895 ) ;
#51895=EDGE_LOOP ( 'NONE', ( #72517, #33674, #73442, #54590, #51642 ) ) ;
#51932=DIRECTION ( 'NONE',  ( -1.000000000000000000, -1.224606353822377258E-16, -0.000000000000000000 ) ) ;
#52000=CARTESIAN_POINT ( 'NONE',  ( 11.56505274454301357, 0.000000000000000000, 2.500000000000000444 ) ) ;
#52007=VECTOR ( 'NONE', #127805, 1000.000000000000000 ) ;
#52021=EDGE_CURVE ( 'NONE', #73316, #59163, #102596, .T. ) ;
#52034=ADVANCED_FACE ( 'NONE', ( #47534 ), #46826, .T. ) ;
#52057=FACE_OUTER_BOUND ( 'NONE', #25082, .T. ) ;
#52077=EDGE_CURVE ( 'NONE', #19525, #21831, #43772, .T. ) ;
#52097=CARTESIAN_POINT ( 'NONE',  ( -12.69999999999998153, 0.000000000000000000, 2.500000000000000444 ) ) ;
#52143=VERTEX_POINT ( 'NONE', #94533 ) ;
#52151=DIRECTION ( 'NONE',  ( 0.000000000000000000, 1.000000000000000000, 0.000000000000000000 ) ) ;
#52212=EDGE_LOOP ( 'NONE', ( #122282, #83433, #82793, #41822, #134397 ) ) ;
#52237=CARTESIAN_POINT ( 'NONE',  ( 1.042387978378689573, -0.3999999999999998002, -2.015694669338588429 ) ) ;
#52274=DIRECTION ( 'NONE',  ( 0.000000000000000000, -1.000000000000000000, 0.000000000000000000 ) ) ;
#52293=CARTESIAN_POINT ( 'NONE',  ( 1.042387978378689573, 4.202752102959690472E-16, 0.000000000000000000 ) ) ;
#52299=ORIENTED_EDGE ( 'NONE', *, *, #81653, .T. ) ;
#52321=DIRECTION ( 'NONE',  ( -0.5735764363510501562, 0.8191520442889890230, 1.003171929053521419E-16 ) ) ;
#52333=ORIENTED_EDGE ( 'NONE', *, *, #31725, .F. ) ;
#52339=VERTEX_POINT ( 'NONE', #75670 ) ;
#52347=EDGE_CURVE ( 'NONE', #118128, #82989, #122602, .T. ) ;
#52373=DIRECTION ( 'NONE',  ( 0.000000000000000000, 0.000000000000000000, 1.000000000000000000 ) ) ;
#52416=VERTEX_POINT ( 'NONE', #111111 ) ;
#52427=DIRECTION ( 'NONE',  ( 1.734723475976806848E-16, -1.000000000000000000, 0.000000000000000000 ) ) ;
#52436=DIRECTION ( 'NONE',  ( 0.000000000000000000, 0.000000000000000000, 1.000000000000000000 ) ) ;
#52448=EDGE_LOOP ( 'NONE', ( #64333, #7083, #58677, #2489, #65657 ) ) ;
#52483=DIRECTION ( 'NONE',  ( -1.000000000000000000, -1.224606353822377258E-16, -0.000000000000000000 ) ) ;
#52543=EDGE_CURVE ( 'NONE', #117239, #23453, #50809, .T. ) ;
#52568=ADVANCED_FACE ( 'NONE', ( #60363 ), #104061, .T. ) ;
#52598=EDGE_LOOP ( 'NONE', ( #12392, #11587, #59486, #129743 ) ) ;
#52602=CARTESIAN_POINT ( 'NONE',  ( 0.4644480930543399833, 0.3999999999999995226, 2.317232462839659668 ) ) ;
#52606=CARTESIAN_POINT ( 'NONE',  ( 19.89359858452208130, -2.055000000000000160, 0.000000000000000000 ) ) ;
#52623=DIRECTION ( 'NONE',  ( 0.000000000000000000, -1.000000000000000000, 0.000000000000000000 ) ) ;
#52629=CARTESIAN_POINT ( 'NONE',  ( 5.443598275411213550, 3.821174125832445049E-16, 0.000000000000000000 ) ) ;
#52637=CONICAL_SURFACE ( 'NONE', #8513, 2.500000000000000444, 0.9599310885968830309 ) ;
#52666=EDGE_CURVE ( 'NONE', #132148, #80135, #19675, .T. ) ;
#52680=ORIENTED_EDGE ( 'NONE', *, *, #116687, .T. ) ;
#52692=CARTESIAN_POINT ( 'NONE',  ( 0.1161069444170889225, -0.4000000000000003553, 2.220360628129160130 ) ) ;
#52694=FACE_OUTER_BOUND ( 'NONE', #142900, .T. ) ;
#52737=ORIENTED_EDGE ( 'NONE', *, *, #14416, .T. ) ;
#52777=AXIS2_PLACEMENT_3D ( 'NONE', #71335, #140835, #93788 ) ;
#52793=DIRECTION ( 'NONE',  ( 0.000000000000000000, -1.000000000000000000, 0.000000000000000000 ) ) ;
#52834=EDGE_CURVE ( 'NONE', #41149, #16173, #53352, .T. ) ;
#52878=VERTEX_POINT ( 'NONE', #20714 ) ;
#52908=ORIENTED_EDGE ( 'NONE', *, *, #69367, .T. ) ;
#52932=DIRECTION ( 'NONE',  ( -0.000000000000000000, 1.301042606982605074E-16, -1.000000000000000000 ) ) ;
#52952=VECTOR ( 'NONE', #39251, 1000.000000000000000 ) ;
#52961=FACE_OUTER_BOUND ( 'NONE', #138967, .T. ) ;
#52969=CARTESIAN_POINT ( 'NONE',  ( 22.25000000000000000, 0.000000000000000000, 0.000000000000000000 ) ) ;
#52981=EDGE_CURVE ( 'NONE', #46699, #133133, #18475, .T. ) ;
#52987=EDGE_CURVE ( 'NONE', #118149, #114653, #143514, .T. ) ;
#52996=DIRECTION ( 'NONE',  ( 1.055184596092948005E-16, -1.000000000000000000, 0.000000000000000000 ) ) ;
#53017=EDGE_LOOP ( 'NONE', ( #126749, #107705, #84386, #61066, #72352 ) ) ;
#53100=CARTESIAN_POINT ( 'NONE',  ( 0.2569208697893817228, -2.055000000000000160, 0.000000000000000000 ) ) ;
#53125=AXIS2_PLACEMENT_3D ( 'NONE', #12438, #135669, #69720 ) ;
#53174=DIRECTION ( 'NONE',  ( 0.000000000000000000, -1.000000000000000000, 0.000000000000000000 ) ) ;
#53195=DIRECTION ( 'NONE',  ( 1.000000000000000000, 0.000000000000000000, 0.000000000000000000 ) ) ;
#53203=AXIS2_PLACEMENT_3D ( 'NONE', #89287, #13122, #90736 ) ;
#53208=CARTESIAN_POINT ( 'NONE',  ( 18.63425672184678916, -2.500000000000000444, 3.061616997868384127E-16 ) ) ;
#53291=UNCERTAINTY_MEASURE_WITH_UNIT (LENGTH_MEASURE( 1.000000000000000082E-05 ), #101351, 'distance_accuracy_value', 'NONE');
#53298=EDGE_CURVE ( 'NONE', #138500, #99466, #74295, .T. ) ;
#53315=ORIENTED_EDGE ( 'NONE', *, *, #30094, .F. ) ;
#53317=DIRECTION ( 'NONE',  ( 0.000000000000000000, -1.000000000000000000, 0.000000000000000000 ) ) ;
#53331=ORIENTED_EDGE ( 'NONE', *, *, #23507, .T. ) ;
#53335=EDGE_CURVE ( 'NONE', #66606, #96111, #28032, .T. ) ;
#53339=ADVANCED_FACE ( 'NONE', ( #118430 ), #37239, .T. ) ;
#53346=CONICAL_SURFACE ( 'NONE', #65286, 2.055000000000000604, 0.9599310885968764806 ) ;
#53352=LINE ( 'NONE', #97565, #43980 ) ;
#53401=ORIENTED_EDGE ( 'NONE', *, *, #117092, .T. ) ;
#53417=CARTESIAN_POINT ( 'NONE',  ( 0.07735795229993523703, -0.4000000000000003553, 2.152165010376130727 ) ) ;
#53418=VERTEX_POINT ( 'NONE', #85098 ) ;
#53453=AXIS2_PLACEMENT_3D ( 'NONE', #131547, #99603, #34374 ) ;
#53510=AXIS2_PLACEMENT_3D ( 'NONE', #89586, #77333, #46864 ) ;
#53543=EDGE_CURVE ( 'NONE', #105369, #136234, #44493, .T. ) ;
#53589=EDGE_CURVE ( 'NONE', #140226, #97836, #90845, .T. ) ;
#53604=EDGE_LOOP ( 'NONE', ( #54936, #26911, #61804, #44400 ) ) ;
#53623=AXIS2_PLACEMENT_3D ( 'NONE', #21082, #132010, #1449 ) ;
#53635=CARTESIAN_POINT ( 'NONE',  ( 21.46453280170069888, 2.055000000000001048, 0.000000000000000000 ) ) ;
#53643=ORIENTED_EDGE ( 'NONE', *, *, #78554, .F. ) ;
#53655=ORIENTED_EDGE ( 'NONE', *, *, #81151, .F. ) ;
#53690=VERTEX_POINT ( 'NONE', #116663 ) ;
#53696=CARTESIAN_POINT ( 'NONE',  ( 0.000000000000000000, -0.3999999999999997446, -2.500000000000000000 ) ) ;
#53718=ORIENTED_EDGE ( 'NONE', *, *, #33154, .F. ) ;
#53742=CONICAL_SURFACE ( 'NONE', #88508, 2.500000000000000444, 0.9599310885968830309 ) ;
#53761=CARTESIAN_POINT ( 'NONE',  ( 12.35051985313232237, -2.500000000000000000, 3.061616997868383634E-16 ) ) ;
#53768=ORIENTED_EDGE ( 'NONE', *, *, #40527, .F. ) ;
#53795=DIRECTION ( 'NONE',  ( -1.000000000000000000, -1.224606353822377258E-16, -0.000000000000000000 ) ) ;
#53870=ORIENTED_EDGE ( 'NONE', *, *, #119442, .F. ) ;
#53874=AXIS2_PLACEMENT_3D ( 'NONE', #9978, #31046, #65844 ) ;
#53901=CARTESIAN_POINT ( 'NONE',  ( 20.99065804761471199, -2.500000000000000444, 3.061616997868384127E-16 ) ) ;
#53970=CARTESIAN_POINT ( 'NONE',  ( 12.03892749862900402, -2.055000000000000160, 0.000000000000000000 ) ) ;
#53985=AXIS2_PLACEMENT_3D ( 'NONE', #100329, #90148, #57554 ) ;
#53989=CARTESIAN_POINT ( 'NONE',  ( 6.852250093007166143, 2.500000000000000444, 0.000000000000000000 ) ) ;
#54002=ORIENTED_EDGE ( 'NONE', *, *, #34020, .T. ) ;
#54013=ORIENTED_EDGE ( 'NONE', *, *, #104200, .T. ) ;
#54032=DIRECTION ( 'NONE',  ( -1.000000000000000000, -1.224606353822377258E-16, -0.000000000000000000 ) ) ;
#54037=CARTESIAN_POINT ( 'NONE',  ( 12.03892749862900402, -2.055000000000000160, 2.789133085058097101E-16 ) ) ;
#54109=EDGE_CURVE ( 'NONE', #12173, #103754, #104666, .T. ) ;
#54116=ORIENTED_EDGE ( 'NONE', *, *, #46548, .T. ) ;
#54123=ORIENTED_EDGE ( 'NONE', *, *, #101258, .T. ) ;
#54129=EDGE_CURVE ( 'NONE', #117239, #58140, #96148, .T. ) ;
#54177=ORIENTED_EDGE ( 'NONE', *, *, #60749, .F. ) ;
#54289=ORIENTED_EDGE ( 'NONE', *, *, #70056, .T. ) ;
#54329=ADVANCED_FACE ( 'NONE', ( #46104 ), #132478, .T. ) ;
#54395=DIRECTION ( 'NONE',  ( -1.000000000000000000, -1.224606353822377258E-16, -0.000000000000000000 ) ) ;
#54436=AXIS2_PLACEMENT_3D ( 'NONE', #108352, #141764, #64194 ) ;
#54451=PLANE ( 'NONE',  #137155 ) ;
#54456=AXIS2_PLACEMENT_3D ( 'NONE', #5981, #61859, #103187 ) ;
#54492=FACE_OUTER_BOUND ( 'NONE', #51895, .T. ) ;
#54509=EDGE_LOOP ( 'NONE', ( #65495, #1415, #101898, #130119, #35721 ) ) ;
#54512=ORIENTED_EDGE ( 'NONE', *, *, #89962, .T. ) ;
#54531=CARTESIAN_POINT ( 'NONE',  ( 3.398789304146614398, -2.055000000000000160, 2.789133085058097101E-16 ) ) ;
#54532=ORIENTED_EDGE ( 'NONE', *, *, #134427, .F. ) ;
#54573=FACE_OUTER_BOUND ( 'NONE', #47897, .T. ) ;
#54590=ORIENTED_EDGE ( 'NONE', *, *, #117441, .T. ) ;
#54612=ORIENTED_EDGE ( 'NONE', *, *, #97689, .F. ) ;
#54643=CIRCLE ( 'NONE', #140035, 2.500000000000000444 ) ;
#54699=VERTEX_POINT ( 'NONE', #135095 ) ;
#54726=ORIENTED_EDGE ( 'NONE', *, *, #52543, .F. ) ;
#54765=CARTESIAN_POINT ( 'NONE',  ( 20.20519093902540320, 4.584330080086930965E-16, 0.000000000000000000 ) ) ;
#54817=AXIS2_PLACEMENT_3D ( 'NONE', #25028, #113464, #36624 ) ;
#54838=ADVANCED_FACE ( 'NONE', ( #28451 ), #70561, .T. ) ;
#54840=DIRECTION ( 'NONE',  ( 1.000000000000000000, 1.224606353822377258E-16, 0.000000000000000000 ) ) ;
#54904=CARTESIAN_POINT ( 'NONE',  ( 13.29826936130429260, 3.821174125832445049E-16, 0.000000000000000000 ) ) ;
#54936=ORIENTED_EDGE ( 'NONE', *, *, #110594, .F. ) ;
#54938=EDGE_LOOP ( 'NONE', ( #32546, #22524, #7411, #124846, #59956, #136505 ) ) ;
#54971=CARTESIAN_POINT ( 'NONE',  ( 7.326124847093153925, 2.055000000000001048, 0.000000000000000000 ) ) ;
#54978=CIRCLE ( 'NONE', #22530, 2.500000000000000444 ) ;
#54984=ORIENTED_EDGE ( 'NONE', *, *, #127067, .T. ) ;
#54995=DIRECTION ( 'NONE',  ( 0.000000000000000000, -1.000000000000000000, 0.000000000000000000 ) ) ;
#55017=ORIENTED_EDGE ( 'NONE', *, *, #60531, .T. ) ;
#55044=ORIENTED_EDGE ( 'NONE', *, *, #91762, .T. ) ;
#55072=CIRCLE ( 'NONE', #69052, 2.500000000000000444 ) ;
#55100=DIRECTION ( 'NONE',  ( -1.000000000000000000, -1.224606353822377258E-16, -0.000000000000000000 ) ) ;
#55131=DIRECTION ( 'NONE',  ( 0.000000000000000000, -1.000000000000000000, 0.000000000000000000 ) ) ;
#55132=DIRECTION ( 'NONE',  ( 0.5735764363510444941, 0.8191520442889929088, 0.000000000000000000 ) ) ;
#55187=CONICAL_SURFACE ( 'NONE', #138487, 2.500000000000000444, 0.9599310885968830309 ) ;
#55193=EDGE_LOOP ( 'NONE', ( #95839, #125568, #42299, #69067, #138683 ) ) ;
#55201=LINE ( 'NONE', #122572, #95343 ) ;
#55213=ORIENTED_EDGE ( 'NONE', *, *, #115258, .T. ) ;
#55225=EDGE_LOOP ( 'NONE', ( #114450, #44831, #18648, #10750, #54512 ) ) ;
#55252=CONICAL_SURFACE ( 'NONE', #38995, 2.500000000000000444, 0.9599310885968830309 ) ;
#55290=CARTESIAN_POINT ( 'NONE',  ( 17.84878961325748037, 2.500000000000000888, 0.000000000000000000 ) ) ;
#55310=DIRECTION ( 'NONE',  ( 0.000000000000000000, 1.000000000000000000, 0.000000000000000000 ) ) ;
#55322=CARTESIAN_POINT ( 'NONE',  ( 10.94186803553636977, 3.061616997868383634E-16, -2.500000000000000444 ) ) ;
#55333=ORIENTED_EDGE ( 'NONE', *, *, #9387, .F. ) ;
#55363=CARTESIAN_POINT ( 'NONE',  ( 12.03892749862900402, 2.055000000000001048, 0.000000000000000000 ) ) ;
#55432=DIRECTION ( 'NONE',  ( 0.000000000000000000, -1.000000000000000000, 0.000000000000000000 ) ) ;
#55477=AXIS2_PLACEMENT_3D ( 'NONE', #94374, #29131, #95088 ) ;
#55482=EDGE_CURVE ( 'NONE', #135742, #140903, #58175, .T. ) ;
#55502=CARTESIAN_POINT ( 'NONE',  ( 3.710381658649934078, -2.500000000000000000, 3.061616997868383634E-16 ) ) ;
#55543=CONICAL_SURFACE ( 'NONE', #134182, 2.055000000000000604, 0.9599310885968764806 ) ;
#55544=CIRCLE ( 'NONE', #53125, 2.500000000000000444 ) ;
#55597=ORIENTED_EDGE ( 'NONE', *, *, #96731, .T. ) ;
#55639=CIRCLE ( 'NONE', #71909, 2.500000000000000444 ) ;
#55729=CARTESIAN_POINT ( 'NONE',  ( 2.139447441471317379, 3.061616997868383141E-16, -2.500000000000000444 ) ) ;
#55744=CIRCLE ( 'NONE', #2504, 2.500000000000000444 ) ;
#55794=ORIENTED_EDGE ( 'NONE', *, *, #79856, .F. ) ;
#55803=CARTESIAN_POINT ( 'NONE',  ( 10.77958563595370833, 2.500000000000000888, 0.000000000000000000 ) ) ;
#55913=VECTOR ( 'NONE', #129135, 1000.000000000000000 ) ;
#55934=ORIENTED_EDGE ( 'NONE', *, *, #57252, .T. ) ;
#55987=ORIENTED_EDGE ( 'NONE', *, *, #141959, .F. ) ;
#56064=ORIENTED_EDGE ( 'NONE', *, *, #42812, .T. ) ;
#56076=ORIENTED_EDGE ( 'NONE', *, *, #118850, .F. ) ;
#56077=ORIENTED_EDGE ( 'NONE', *, *, #117320, .F. ) ;
#56078=AXIS2_PLACEMENT_3D ( 'NONE', #43204, #22126, #10532 ) ;
#56084=ORIENTED_EDGE ( 'NONE', *, *, #104552, .T. ) ;
#56107=AXIS2_PLACEMENT_3D ( 'NONE', #134788, #66652, #56535 ) ;
#56134=EDGE_LOOP ( 'NONE', ( #17534, #11987, #124372, #119481, #99330 ) ) ;
#56188=AXIS2_PLACEMENT_3D ( 'NONE', #140176, #7491, #107529 ) ;
#56189=DIRECTION ( 'NONE',  ( -1.000000000000000000, -0.000000000000000000, -0.000000000000000000 ) ) ;
#56224=DIRECTION ( 'NONE',  ( 1.000000000000000000, 1.224606353822377258E-16, 0.000000000000000000 ) ) ;
#56261=CARTESIAN_POINT ( 'NONE',  ( 18.01107201284014536, 3.821174125832445049E-16, 0.000000000000000000 ) ) ;
#56269=CARTESIAN_POINT ( 'NONE',  ( 8.585466709768445170, 3.821174125832445049E-16, 0.000000000000000000 ) ) ;
#56282=ORIENTED_EDGE ( 'NONE', *, *, #17441, .F. ) ;
#56292=CARTESIAN_POINT ( 'NONE',  ( 15.49238828748955576, 2.500000000000000444, 0.000000000000000000 ) ) ;
#56301=FACE_OUTER_BOUND ( 'NONE', #114011, .T. ) ;
#56328=CARTESIAN_POINT ( 'NONE',  ( -12.69999999999998153, 0.000000000000000000, 2.500000000000000444 ) ) ;
#56329=DIRECTION ( 'NONE',  ( -1.000000000000000000, -0.000000000000000000, -0.000000000000000000 ) ) ;
#56340=STYLED_ITEM ( 'NONE', ( #68644 ), #46161 ) ;
#56350=VERTEX_POINT ( 'NONE', #69680 ) ;
#56388=CYLINDRICAL_SURFACE ( 'NONE', #60439, 2.500000000000000444 ) ;
#56429=CARTESIAN_POINT ( 'NONE',  ( 17.06332250466817158, 0.000000000000000000, 2.500000000000000444 ) ) ;
#56436=CARTESIAN_POINT ( 'NONE',  ( 7.637717201596474048, -2.500000000000000000, 3.061616997868383634E-16 ) ) ;
#56481=ORIENTED_EDGE ( 'NONE', *, *, #86557, .F. ) ;
#56535=DIRECTION ( 'NONE',  ( 0.000000000000000000, 0.000000000000000000, 1.000000000000000000 ) ) ;
#56569=CIRCLE ( 'NONE', #105139, 2.055000000000000604 ) ;
#56586=CARTESIAN_POINT ( 'NONE',  ( 11.56505274454301357, 4.584330080086930965E-16, 0.000000000000000000 ) ) ;
#56599=ORIENTED_EDGE ( 'NONE', *, *, #14184, .F. ) ;
#56614=CARTESIAN_POINT ( 'NONE',  ( 4.495848767239241539, 4.584330080086930965E-16, 0.000000000000000000 ) ) ;
#56672=CARTESIAN_POINT ( 'NONE',  ( 7.799999601179139042, 2.500000000000001776, 3.061616997868385113E-16 ) ) ;
#56673=ADVANCED_FACE ( 'NONE', ( #88394 ), #89105, .T. ) ;
#56691=DIRECTION ( 'NONE',  ( -1.000000000000000000, -1.224606353822377258E-16, -0.000000000000000000 ) ) ;
#56735=DIRECTION ( 'NONE',  ( -1.000000000000000000, -1.224606353822377258E-16, -0.000000000000000000 ) ) ;
#56831=ADVANCED_FACE ( 'NONE', ( #78779 ), #102677, .T. ) ;
#56842=ORIENTED_EDGE ( 'NONE', *, *, #29111, .T. ) ;
#56863=CARTESIAN_POINT ( 'NONE',  ( 17.84878961325748037, -2.500000000000000000, 3.061616997868383634E-16 ) ) ;
#56920=DIRECTION ( 'NONE',  ( 0.000000000000000000, -1.000000000000000000, 0.000000000000000000 ) ) ;
#56931=FACE_OUTER_BOUND ( 'NONE', #9730, .T. ) ;
#56937=EDGE_CURVE ( 'NONE', #106357, #105369, #115553, .T. ) ;
#57011=DIRECTION ( 'NONE',  ( 0.000000000000000000, 1.000000000000000000, 0.000000000000000000 ) ) ;
#57013=DIRECTION ( 'NONE',  ( 0.000000000000000000, 4.440892098500626162E-15, -1.000000000000000000 ) ) ;
#57022=LINE ( 'NONE', #135292, #44516 ) ;
#57030=EDGE_LOOP ( 'NONE', ( #112194, #71036, #88673, #76332, #25671 ) ) ;
#57039=ORIENTED_EDGE ( 'NONE', *, *, #139622, .F. ) ;
#57055=VERTEX_POINT ( 'NONE', #11691 ) ;
#57063=ORIENTED_EDGE ( 'NONE', *, *, #91288, .T. ) ;
#57066=CARTESIAN_POINT ( 'NONE',  ( 8.111591955682463606, 2.055000000000001048, 2.516649172247811554E-16 ) ) ;
#57083=AXIS2_PLACEMENT_3D ( 'NONE', #68509, #67812, #56920 ) ;
#57098=CARTESIAN_POINT ( 'NONE',  ( 0.5685132242927012358, 4.584330080086930965E-16, 0.000000000000000000 ) ) ;
#57099=CIRCLE ( 'NONE', #114877, 2.337593264352433753 ) ;
#57107=VECTOR ( 'NONE', #19336, 1000.000000000000000 ) ;
#57109=CYLINDRICAL_SURFACE ( 'NONE', #61171, 2.500000000000000444 ) ;
#57146=AXIS2_PLACEMENT_3D ( 'NONE', #137372, #91705, #38064 ) ;
#57248=CARTESIAN_POINT ( 'NONE',  ( 8.585466709768445170, 3.821174125832445049E-16, 0.000000000000000000 ) ) ;
#57252=EDGE_CURVE ( 'NONE', #31140, #25493, #39236, .T. ) ;
#57256=CARTESIAN_POINT ( 'NONE',  ( 3.710381658649933634, 4.584330080086930965E-16, 0.000000000000000000 ) ) ;
#57263=VERTEX_POINT ( 'NONE', #122106 ) ;
#57312=CYLINDRICAL_SURFACE ( 'NONE', #128621, 2.500000000000000444 ) ;
#57380=DIRECTION ( 'NONE',  ( 0.000000000000000000, -1.000000000000000000, 0.000000000000000000 ) ) ;
#57382=ORIENTED_EDGE ( 'NONE', *, *, #18248, .F. ) ;
#57394=CARTESIAN_POINT ( 'NONE',  ( 0.000000000000000000, 0.3999999999999995781, 2.015694669338588429 ) ) ;
#57406=ORIENTED_EDGE ( 'NONE', *, *, #54129, .T. ) ;
#57414=VERTEX_POINT ( 'NONE', #112671 ) ;
#57441=LINE ( 'NONE', #55290, #104892 ) ;
#57473=FACE_OUTER_BOUND ( 'NONE', #20608, .T. ) ;
#57476=FACE_OUTER_BOUND ( 'NONE', #28828, .T. ) ;
#57547=AXIS2_PLACEMENT_3D ( 'NONE', #38686, #70640, #29219 ) ;
#57550=CARTESIAN_POINT ( 'NONE',  ( 1.827855086967997922, -2.055000000000000160, 2.789133085058097101E-16 ) ) ;
#57554=DIRECTION ( 'NONE',  ( 0.000000000000000000, -1.000000000000000000, 0.000000000000000000 ) ) ;
#57629=EDGE_CURVE ( 'NONE', #2459, #90362, #64462, .T. ) ;
#57636=CARTESIAN_POINT ( 'NONE',  ( 9.208651418775088970, 3.061616997868383634E-16, -2.500000000000000444 ) ) ;
#57662=DIRECTION ( 'NONE',  ( 0.000000000000000000, 1.000000000000000000, 0.000000000000000000 ) ) ;
#57679=CIRCLE ( 'NONE', #96923, 2.055000000000000604 ) ;
#57688=LINE ( 'NONE', #101866, #47600 ) ;
#57716=CARTESIAN_POINT ( 'NONE',  ( 20.36747333860806819, 3.821174125832445049E-16, 0.000000000000000000 ) ) ;
#57733=ORIENTED_EDGE ( 'NONE', *, *, #140335, .T. ) ;
#57795=DIRECTION ( 'NONE',  ( 0.000000000000000000, -1.000000000000000000, 0.000000000000000000 ) ) ;
#57804=ORIENTED_EDGE ( 'NONE', *, *, #93938, .T. ) ;
#57816=DIRECTION ( 'NONE',  ( -1.000000000000000000, -0.000000000000000000, -0.000000000000000000 ) ) ;
#57819=DIRECTION ( 'NONE',  ( 0.000000000000000000, -1.000000000000000000, 0.000000000000000000 ) ) ;
#57885=DIRECTION ( 'NONE',  ( -1.000000000000000000, 0.000000000000000000, -0.000000000000000000 ) ) ;
#57895=ORIENTED_EDGE ( 'NONE', *, *, #59300, .T. ) ;
#57912=ORIENTED_EDGE ( 'NONE', *, *, #74290, .F. ) ;
#57923=DIRECTION ( 'NONE',  ( 0.5735764363510448272, -0.8191520442889927978, 1.003171929053526103E-16 ) ) ;
#57953=EDGE_LOOP ( 'NONE', ( #96040, #141659, #126357, #32804, #121568 ) ) ;
#57973=AXIS2_PLACEMENT_3D ( 'NONE', #102592, #135914, #3239 ) ;
#58101=ADVANCED_FACE ( 'NONE', ( #134642 ), #124696, .T. ) ;
#58110=CARTESIAN_POINT ( 'NONE',  ( 19.41972383043609440, 4.584330080086930965E-16, 0.000000000000000000 ) ) ;
#58116=ORIENTED_EDGE ( 'NONE', *, *, #84383, .F. ) ;
#58129=CIRCLE ( 'NONE', #51066, 2.055000000000000604 ) ;
#58140=VERTEX_POINT ( 'NONE', #16376 ) ;
#58160=CIRCLE ( 'NONE', #129926, 2.500000000000000444 ) ;
#58169=AXIS2_PLACEMENT_3D ( 'NONE', #112205, #91852, #45543 ) ;
#58175=CIRCLE ( 'NONE', #30393, 2.500000000000000444 ) ;
#58183=CARTESIAN_POINT ( 'NONE',  ( -12.69999999999998153, 0.000000000000000000, 0.000000000000000000 ) ) ;
#58226=DIRECTION ( 'NONE',  ( 1.000000000000000000, 1.224606353822377258E-16, 0.000000000000000000 ) ) ;
#58250=VECTOR ( 'NONE', #63009, 1000.000000000000000 ) ;
#58251=DIRECTION ( 'NONE',  ( 8.673617379884034239E-17, -1.000000000000000000, 0.000000000000000000 ) ) ;
#58254=CARTESIAN_POINT ( 'NONE',  ( 21.66240673564756491, 0.000000000000000000, 0.000000000000000000 ) ) ;
#58272=AXIS2_PLACEMENT_3D ( 'NONE', #103876, #61858, #18288 ) ;
#58363=AXIS2_PLACEMENT_3D ( 'NONE', #75567, #76286, #824 ) ;
#58375=DIRECTION ( 'NONE',  ( 1.734723475976806848E-16, -1.000000000000000000, 0.000000000000000000 ) ) ;
#58395=CARTESIAN_POINT ( 'NONE',  ( -12.69999999999998153, 0.000000000000000000, 0.000000000000000000 ) ) ;
#58397=VECTOR ( 'NONE', #119358, 999.9999999999998863 ) ;
#58404=ORIENTED_EDGE ( 'NONE', *, *, #38478, .F. ) ;
#58415=DIRECTION ( 'NONE',  ( -1.000000000000000000, -1.224606353822377258E-16, -0.000000000000000000 ) ) ;
#58427=VECTOR ( 'NONE', #126635, 1000.000000000000000 ) ;
#58431=ORIENTED_EDGE ( 'NONE', *, *, #113792, .T. ) ;
#58442=EDGE_CURVE ( 'NONE', #111882, #82210, #85951, .T. ) ;
#58443=EDGE_CURVE ( 'NONE', #46733, #37203, #90118, .T. ) ;
#58470=ORIENTED_EDGE ( 'NONE', *, *, #137121, .T. ) ;
#58474=FACE_OUTER_BOUND ( 'NONE', #139038, .T. ) ;
#58505=ORIENTED_EDGE ( 'NONE', *, *, #143117, .T. ) ;
#58517=FACE_OUTER_BOUND ( 'NONE', #88990, .T. ) ;
#58522=CARTESIAN_POINT ( 'NONE',  ( 4.658131166821905644, -2.500000000000000444, 0.000000000000000000 ) ) ;
#58526=AXIS2_PLACEMENT_3D ( 'NONE', #104727, #61286, #128633 ) ;
#58554=CIRCLE ( 'NONE', #63080, 2.055000000000000604 ) ;
#58566=CARTESIAN_POINT ( 'NONE',  ( 13.92145407031093818, 4.584330080086930965E-16, 0.000000000000000000 ) ) ;
#58572=EDGE_LOOP ( 'NONE', ( #134959, #123301, #70873, #3434, #21677, #139604 ) ) ;
#58583=ORIENTED_EDGE ( 'NONE', *, *, #99089, .T. ) ;
#58598=VERTEX_POINT ( 'NONE', #33039 ) ;
#58603=DIRECTION ( 'NONE',  ( -1.000000000000000000, -0.000000000000000000, -0.000000000000000000 ) ) ;
#58617=EDGE_CURVE ( 'NONE', #73381, #38444, #122503, .T. ) ;
#58677=ORIENTED_EDGE ( 'NONE', *, *, #89015, .T. ) ;
#58697=CARTESIAN_POINT ( 'NONE',  ( 1.042387978378689350, 2.055000000000001048, 0.000000000000000000 ) ) ;
#58763=CARTESIAN_POINT ( 'NONE',  ( 10.15640092694706453, 3.821174125832445049E-16, 0.000000000000000000 ) ) ;
#58764=DIRECTION ( 'NONE',  ( 0.000000000000000000, -1.000000000000000000, 0.000000000000000000 ) ) ;
#58772=VECTOR ( 'NONE', #119377, 999.9999999999998863 ) ;
#58780=CARTESIAN_POINT ( 'NONE',  ( 13.13598696172163116, 0.000000000000000000, 2.500000000000000444 ) ) ;
#58897=EDGE_LOOP ( 'NONE', ( #26864, #55213, #54002, #2014, #46672, #13773 ) ) ;
#58918=EDGE_CURVE ( 'NONE', #134578, #54699, #66957, .T. ) ;
#58948=DIRECTION ( 'NONE',  ( -1.000000000000000000, -0.000000000000000000, -0.000000000000000000 ) ) ;
#59024=ORIENTED_EDGE ( 'NONE', *, *, #111050, .T. ) ;
#59058=FACE_OUTER_BOUND ( 'NONE', #89531, .T. ) ;
#59073=VERTEX_POINT ( 'NONE', #45869 ) ;
#59101=EDGE_CURVE ( 'NONE', #64882, #32697, #36930, .T. ) ;
#59133=CARTESIAN_POINT ( 'NONE',  ( 12.82439460721831104, 4.202752102959690472E-16, 0.000000000000000000 ) ) ;
#59141=ORIENTED_EDGE ( 'NONE', *, *, #86999, .F. ) ;
#59156=EDGE_LOOP ( 'NONE', ( #125461, #114095, #56064, #52908, #73566 ) ) ;
#59163=VERTEX_POINT ( 'NONE', #5157 ) ;
#59171=DIRECTION ( 'NONE',  ( -1.000000000000000000, -1.224606353822377258E-16, -0.000000000000000000 ) ) ;
#59185=CONICAL_SURFACE ( 'NONE', #61466, 2.055000000000000604, 0.9599310885968764806 ) ;
#59200=ADVANCED_FACE ( 'NONE', ( #96444 ), #101818, .T. ) ;
#59206=CARTESIAN_POINT ( 'NONE',  ( 9.994118527364397764, 4.584330080086930965E-16, 0.000000000000000000 ) ) ;
#59257=CARTESIAN_POINT ( 'NONE',  ( 9.682526172861077640, 4.202752102959690472E-16, 0.000000000000000000 ) ) ;
#59300=EDGE_CURVE ( 'NONE', #140903, #67994, #6975, .T. ) ;
#59303=ORIENTED_EDGE ( 'NONE', *, *, #6532, .F. ) ;
#59307=EDGE_CURVE ( 'NONE', #26888, #12905, #43983, .T. ) ;
#59317=CIRCLE ( 'NONE', #15174, 2.500000000000000444 ) ;
#59344=VERTEX_POINT ( 'NONE', #11582 ) ;
#59356=DIRECTION ( 'NONE',  ( -1.000000000000000000, -0.000000000000000000, -0.000000000000000000 ) ) ;
#59358=FACE_OUTER_BOUND ( 'NONE', #123031, .T. ) ;
#59411=EDGE_LOOP ( 'NONE', ( #47162, #91012, #22418, #5755, #84418, #17958 ) ) ;
#59465=DIRECTION ( 'NONE',  ( -1.000000000000000000, -1.224606353822377258E-16, -0.000000000000000000 ) ) ;
#59486=ORIENTED_EDGE ( 'NONE', *, *, #65496, .T. ) ;
#59504=VERTEX_POINT ( 'NONE', #111654 ) ;
#59544=ORIENTED_EDGE ( 'NONE', *, *, #30079, .F. ) ;
#59557=DIRECTION ( 'NONE',  ( -1.000000000000000000, -0.000000000000000000, -0.000000000000000000 ) ) ;
#59676=ORIENTED_EDGE ( 'NONE', *, *, #59307, .F. ) ;
#59713=EDGE_CURVE ( 'NONE', #66625, #109461, #116430, .T. ) ;
#59721=CARTESIAN_POINT ( 'NONE',  ( 14.86920357848291196, 0.000000000000000000, 2.500000000000000444 ) ) ;
#59727=ORIENTED_EDGE ( 'NONE', *, *, #52834, .T. ) ;
#59739=LINE ( 'NONE', #16171, #20590 ) ;
#59754=CARTESIAN_POINT ( 'NONE',  ( 8.585466709768445170, 0.000000000000000000, 2.500000000000000444 ) ) ;
#59813=CARTESIAN_POINT ( 'NONE',  ( 17.84878961325748037, 4.584330080086930965E-16, 0.000000000000000000 ) ) ;
#59855=VERTEX_POINT ( 'NONE', #76515 ) ;
#59887=AXIS2_PLACEMENT_3D ( 'NONE', #41823, #65763, #86043 ) ;
#59904=CARTESIAN_POINT ( 'NONE',  ( 18.32266436734346726, 4.202752102959690472E-16, 0.000000000000000000 ) ) ;
#59910=VERTEX_POINT ( 'NONE', #65667 ) ;
#59934=CARTESIAN_POINT ( 'NONE',  ( 8.423184310185783730, 4.584330080086930965E-16, 0.000000000000000000 ) ) ;
#59956=ORIENTED_EDGE ( 'NONE', *, *, #77670, .F. ) ;
#59957=CARTESIAN_POINT ( 'NONE',  ( 11.56505274454301357, -2.500000000000000000, 3.061616997868383634E-16 ) ) ;
#59993=AXIS2_PLACEMENT_3D ( 'NONE', #29830, #28435, #29133 ) ;
#60050=CARTESIAN_POINT ( 'NONE',  ( 10.77958563595370833, 4.584330080086930965E-16, 0.000000000000000000 ) ) ;
#60114=CARTESIAN_POINT ( 'NONE',  ( 13.92145407031093818, 2.500000000000000888, 0.000000000000000000 ) ) ;
#60143=AXIS2_PLACEMENT_3D ( 'NONE', #47332, #112524, #91503 ) ;
#60186=ORIENTED_EDGE ( 'NONE', *, *, #16788, .F. ) ;
#60193=ORIENTED_EDGE ( 'NONE', *, *, #21591, .T. ) ;
#60212=ORIENTED_EDGE ( 'NONE', *, *, #90372, .F. ) ;
#60214=VERTEX_POINT ( 'NONE', #114114 ) ;
#60235=CIRCLE ( 'NONE', #118123, 2.500000000000000444 ) ;
#60245=AXIS2_PLACEMENT_3D ( 'NONE', #73116, #5663, #84682 ) ;
#60313=CARTESIAN_POINT ( 'NONE',  ( 5.443598275411213550, 3.061616997868383634E-16, -2.500000000000000444 ) ) ;
#60351=DIRECTION ( 'NONE',  ( -1.000000000000000000, -1.224606353822377258E-16, -0.000000000000000000 ) ) ;
#60360=VERTEX_POINT ( 'NONE', #116961 ) ;
#60363=FACE_OUTER_BOUND ( 'NONE', #42533, .T. ) ;
#60390=ORIENTED_EDGE ( 'NONE', *, *, #96006, .F. ) ;
#60419=DIRECTION ( 'NONE',  ( -1.000000000000000000, -1.224606353822377258E-16, -0.000000000000000000 ) ) ;
#60428=ORIENTED_EDGE ( 'NONE', *, *, #9613, .T. ) ;
#60439=AXIS2_PLACEMENT_3D ( 'NONE', #100570, #1214, #78817 ) ;
#60464=ORIENTED_EDGE ( 'NONE', *, *, #122066, .F. ) ;
#60526=CIRCLE ( 'NONE', #58272, 2.500000000000000444 ) ;
#60529=CARTESIAN_POINT ( 'NONE',  ( 15.18079593298623564, 4.202752102959690472E-16, 0.000000000000000000 ) ) ;
#60531=EDGE_CURVE ( 'NONE', #43404, #63283, #113711, .T. ) ;
#60532=EDGE_CURVE ( 'NONE', #28611, #83522, #23345, .T. ) ;
#60538=VECTOR ( 'NONE', #8901, 1000.000000000000000 ) ;
#60556=ADVANCED_FACE ( 'NONE', ( #116069 ), #61044, .T. ) ;
#60589=LINE ( 'NONE', #116357, #101675 ) ;
#60614=CARTESIAN_POINT ( 'NONE',  ( 9.208651418775088970, 4.584330080086930965E-16, 0.000000000000000000 ) ) ;
#60670=CARTESIAN_POINT ( 'NONE',  ( 20.36747333860806819, 2.499999999999998224, 3.061616997868380183E-16 ) ) ;
#60679=CARTESIAN_POINT ( 'NONE',  ( 2.139447441471317379, 4.584330080086930965E-16, 0.000000000000000000 ) ) ;
#60688=AXIS2_PLACEMENT_3D ( 'NONE', #7566, #40941, #41638 ) ;
#60712=CARTESIAN_POINT ( 'NONE',  ( 1.516262732464673579, 3.821174125832445049E-16, 0.000000000000000000 ) ) ;
#60717=FACE_OUTER_BOUND ( 'NONE', #66842, .T. ) ;
#60732=CIRCLE ( 'NONE', #81609, 2.055000000000000604 ) ;
#60734=ADVANCED_FACE ( 'NONE', ( #28375 ), #99739, .T. ) ;
#60738=AXIS2_PLACEMENT_3D ( 'NONE', #101719, #135105, #110431 ) ;
#60749=EDGE_CURVE ( 'NONE', #79680, #53418, #29766, .T. ) ;
#60788=LINE ( 'NONE', #139759, #49689 ) ;
#60796=CARTESIAN_POINT ( 'NONE',  ( 15.65467068707222076, -2.499999999999996447, 0.000000000000000000 ) ) ;
#60801=ORIENTED_EDGE ( 'NONE', *, *, #138891, .F. ) ;
#60842=AXIS2_PLACEMENT_3D ( 'NONE', #137327, #136584, #48169 ) ;
#60885=CARTESIAN_POINT ( 'NONE',  ( 18.63425672184678916, 3.061616997868383634E-16, -2.500000000000000444 ) ) ;
#60895=ORIENTED_EDGE ( 'NONE', *, *, #121526, .T. ) ;
#60908=CARTESIAN_POINT ( 'NONE',  ( -12.69999999999998153, 0.000000000000000000, 0.000000000000000000 ) ) ;
#60935=EDGE_CURVE ( 'NONE', #103049, #46733, #37356, .T. ) ;
#60981=EDGE_LOOP ( 'NONE', ( #115830, #5228, #32943, #72374, #127642 ) ) ;
#61021=EDGE_LOOP ( 'NONE', ( #110745, #94558, #101266, #19432, #94093 ) ) ;
#61044=CYLINDRICAL_SURFACE ( 'NONE', #39655, 2.500000000000000444 ) ;
#61066=ORIENTED_EDGE ( 'NONE', *, *, #102888, .T. ) ;
#61076=LINE ( 'NONE', #105234, #118014 ) ;
#61141=ORIENTED_EDGE ( 'NONE', *, *, #40147, .F. ) ;
#61146=ORIENTED_EDGE ( 'NONE', *, *, #34376, .T. ) ;
#61171=AXIS2_PLACEMENT_3D ( 'NONE', #68689, #46972, #125189 ) ;
#61184=AXIS2_PLACEMENT_3D ( 'NONE', #123559, #114756, #18292 ) ;
#61221=EDGE_CURVE ( 'NONE', #128013, #39184, #92912, .T. ) ;
#61265=CARTESIAN_POINT ( 'NONE',  ( 21.46453280170069888, -2.055000000000000160, 0.000000000000000000 ) ) ;
#61271=DIRECTION ( 'NONE',  ( -1.000000000000000000, -0.000000000000000000, -0.000000000000000000 ) ) ;
#61275=VERTEX_POINT ( 'NONE', #141974 ) ;
#61286=DIRECTION ( 'NONE',  ( -1.000000000000000000, -0.000000000000000000, -0.000000000000000000 ) ) ;
#61379=ADVANCED_FACE ( 'NONE', ( #36747 ), #112192, .T. ) ;
#61399=ORIENTED_EDGE ( 'NONE', *, *, #125814, .T. ) ;
#61420=ORIENTED_EDGE ( 'NONE', *, *, #35279, .T. ) ;
#61448=DIRECTION ( 'NONE',  ( 1.000000000000000000, 1.224606353822377258E-16, 0.000000000000000000 ) ) ;
#61463=ORIENTED_EDGE ( 'NONE', *, *, #118850, .T. ) ;
#61466=AXIS2_PLACEMENT_3D ( 'NONE', #123656, #69262, #101148 ) ;
#61548=VERTEX_POINT ( 'NONE', #45185 ) ;
#61616=ORIENTED_EDGE ( 'NONE', *, *, #65951, .F. ) ;
#61618=ORIENTED_EDGE ( 'NONE', *, *, #24560, .T. ) ;
#61637=ORIENTED_EDGE ( 'NONE', *, *, #52347, .F. ) ;
#61646=CARTESIAN_POINT ( 'NONE',  ( 1.516262732464673579, 0.4000000000000001887, -2.467792535850613866 ) ) ;
#61702=CARTESIAN_POINT ( 'NONE',  ( 19.41972383043609440, 0.000000000000000000, 2.500000000000000444 ) ) ;
#61716=ADVANCED_FACE ( 'NONE', ( #16797 ), #42130, .T. ) ;
#61737=EDGE_CURVE ( 'NONE', #117017, #121969, #111529, .T. ) ;
#61751=DIRECTION ( 'NONE',  ( 0.000000000000000000, 0.000000000000000000, 1.000000000000000000 ) ) ;
#61752=DIRECTION ( 'NONE',  ( 0.000000000000000000, -1.000000000000000000, 0.000000000000000000 ) ) ;
#61792=ORIENTED_EDGE ( 'NONE', *, *, #28788, .T. ) ;
#61804=ORIENTED_EDGE ( 'NONE', *, *, #123288, .T. ) ;
#61822=CIRCLE ( 'NONE', #38724, 2.500000000000000444 ) ;
#61846=DIRECTION ( 'NONE',  ( 1.000000000000000000, 1.224606353822377258E-16, 0.000000000000000000 ) ) ;
#61858=DIRECTION ( 'NONE',  ( -1.000000000000000000, -1.224606353822377258E-16, -0.000000000000000000 ) ) ;
#61859=DIRECTION ( 'NONE',  ( 1.000000000000000000, 1.224606353822377258E-16, 0.000000000000000000 ) ) ;
#61868=LINE ( 'NONE', #106025, #91066 ) ;
#61875=DIRECTION ( 'NONE',  ( -1.000000000000000000, -0.000000000000000000, -0.000000000000000000 ) ) ;
#61922=DIRECTION ( 'NONE',  ( -1.000000000000000000, -1.224606353822377258E-16, -0.000000000000000000 ) ) ;
#61983=LINE ( 'NONE', #3448, #142891 ) ;
#62007=DIRECTION ( 'NONE',  ( -1.000000000000000000, -1.224606353822377258E-16, -0.000000000000000000 ) ) ;
#62042=ORIENTED_EDGE ( 'NONE', *, *, #98556, .F. ) ;
#62055=LINE ( 'NONE', #5479, #34632 ) ;
#62066=CARTESIAN_POINT ( 'NONE',  ( 1.629999999999999893, 0.4000000000000001887, -2.500000000000000000 ) ) ;
#62088=DIRECTION ( 'NONE',  ( 0.000000000000000000, -1.000000000000000000, 0.000000000000000000 ) ) ;
#62092=EDGE_CURVE ( 'NONE', #27734, #119393, #130184, .T. ) ;
#62105=CARTESIAN_POINT ( 'NONE',  ( 5.281315875828549444, 4.584330080086930965E-16, 0.000000000000000000 ) ) ;
#62141=EDGE_CURVE ( 'NONE', #104460, #34275, #66044, .T. ) ;
#62256=DIRECTION ( 'NONE',  ( -1.000000000000000000, -1.224606353822377258E-16, -0.000000000000000000 ) ) ;
#62273=AXIS2_PLACEMENT_3D ( 'NONE', #67152, #121505, #12033 ) ;
#62275=AXIS2_PLACEMENT_3D ( 'NONE', #22517, #21116, #65378 ) ;
#62280=DIRECTION ( 'NONE',  ( 0.000000000000000000, -1.000000000000000000, 0.000000000000000000 ) ) ;
#62300=DIRECTION ( 'NONE',  ( 0.000000000000000000, 0.000000000000000000, 1.000000000000000000 ) ) ;
#62430=CARTESIAN_POINT ( 'NONE',  ( -12.69999999999998153, 0.000000000000000000, 0.000000000000000000 ) ) ;
#62470=CARTESIAN_POINT ( 'NONE',  ( -12.69999999999998153, 3.061616997868383634E-16, -2.500000000000000444 ) ) ;
#62485=ORIENTED_EDGE ( 'NONE', *, *, #99589, .F. ) ;
#62490=AXIS2_PLACEMENT_3D ( 'NONE', #79596, #57816, #123779 ) ;
#62495=ADVANCED_FACE ( 'NONE', ( #13571 ), #123358, .T. ) ;
#62525=AXIS2_PLACEMENT_3D ( 'NONE', #113612, #109522, #47002 ) ;
#62544=CIRCLE ( 'NONE', #44014, 2.500000000000000444 ) ;
#62548=ORIENTED_EDGE ( 'NONE', *, *, #15646, .F. ) ;
#62561=ADVANCED_FACE ( 'NONE', ( #60717 ), #118669, .T. ) ;
#62570=ORIENTED_EDGE ( 'NONE', *, *, #108828, .F. ) ;
#62579=DIRECTION ( 'NONE',  ( 0.000000000000000000, 1.000000000000000000, 0.000000000000000000 ) ) ;
#62595=DIRECTION ( 'NONE',  ( 0.000000000000000000, -1.000000000000000000, 0.000000000000000000 ) ) ;
#62623=LINE ( 'NONE', #119120, #40348 ) ;
#62648=DIRECTION ( 'NONE',  ( -1.000000000000000000, -1.224606353822377258E-16, -0.000000000000000000 ) ) ;
#62656=CONICAL_SURFACE ( 'NONE', #111258, 1.749999999999999778, 0.7853981633974480570 ) ;
#62672=CIRCLE ( 'NONE', #67326, 2.500000000000000444 ) ;
#62713=CARTESIAN_POINT ( 'NONE',  ( 9.370933818357753964, 3.061616997868383634E-16, -2.500000000000000444 ) ) ;
#62744=ORIENTED_EDGE ( 'NONE', *, *, #139622, .T. ) ;
#62751=VERTEX_POINT ( 'NONE', #110571 ) ;
#62793=CIRCLE ( 'NONE', #97523, 2.500000000000000444 ) ;
#62807=VECTOR ( 'NONE', #35381, 999.9999999999998863 ) ;
#62851=AXIS2_PLACEMENT_3D ( 'NONE', #91134, #128558, #62595 ) ;
#62852=DIRECTION ( 'NONE',  ( -1.000000000000000000, -0.000000000000000000, -0.000000000000000000 ) ) ;
#62861=VECTOR ( 'NONE', #68154, 1000.000000000000000 ) ;
#62910=DIRECTION ( 'NONE',  ( -1.000000000000000000, -1.224606353822377258E-16, -0.000000000000000000 ) ) ;
#62925=CARTESIAN_POINT ( 'NONE',  ( 0.8348607551137287031, 0.4000000000000001887, -2.317232462839658336 ) ) ;
#62929=ORIENTED_EDGE ( 'NONE', *, *, #22242, .T. ) ;
#62985=CARTESIAN_POINT ( 'NONE',  ( 11.25346039003969523, 4.202752102959690472E-16, 0.000000000000000000 ) ) ;
#62993=AXIS2_PLACEMENT_3D ( 'NONE', #89635, #464, #44761 ) ;
#63009=DIRECTION ( 'NONE',  ( -1.000000000000000000, -0.000000000000000000, -0.000000000000000000 ) ) ;
#63043=ORIENTED_EDGE ( 'NONE', *, *, #15646, .T. ) ;
#63059=AXIS2_PLACEMENT_3D ( 'NONE', #124639, #81156, #113764 ) ;
#63080=AXIS2_PLACEMENT_3D ( 'NONE', #27658, #28398, #61752 ) ;
#63099=EDGE_LOOP ( 'NONE', ( #96415, #71214, #82523, #26275 ) ) ;
#63102=CIRCLE ( 'NONE', #56188, 2.500000000000000444 ) ;
#63113=ORIENTED_EDGE ( 'NONE', *, *, #78695, .F. ) ;
#63158=EDGE_CURVE ( 'NONE', #104460, #64781, #94814, .T. ) ;
#63205=CARTESIAN_POINT ( 'NONE',  ( 11.25346039003969523, 2.055000000000001048, 0.000000000000000000 ) ) ;
#63283=VERTEX_POINT ( 'NONE', #134342 ) ;
#63284=CARTESIAN_POINT ( 'NONE',  ( 12.51280225271498736, 0.000000000000000000, 2.500000000000000444 ) ) ;
#63294=VERTEX_POINT ( 'NONE', #130422 ) ;
#63371=EDGE_LOOP ( 'NONE', ( #11090, #89233 ) ) ;
#63385=CIRCLE ( 'NONE', #100405, 2.500000000000000444 ) ;
#63402=CIRCLE ( 'NONE', #121501, 2.055000000000000604 ) ;
#63425=DIRECTION ( 'NONE',  ( -1.000000000000000000, -0.000000000000000000, -0.000000000000000000 ) ) ;
#63438=DIRECTION ( 'NONE',  ( 0.000000000000000000, 0.000000000000000000, 1.000000000000000000 ) ) ;
#63447=CARTESIAN_POINT ( 'NONE',  ( 6.066782984417857350, 4.584330080086930965E-16, 0.000000000000000000 ) ) ;
#63457=EDGE_CURVE ( 'NONE', #105369, #25809, #20450, .T. ) ;
#63486=DIRECTION ( 'NONE',  ( -1.000000000000000000, -1.224606353822377258E-16, -0.000000000000000000 ) ) ;
#63489=DIRECTION ( 'NONE',  ( 0.000000000000000000, 1.000000000000000000, 0.000000000000000000 ) ) ;
#63504=DIRECTION ( 'NONE',  ( -1.000000000000000000, -0.000000000000000000, -0.000000000000000000 ) ) ;
#63524=EDGE_LOOP ( 'NONE', ( #72982, #124734, #1751, #141102, #44881, #18490 ) ) ;
#63534=VECTOR ( 'NONE', #45434, 1000.000000000000000 ) ;
#63553=EDGE_CURVE ( 'NONE', #1294, #97836, #55544, .T. ) ;
#63613=CARTESIAN_POINT ( 'NONE',  ( 19.89359858452208130, 2.055000000000001048, 2.516649172247811554E-16 ) ) ;
#63619=DIRECTION ( 'NONE',  ( 2.110369192185896011E-16, -1.000000000000000000, 0.000000000000000000 ) ) ;
#63628=VECTOR ( 'NONE', #112377, 999.9999999999998863 ) ;
#63633=CIRCLE ( 'NONE', #5620, 2.500000000000000444 ) ;
#63686=ORIENTED_EDGE ( 'NONE', *, *, #57629, .F. ) ;
#63688=EDGE_LOOP ( 'NONE', ( #136608, #101725, #41311, #45208, #28007 ) ) ;
#63780=ADVANCED_FACE ( 'NONE', ( #108697 ), #106499, .T. ) ;
#63800=ORIENTED_EDGE ( 'NONE', *, *, #143347, .F. ) ;
#63827=CARTESIAN_POINT ( 'NONE',  ( 15.96626304157554266, 4.202752102959690472E-16, 0.000000000000000000 ) ) ;
#63834=CONICAL_SURFACE ( 'NONE', #132974, 2.500000000000000444, 0.9599310885968830309 ) ;
#63854=DIRECTION ( 'NONE',  ( 0.000000000000000000, 0.000000000000000000, 1.000000000000000000 ) ) ;
#63866=CARTESIAN_POINT ( 'NONE',  ( 1.629999999999999893, 0.4000000000000001887, -2.500000000000000000 ) ) ;
#63878=DIRECTION ( 'NONE',  ( -1.000000000000000000, -1.224606353822377258E-16, -0.000000000000000000 ) ) ;
#63893=ORIENTED_EDGE ( 'NONE', *, *, #120601, .F. ) ;
#63908=DIRECTION ( 'NONE',  ( 0.000000000000000000, -1.000000000000000000, 0.000000000000000000 ) ) ;
#63946=EDGE_CURVE ( 'NONE', #21831, #121565, #97192, .T. ) ;
#63981=EDGE_CURVE ( 'NONE', #99111, #79754, #101882, .T. ) ;
#64009=EDGE_CURVE ( 'NONE', #136985, #98372, #108885, .T. ) ;
#64015=AXIS2_PLACEMENT_3D ( 'NONE', #96155, #142560, #76605 ) ;
#64037=CARTESIAN_POINT ( 'NONE',  ( 17.53719725875415847, 2.055000000000001048, 0.000000000000000000 ) ) ;
#64102=LINE ( 'NONE', #97415, #123112 ) ;
#64103=LINE ( 'NONE', #53970, #98886 ) ;
#64119=EDGE_CURVE ( 'NONE', #121969, #64882, #30267, .T. ) ;
#64154=AXIS2_PLACEMENT_3D ( 'NONE', #31088, #107879, #52793 ) ;
#64194=DIRECTION ( 'NONE',  ( 0.000000000000000000, -1.000000000000000000, 0.000000000000000000 ) ) ;
#64200=DIRECTION ( 'NONE',  ( -1.000000000000000000, -1.224606353822377258E-16, -0.000000000000000000 ) ) ;
#64207=ORIENTED_EDGE ( 'NONE', *, *, #113401, .F. ) ;
#64211=LINE ( 'NONE', #105012, #50831 ) ;
#64246=CARTESIAN_POINT ( 'NONE',  ( 21.46453280170069888, 4.202752102959690472E-16, 0.000000000000000000 ) ) ;
#64307=ORIENTED_EDGE ( 'NONE', *, *, #7084, .T. ) ;
#64312=ORIENTED_EDGE ( 'NONE', *, *, #22962, .F. ) ;
#64328=ORIENTED_EDGE ( 'NONE', *, *, #94999, .F. ) ;
#64333=ORIENTED_EDGE ( 'NONE', *, *, #46004, .F. ) ;
#64342=VECTOR ( 'NONE', #95837, 1000.000000000000000 ) ;
#64373=CARTESIAN_POINT ( 'NONE',  ( 18.79653912142945060, 3.821174125832445049E-16, 0.000000000000000000 ) ) ;
#64389=SHAPE_REPRESENTATION ( 'slotted set screw dog point_iso_ISO 7435 - M5 x 25-S', ( #127880 ), #97842 ) ;
#64398=CARTESIAN_POINT ( 'NONE',  ( -12.69999999999998153, 0.000000000000000000, 0.000000000000000000 ) ) ;
#64434=CARTESIAN_POINT ( 'NONE',  ( -12.69999999999998153, 3.061616997868383634E-16, -2.500000000000000444 ) ) ;
#64462=CIRCLE ( 'NONE', #136174, 2.500000000000000444 ) ;
#64481=DIRECTION ( 'NONE',  ( 0.000000000000000000, -1.000000000000000000, 0.000000000000000000 ) ) ;
#64491=ORIENTED_EDGE ( 'NONE', *, *, #127229, .T. ) ;
#64536=CARTESIAN_POINT ( 'NONE',  ( 7.637717201596474048, 2.500000000000000444, 0.000000000000000000 ) ) ;
#64550=CYLINDRICAL_SURFACE ( 'NONE', #79111, 2.500000000000000444 ) ;
#64639=EDGE_CURVE ( 'NONE', #91199, #8776, #118548, .T. ) ;
#64678=AXIS2_PLACEMENT_3D ( 'NONE', #27624, #17464, #129798 ) ;
#64685=AXIS2_PLACEMENT_3D ( 'NONE', #22978, #133235, #25874 ) ;
#64702=ORIENTED_EDGE ( 'NONE', *, *, #13663, .T. ) ;
#64720=CARTESIAN_POINT ( 'NONE',  ( -12.69999999999998153, 0.000000000000000000, 2.500000000000000444 ) ) ;
#64738=AXIS2_PLACEMENT_3D ( 'NONE', #23321, #133545, #21909 ) ;
#64739=VECTOR ( 'NONE', #21182, 999.9999999999998863 ) ;
#64741=CARTESIAN_POINT ( 'NONE',  ( 0.1630955763144136539, 0.3999999999999995781, 2.152173649344992779 ) ) ;
#64751=CYLINDRICAL_SURFACE ( 'NONE', #108920, 2.500000000000000444 ) ;
#64753=AXIS2_PLACEMENT_3D ( 'NONE', #94134, #105708, #94833 ) ;
#64756=CARTESIAN_POINT ( 'NONE',  ( 0.2569208697893815008, -0.3999999999999998002, -2.015694669338588429 ) ) ;
#64781=VERTEX_POINT ( 'NONE', #98931 ) ;
#64819=EDGE_CURVE ( 'NONE', #86117, #19554, #58160, .T. ) ;
#64844=CARTESIAN_POINT ( 'NONE',  ( 21.66240673564756491, 0.000000000000000000, 0.000000000000000000 ) ) ;
#64858=CIRCLE ( 'NONE', #46363, 2.500000000000000444 ) ;
#64868=CARTESIAN_POINT ( 'NONE',  ( 20.99065804761471199, 0.000000000000000000, 2.500000000000000444 ) ) ;
#64873=ORIENTED_EDGE ( 'NONE', *, *, #72980, .F. ) ;
#64882=VERTEX_POINT ( 'NONE', #137839 ) ;
#64886=ORIENTED_EDGE ( 'NONE', *, *, #84488, .F. ) ;
#64924=FACE_OUTER_BOUND ( 'NONE', #101959, .T. ) ;
#64957=CIRCLE ( 'NONE', #101977, 2.055000000000000604 ) ;
#64987=FACE_OUTER_BOUND ( 'NONE', #9054, .T. ) ;
#65025=CARTESIAN_POINT ( 'NONE',  ( 2.301729841053981485, 3.821174125832445049E-16, 0.000000000000000000 ) ) ;
#65047=CARTESIAN_POINT ( 'NONE',  ( 0.03865102804815071652, 0.4000000000000001332, -2.083945628037807030 ) ) ;
#65154=EDGE_CURVE ( 'NONE', #28611, #23453, #102892, .T. ) ;
#65168=AXIS2_PLACEMENT_3D ( 'NONE', #127201, #48224, #18412 ) ;
#65198=ORIENTED_EDGE ( 'NONE', *, *, #71617, .F. ) ;
#65271=AXIS2_PLACEMENT_3D ( 'NONE', #75913, #131017, #117943 ) ;
#65283=ORIENTED_EDGE ( 'NONE', *, *, #126761, .F. ) ;
#65286=AXIS2_PLACEMENT_3D ( 'NONE', #140048, #51610, #63908 ) ;
#65357=ORIENTED_EDGE ( 'NONE', *, *, #14184, .T. ) ;
#65378=DIRECTION ( 'NONE',  ( 0.000000000000000000, -1.000000000000000000, 0.000000000000000000 ) ) ;
#65395=DIRECTION ( 'NONE',  ( 0.000000000000000000, -1.000000000000000000, 0.000000000000000000 ) ) ;
#65452=CARTESIAN_POINT ( 'NONE',  ( 14.70692117890024697, -2.500000000000000444, 3.061616997868384127E-16 ) ) ;
#65479=ORIENTED_EDGE ( 'NONE', *, *, #59713, .T. ) ;
#65486=( GEOMETRIC_REPRESENTATION_CONTEXT ( 3 ) GLOBAL_UNCERTAINTY_ASSIGNED_CONTEXT ( ( #22770 ) ) GLOBAL_UNIT_ASSIGNED_CONTEXT ( ( #123847, #24501, #48398 ) ) REPRESENTATION_CONTEXT ( 'NONE', 'WORKASPACE' ) );
#65495=ORIENTED_EDGE ( 'NONE', *, *, #105507, .F. ) ;
#65496=EDGE_CURVE ( 'NONE', #52878, #106919, #335, .T. ) ;
#65503=CARTESIAN_POINT ( 'NONE',  ( 7.326124847093153925, 2.055000000000001048, 2.516649172247811554E-16 ) ) ;
#65523=ORIENTED_EDGE ( 'NONE', *, *, #90688, .F. ) ;
#65558=ADVANCED_FACE ( 'NONE', ( #133225 ), #9656, .T. ) ;
#65590=DIRECTION ( 'NONE',  ( 0.000000000000000000, 1.000000000000000000, 0.000000000000000000 ) ) ;
#65634=CARTESIAN_POINT ( 'NONE',  ( 8.423184310185783730, 4.584330080086930965E-16, 0.000000000000000000 ) ) ;
#65640=CIRCLE ( 'NONE', #14684, 2.500000000000000444 ) ;
#65657=ORIENTED_EDGE ( 'NONE', *, *, #50286, .T. ) ;
#65667=CARTESIAN_POINT ( 'NONE',  ( 3.872664058232598627, -2.500000000000000444, 0.000000000000000000 ) ) ;
#65713=DIRECTION ( 'NONE',  ( 0.000000000000000000, -1.000000000000000000, 0.000000000000000000 ) ) ;
#65718=DIRECTION ( 'NONE',  ( 0.000000000000000000, -1.000000000000000000, 0.000000000000000000 ) ) ;
#65724=ORIENTED_EDGE ( 'NONE', *, *, #58442, .F. ) ;
#65729=CARTESIAN_POINT ( 'NONE',  ( 17.53719725875415847, 4.202752102959690472E-16, 0.000000000000000000 ) ) ;
#65730=CARTESIAN_POINT ( 'NONE',  ( 3.872664058232598183, 0.000000000000000000, 2.500000000000000444 ) ) ;
#65753=CONICAL_SURFACE ( 'NONE', #111980, 2.500000000000000444, 0.9599310885968830309 ) ;
#65763=DIRECTION ( 'NONE',  ( -1.000000000000000000, -1.224606353822377258E-16, -0.000000000000000000 ) ) ;
#65764=LINE ( 'NONE', #129525, #17115 ) ;
#65785=EDGE_CURVE ( 'NONE', #41872, #91199, #5078, .T. ) ;
#65796=FACE_OUTER_BOUND ( 'NONE', #106472, .T. ) ;
#65844=DIRECTION ( 'NONE',  ( 0.000000000000000000, -1.000000000000000000, 0.000000000000000000 ) ) ;
#65889=LINE ( 'NONE', #139868, #1641 ) ;
#65897=ADVANCED_FACE ( 'NONE', ( #56931 ), #16593, .T. ) ;
#65900=ORIENTED_EDGE ( 'NONE', *, *, #103649, .F. ) ;
#65951=EDGE_CURVE ( 'NONE', #68546, #73287, #16703, .T. ) ;
#65974=EDGE_CURVE ( 'NONE', #59163, #76525, #100125, .T. ) ;
#65999=CARTESIAN_POINT ( 'NONE',  ( 1.827855086967997700, 4.202752102959690472E-16, 0.000000000000000000 ) ) ;
#66044=LINE ( 'NONE', #89206, #2868 ) ;
#66056=ADVANCED_FACE ( 'NONE', ( #128578 ), #72826, .T. ) ;
#66094=ORIENTED_EDGE ( 'NONE', *, *, #132283, .F. ) ;
#66095=CONICAL_SURFACE ( 'NONE', #70761, 2.055000000000000160, 1.047197551196600962 ) ;
#66104=EDGE_CURVE ( 'NONE', #71093, #24475, #63102, .T. ) ;
#66152=ORIENTED_EDGE ( 'NONE', *, *, #21704, .F. ) ;
#66162=ORIENTED_EDGE ( 'NONE', *, *, #40573, .T. ) ;
#66222=ORIENTED_EDGE ( 'NONE', *, *, #67139, .T. ) ;
#66239=CARTESIAN_POINT ( 'NONE',  ( 6.540657738503846907, 2.055000000000001048, 2.516649172247811554E-16 ) ) ;
#66260=DIRECTION ( 'NONE',  ( 0.000000000000000000, 0.000000000000000000, 1.000000000000000000 ) ) ;
#66325=CIRCLE ( 'NONE', #91751, 2.500000000000000444 ) ;
#66333=AXIS2_PLACEMENT_3D ( 'NONE', #47535, #61271, #38052 ) ;
#66358=DIRECTION ( 'NONE',  ( 0.000000000000000000, -1.000000000000000000, 0.000000000000000000 ) ) ;
#66372=DIRECTION ( 'NONE',  ( 0.000000000000000000, -1.000000000000000000, 0.000000000000000000 ) ) ;
#66406=AXIS2_PLACEMENT_3D ( 'NONE', #44712, #78015, #24329 ) ;
#66413=ORIENTED_EDGE ( 'NONE', *, *, #33154, .T. ) ;
#66459=CARTESIAN_POINT ( 'NONE',  ( 3.398789304146614398, -2.055000000000000160, 0.000000000000000000 ) ) ;
#66500=DIRECTION ( 'NONE',  ( -1.000000000000000000, -1.224606353822377258E-16, -0.000000000000000000 ) ) ;
#66541=DIRECTION ( 'NONE',  ( 1.000000000000000000, 1.224606353822377258E-16, 0.000000000000000000 ) ) ;
#66553=EDGE_CURVE ( 'NONE', #69267, #130434, #138581, .T. ) ;
#66574=ADVANCED_FACE ( 'NONE', ( #101305 ), #134923, .T. ) ;
#66579=DIRECTION ( 'NONE',  ( -1.000000000000000000, -1.224606353822377258E-16, -0.000000000000000000 ) ) ;
#66606=VERTEX_POINT ( 'NONE', #56429 ) ;
#66625=VERTEX_POINT ( 'NONE', #134678 ) ;
#66627=VERTEX_POINT ( 'NONE', #24454 ) ;
#66631=CONICAL_SURFACE ( 'NONE', #43442, 2.500000000000000444, 0.9599310885968830309 ) ;
#66647=ORIENTED_EDGE ( 'NONE', *, *, #115258, .F. ) ;
#66652=DIRECTION ( 'NONE',  ( -1.000000000000000000, -0.000000000000000000, -0.000000000000000000 ) ) ;
#66675=DIRECTION ( 'NONE',  ( -1.000000000000000000, -1.224606353822377258E-16, -0.000000000000000000 ) ) ;
#66720=DIRECTION ( 'NONE',  ( 0.000000000000000000, -1.000000000000000000, 0.000000000000000000 ) ) ;
#66730=VECTOR ( 'NONE', #24887, 1000.000000000000000 ) ;
#66842=EDGE_LOOP ( 'NONE', ( #102619, #118283, #61792, #53643, #107227 ) ) ;
#66864=EDGE_LOOP ( 'NONE', ( #111525, #67018, #87889, #27877, #115920, #59141 ) ) ;
#66887=CARTESIAN_POINT ( 'NONE',  ( 0.2100385686636474791, 0.3999999999999995781, 2.083955130345453099 ) ) ;
#66952=ORIENTED_EDGE ( 'NONE', *, *, #18248, .T. ) ;
#66957=B_SPLINE_CURVE_WITH_KNOTS ( 'NONE', 3,
 ( #98773, #64741, #66887, #143011 ),
 .UNSPECIFIED., .F., .F.,
 ( 4, 4 ),
 ( 0.003913914403404827880, 0.004162342877716043374 ),
 .UNSPECIFIED. ) ;
#66966=CARTESIAN_POINT ( 'NONE',  ( 18.63425672184678916, 4.584330080086930965E-16, 0.000000000000000000 ) ) ;
#66994=ORIENTED_EDGE ( 'NONE', *, *, #117887, .T. ) ;
#67004=VERTEX_POINT ( 'NONE', #59721 ) ;
#67010=ORIENTED_EDGE ( 'NONE', *, *, #115746, .T. ) ;
#67018=ORIENTED_EDGE ( 'NONE', *, *, #88367, .T. ) ;
#67019=CARTESIAN_POINT ( 'NONE',  ( 1.042387978378689573, -0.4000000000000003553, 2.015694669338588429 ) ) ;
#67081=ORIENTED_EDGE ( 'NONE', *, *, #96960, .T. ) ;
#67118=ORIENTED_EDGE ( 'NONE', *, *, #69656, .T. ) ;
#67122=ORIENTED_EDGE ( 'NONE', *, *, #102791, .F. ) ;
#67139=EDGE_CURVE ( 'NONE', #41149, #31359, #2344, .T. ) ;
#67152=CARTESIAN_POINT ( 'NONE',  ( 10.77958563595370833, 4.584330080086930965E-16, 0.000000000000000000 ) ) ;
#67175=CARTESIAN_POINT ( 'NONE',  ( 0.1161069444170879233, 0.4000000000000001332, -2.220360628129161462 ) ) ;
#67196=ORIENTED_EDGE ( 'NONE', *, *, #53543, .F. ) ;
#67238=ORIENTED_EDGE ( 'NONE', *, *, #40147, .T. ) ;
#67241=DIRECTION ( 'NONE',  ( 0.000000000000000000, 0.000000000000000000, 1.000000000000000000 ) ) ;
#67251=CARTESIAN_POINT ( 'NONE',  ( 20.99065804761471199, 4.584330080086930965E-16, 0.000000000000000000 ) ) ;
#67311=CARTESIAN_POINT ( 'NONE',  ( 2.301729841053981485, 3.821174125832445049E-16, 0.000000000000000000 ) ) ;
#67322=ORIENTED_EDGE ( 'NONE', *, *, #15795, .T. ) ;
#67326=AXIS2_PLACEMENT_3D ( 'NONE', #25241, #113682, #36147 ) ;
#67338=AXIS2_PLACEMENT_3D ( 'NONE', #126055, #137645, #36871 ) ;
#67340=CYLINDRICAL_SURFACE ( 'NONE', #136995, 1.749999999999999778 ) ;
#67385=ORIENTED_EDGE ( 'NONE', *, *, #127434, .F. ) ;
#67462=EDGE_CURVE ( 'NONE', #142044, #42523, #121123, .T. ) ;
#67468=DIRECTION ( 'NONE',  ( -1.000000000000000000, -0.000000000000000000, -0.000000000000000000 ) ) ;
#67487=CIRCLE ( 'NONE', #139297, 2.500000000000000444 ) ;
#67508=ORIENTED_EDGE ( 'NONE', *, *, #74455, .T. ) ;
#67512=CIRCLE ( 'NONE', #104406, 2.055000000000000604 ) ;
#67531=VECTOR ( 'NONE', #103957, 1000.000000000000000 ) ;
#67534=ORIENTED_EDGE ( 'NONE', *, *, #379, .T. ) ;
#67568=EDGE_CURVE ( 'NONE', #12106, #122233, #68228, .T. ) ;
#67594=AXIS2_PLACEMENT_3D ( 'NONE', #26257, #115352, #138587 ) ;
#67618=CARTESIAN_POINT ( 'NONE',  ( 9.994118527364397764, 2.500000000000000888, 0.000000000000000000 ) ) ;
#67658=CIRCLE ( 'NONE', #28196, 2.500000000000000444 ) ;
#67663=AXIS2_PLACEMENT_3D ( 'NONE', #120402, #43596, #108823 ) ;
#67740=DIRECTION ( 'NONE',  ( -1.000000000000000000, -1.224606353822377258E-16, -0.000000000000000000 ) ) ;
#67785=EDGE_CURVE ( 'NONE', #46733, #1294, #142022, .T. ) ;
#67812=DIRECTION ( 'NONE',  ( -1.000000000000000000, -1.224606353822377258E-16, -0.000000000000000000 ) ) ;
#67816=CARTESIAN_POINT ( 'NONE',  ( 19.58200623001875940, 2.499999999999998224, 3.061616997868380183E-16 ) ) ;
#67821=DIRECTION ( 'NONE',  ( -1.000000000000000000, -1.224606353822377258E-16, -0.000000000000000000 ) ) ;
#67828=CARTESIAN_POINT ( 'NONE',  ( 13.60986171580761805, 4.202752102959690472E-16, 0.000000000000000000 ) ) ;
#67831=CARTESIAN_POINT ( 'NONE',  ( 4.495848767239241539, -2.500000000000000000, 3.061616997868383634E-16 ) ) ;
#67836=AXIS2_PLACEMENT_3D ( 'NONE', #122877, #87411, #109860 ) ;
#67853=ORIENTED_EDGE ( 'NONE', *, *, #94999, .T. ) ;
#67854=CARTESIAN_POINT ( 'NONE',  ( 4.969723521325230209, 2.055000000000001048, 2.516649172247811554E-16 ) ) ;
#67909=CONICAL_SURFACE ( 'NONE', #104903, 2.500000000000000444, 0.9599310885968830309 ) ;
#67967=VECTOR ( 'NONE', #17449, 1000.000000000000000 ) ;
#67983=ORIENTED_EDGE ( 'NONE', *, *, #83873, .T. ) ;
#67994=VERTEX_POINT ( 'NONE', #113641 ) ;
#68011=AXIS2_PLACEMENT_3D ( 'NONE', #14759, #113339, #37229 ) ;
#68086=ORIENTED_EDGE ( 'NONE', *, *, #87896, .F. ) ;
#68087=CARTESIAN_POINT ( 'NONE',  ( 3.710381658649933634, 3.061616997868382648E-16, -2.500000000000000444 ) ) ;
#68154=DIRECTION ( 'NONE',  ( -0.5735764363510499342, -0.8191520442889891340, 0.000000000000000000 ) ) ;
#68178=CARTESIAN_POINT ( 'NONE',  ( 3.398789304146613954, 4.202752102959690472E-16, 0.000000000000000000 ) ) ;
#68201=LINE ( 'NONE', #33422, #63628 ) ;
#68221=ORIENTED_EDGE ( 'NONE', *, *, #63457, .F. ) ;
#68228=LINE ( 'NONE', #101513, #74566 ) ;
#68255=DIRECTION ( 'NONE',  ( 1.000000000000000000, 0.000000000000000000, 0.000000000000000000 ) ) ;
#68268=EDGE_CURVE ( 'NONE', #98637, #88783, #41603, .T. ) ;
#68318=ORIENTED_EDGE ( 'NONE', *, *, #141689, .T. ) ;
#68322=LINE ( 'NONE', #123404, #32356 ) ;
#68467=FACE_OUTER_BOUND ( 'NONE', #61021, .T. ) ;
#68480=DIRECTION ( 'NONE',  ( -0.5735764363510501562, 0.8191520442889890230, 1.003171929053521419E-16 ) ) ;
#68487=DIRECTION ( 'NONE',  ( -1.000000000000000000, -0.000000000000000000, -0.000000000000000000 ) ) ;
#68509=CARTESIAN_POINT ( 'NONE',  ( 5.443598275411213550, 3.821174125832445049E-16, 0.000000000000000000 ) ) ;
#68512=CARTESIAN_POINT ( 'NONE',  ( 1.146006882977913088, 0.4000000000000001332, -2.166563419957292957 ) ) ;
#68516=VERTEX_POINT ( 'NONE', #8077 ) ;
#68525=CIRCLE ( 'NONE', #19841, 2.500000000000000444 ) ;
#68536=CARTESIAN_POINT ( 'NONE',  ( 13.13598696172163116, -2.500000000000000000, 3.061616997868383634E-16 ) ) ;
#68546=VERTEX_POINT ( 'NONE', #104564 ) ;
#68567=DIRECTION ( 'NONE',  ( 0.000000000000000000, -1.000000000000000000, 0.000000000000000000 ) ) ;
#68580=EDGE_CURVE ( 'NONE', #69001, #83013, #103820, .T. ) ;
#68583=AXIS2_PLACEMENT_3D ( 'NONE', #62066, #49769, #5490 ) ;
#68644=PRESENTATION_STYLE_ASSIGNMENT (( #24395 ) ) ;
#68662=EDGE_CURVE ( 'NONE', #130434, #14650, #136242, .T. ) ;
#68674=ADVANCED_FACE ( 'NONE', ( #54492 ), #34424, .T. ) ;
#68680=DIRECTION ( 'NONE',  ( 1.000000000000000000, 1.224606353822377258E-16, 0.000000000000000000 ) ) ;
#68689=CARTESIAN_POINT ( 'NONE',  ( -12.69999999999998153, 0.000000000000000000, 0.000000000000000000 ) ) ;
#68698=CIRCLE ( 'NONE', #87201, 2.500000000000000444 ) ;
#68703=ORIENTED_EDGE ( 'NONE', *, *, #106769, .T. ) ;
#68739=CARTESIAN_POINT ( 'NONE',  ( 17.22560490425083657, 3.821174125832445049E-16, 0.000000000000000000 ) ) ;
#68757=SURFACE_STYLE_USAGE ( .BOTH. , #35429 ) ;
#68769=B_SPLINE_CURVE_WITH_KNOTS ( 'NONE', 3,
 ( #30940, #120027, #87456, #76597 ),
 .UNSPECIFIED., .F., .F.,
 ( 4, 4 ),
 ( 0.008853860144884175692, 0.009403245473020184833 ),
 .UNSPECIFIED. ) ;
#68795=DIRECTION ( 'NONE',  ( -1.000000000000000000, -1.224606353822377258E-16, -0.000000000000000000 ) ) ;
#68802=CARTESIAN_POINT ( 'NONE',  ( 5.281315875828549444, -2.500000000000000444, 3.061616997868384127E-16 ) ) ;
#68810=DIRECTION ( 'NONE',  ( 1.301042606982605074E-16, -1.000000000000000000, 0.000000000000000000 ) ) ;
#68868=AXIS2_PLACEMENT_3D ( 'NONE', #570, #77471, #22305 ) ;
#68889=DIRECTION ( 'NONE',  ( 0.000000000000000000, -1.000000000000000000, 0.000000000000000000 ) ) ;
#68894=DIRECTION ( 'NONE',  ( 0.000000000000000000, 0.000000000000000000, 1.000000000000000000 ) ) ;
#68897=ORIENTED_EDGE ( 'NONE', *, *, #85604, .F. ) ;
#68980=ORIENTED_EDGE ( 'NONE', *, *, #115252, .F. ) ;
#69001=VERTEX_POINT ( 'NONE', #97037 ) ;
#69023=ADVANCED_FACE ( 'NONE', ( #143434 ), #18233, .T. ) ;
#69052=AXIS2_PLACEMENT_3D ( 'NONE', #26853, #137781, #138486 ) ;
#69067=ORIENTED_EDGE ( 'NONE', *, *, #30106, .T. ) ;
#69144=ORIENTED_EDGE ( 'NONE', *, *, #24976, .T. ) ;
#69151=CIRCLE ( 'NONE', #6580, 2.500000000000000444 ) ;
#69155=CARTESIAN_POINT ( 'NONE',  ( 16.27785539607886633, 2.500000000000000444, 0.000000000000000000 ) ) ;
#69156=VERTEX_POINT ( 'NONE', #91240 ) ;
#69160=DIRECTION ( 'NONE',  ( 0.000000000000000000, -1.000000000000000000, 0.000000000000000000 ) ) ;
#69178=CARTESIAN_POINT ( 'NONE',  ( 4.495848767239241539, 4.584330080086930965E-16, 0.000000000000000000 ) ) ;
#69183=CARTESIAN_POINT ( 'NONE',  ( 7.799999601179139042, 3.821174125832445049E-16, 0.000000000000000000 ) ) ;
#69200=CARTESIAN_POINT ( 'NONE',  ( -12.69999999999998153, 3.061616997868383634E-16, -2.500000000000000444 ) ) ;
#69262=DIRECTION ( 'NONE',  ( -1.000000000000000000, -1.224606353822377258E-16, -0.000000000000000000 ) ) ;
#69267=VERTEX_POINT ( 'NONE', #139005 ) ;
#69270=DIRECTION ( 'NONE',  ( -1.000000000000000000, -1.224606353822377258E-16, -0.000000000000000000 ) ) ;
#69361=ORIENTED_EDGE ( 'NONE', *, *, #99021, .F. ) ;
#69367=EDGE_CURVE ( 'NONE', #34230, #22757, #87611, .T. ) ;
#69385=ORIENTED_EDGE ( 'NONE', *, *, #80867, .F. ) ;
#69386=CARTESIAN_POINT ( 'NONE',  ( 16.75173015016484968, 4.202752102959690472E-16, 0.000000000000000000 ) ) ;
#69393=CYLINDRICAL_SURFACE ( 'NONE', #115610, 2.500000000000000444 ) ;
#69402=DIRECTION ( 'NONE',  ( 0.000000000000000000, 1.000000000000000000, 0.000000000000000000 ) ) ;
#69415=CONICAL_SURFACE ( 'NONE', #6837, 2.055000000000000160, 1.047197551196600962 ) ;
#69425=CARTESIAN_POINT ( 'NONE',  ( 21.46453280170069888, -2.055000000000000160, 2.689687640572715640E-16 ) ) ;
#69438=EDGE_CURVE ( 'NONE', #103754, #13745, #85306, .T. ) ;
#69456=ORIENTED_EDGE ( 'NONE', *, *, #88408, .F. ) ;
#69462=EDGE_CURVE ( 'NONE', #66625, #53418, #46038, .T. ) ;
#69478=EDGE_CURVE ( 'NONE', #98372, #8776, #94524, .T. ) ;
#69559=ORIENTED_EDGE ( 'NONE', *, *, #121073, .F. ) ;
#69593=ORIENTED_EDGE ( 'NONE', *, *, #88367, .F. ) ;
#69601=ORIENTED_EDGE ( 'NONE', *, *, #142124, .F. ) ;
#69610=FACE_OUTER_BOUND ( 'NONE', #20727, .T. ) ;
#69617=ORIENTED_EDGE ( 'NONE', *, *, #92965, .T. ) ;
#69656=EDGE_CURVE ( 'NONE', #43279, #82989, #60589, .T. ) ;
#69680=CARTESIAN_POINT ( 'NONE',  ( 7.637717201596474048, -2.500000000000000444, 3.061616997868384127E-16 ) ) ;
#69690=LINE ( 'NONE', #16695, #138890 ) ;
#69707=CARTESIAN_POINT ( 'NONE',  ( 0.2569208697893814453, 4.202752102959690472E-16, 0.000000000000000000 ) ) ;
#69720=DIRECTION ( 'NONE',  ( 0.000000000000000000, -1.000000000000000000, 0.000000000000000000 ) ) ;
#69751=CARTESIAN_POINT ( 'NONE',  ( 7.799999601179139042, 3.061616997868383634E-16, -2.500000000000000444 ) ) ;
#69764=ORIENTED_EDGE ( 'NONE', *, *, #22906, .F. ) ;
#69810=ORIENTED_EDGE ( 'NONE', *, *, #52981, .F. ) ;
#69852=VECTOR ( 'NONE', #92380, 1000.000000000000000 ) ;
#69853=DIRECTION ( 'NONE',  ( 0.000000000000000000, 1.000000000000000000, 0.000000000000000000 ) ) ;
#69868=CARTESIAN_POINT ( 'NONE',  ( 5.281315875828549444, -2.500000000000000000, 3.061616997868383634E-16 ) ) ;
#69885=APPLICATION_CONTEXT ( 'automotive_design' ) ;
#69921=CARTESIAN_POINT ( 'NONE',  ( 0.1161069444170877152, -0.3999999999999998002, -2.220360628129161906 ) ) ;
#69960=DIRECTION ( 'NONE',  ( -1.000000000000000000, -0.000000000000000000, -0.000000000000000000 ) ) ;
#69990=LINE ( 'NONE', #93831, #69852 ) ;
#70006=LINE ( 'NONE', #3257, #20032 ) ;
#70015=CARTESIAN_POINT ( 'NONE',  ( 18.01107201284014536, -2.499999999999996447, 0.000000000000000000 ) ) ;
#70027=ADVANCED_FACE ( 'NONE', ( #136322 ), #133666, .T. ) ;
#70056=EDGE_CURVE ( 'NONE', #116730, #46699, #97073, .T. ) ;
#70057=DIRECTION ( 'NONE',  ( -1.000000000000000000, -0.000000000000000000, -0.000000000000000000 ) ) ;
#70115=ADVANCED_FACE ( 'NONE', ( #94944 ), #73947, .T. ) ;
#70123=ORIENTED_EDGE ( 'NONE', *, *, #34376, .F. ) ;
#70133=FACE_OUTER_BOUND ( 'NONE', #103538, .T. ) ;
#70178=ORIENTED_EDGE ( 'NONE', *, *, #71622, .F. ) ;
#70197=CARTESIAN_POINT ( 'NONE',  ( 15.65467068707222076, 2.499999999999998224, 3.061616997868380183E-16 ) ) ;
#70210=CONICAL_SURFACE ( 'NONE', #44748, 2.055000000000000604, 0.9599310885968764806 ) ;
#70275=CIRCLE ( 'NONE', #7704, 2.500000000000000444 ) ;
#70346=FACE_OUTER_BOUND ( 'NONE', #112777, .T. ) ;
#70386=ADVANCED_FACE ( 'NONE', ( #73427 ), #106296, .T. ) ;
#70411=AXIS2_PLACEMENT_3D ( 'NONE', #2646, #80256, #34589 ) ;
#70431=AXIS2_PLACEMENT_3D ( 'NONE', #36870, #85367, #39025 ) ;
#70440=CYLINDRICAL_SURFACE ( 'NONE', #115888, 2.500000000000000444 ) ;
#70448=CARTESIAN_POINT ( 'NONE',  ( 6.066782984417857350, 4.584330080086930965E-16, 0.000000000000000000 ) ) ;
#70472=ORIENTED_EDGE ( 'NONE', *, *, #16788, .T. ) ;
#70474=ORIENTED_EDGE ( 'NONE', *, *, #28782, .F. ) ;
#70483=VERTEX_POINT ( 'NONE', #10970 ) ;
#70501=CIRCLE ( 'NONE', #121545, 2.500000000000000444 ) ;
#70508=CONICAL_SURFACE ( 'NONE', #137627, 2.055000000000000604, 0.9599310885968764806 ) ;
#70512=EDGE_CURVE ( 'NONE', #120212, #128359, #46357, .T. ) ;
#70533=CARTESIAN_POINT ( 'NONE',  ( 0.07735809023238571225, 0.3999999999999995781, 2.152165253127958700 ) ) ;
#70561=CYLINDRICAL_SURFACE ( 'NONE', #122914, 2.500000000000000444 ) ;
#70577=EDGE_LOOP ( 'NONE', ( #8838, #52299, #96414, #64886, #76615 ) ) ;
#70601=DIRECTION ( 'NONE',  ( 0.000000000000000000, -1.000000000000000000, 0.000000000000000000 ) ) ;
#70618=ORIENTED_EDGE ( 'NONE', *, *, #129527, .T. ) ;
#70630=ORIENTED_EDGE ( 'NONE', *, *, #132798, .F. ) ;
#70640=DIRECTION ( 'NONE',  ( -1.000000000000000000, -1.224606353822377258E-16, -0.000000000000000000 ) ) ;
#70682=DIRECTION ( 'NONE',  ( 0.000000000000000000, -1.000000000000000000, 0.000000000000000000 ) ) ;
#70684=DIRECTION ( 'NONE',  ( 0.000000000000000000, -1.000000000000000000, 0.000000000000000000 ) ) ;
#70720=EDGE_LOOP ( 'NONE', ( #141333, #140097, #13115, #50361, #125949 ) ) ;
#70725=ADVANCED_FACE ( 'NONE', ( #113155 ), #41650, .T. ) ;
#70752=DIRECTION ( 'NONE',  ( -1.000000000000000000, -0.000000000000000000, 0.000000000000000000 ) ) ;
#70759=EDGE_LOOP ( 'NONE', ( #95004, #42605, #77725, #93967, #89732 ) ) ;
#70761=AXIS2_PLACEMENT_3D ( 'NONE', #142357, #43047, #24657 ) ;
#70777=AXIS2_PLACEMENT_3D ( 'NONE', #8358, #41028, #141791 ) ;
#70790=DIRECTION ( 'NONE',  ( -1.000000000000000000, -1.224606353822377258E-16, -0.000000000000000000 ) ) ;
#70794=CARTESIAN_POINT ( 'NONE',  ( 8.423184310185783730, 2.500000000000000888, 0.000000000000000000 ) ) ;
#70840=B_SPLINE_CURVE_WITH_KNOTS ( 'NONE', 3,
 ( #44330, #133462, #77662, #123317 ),
 .UNSPECIFIED., .F., .F.,
 ( 4, 4 ),
 ( 0.008851590069444708123, 0.009100162336955338813 ),
 .UNSPECIFIED. ) ;
#70858=CARTESIAN_POINT ( 'NONE',  ( 15.49238828748955576, 3.061616997868383634E-16, -2.500000000000000444 ) ) ;
#70873=ORIENTED_EDGE ( 'NONE', *, *, #110596, .T. ) ;
#70903=ADVANCED_FACE ( 'NONE', ( #72579 ), #69415, .T. ) ;
#70981=CIRCLE ( 'NONE', #117290, 2.055000000000000604 ) ;
#71036=ORIENTED_EDGE ( 'NONE', *, *, #77234, .T. ) ;
#71051=CIRCLE ( 'NONE', #131254, 2.500000000000000444 ) ;
#71093=VERTEX_POINT ( 'NONE', #47787 ) ;
#71106=EDGE_CURVE ( 'NONE', #74147, #69156, #55639, .T. ) ;
#71193=EDGE_LOOP ( 'NONE', ( #126853, #67385, #31275, #138416, #10208 ) ) ;
#71194=DIRECTION ( 'NONE',  ( 0.000000000000000000, -1.000000000000000000, 0.000000000000000000 ) ) ;
#71212=LINE ( 'NONE', #16803, #78761 ) ;
#71214=ORIENTED_EDGE ( 'NONE', *, *, #127537, .T. ) ;
#71295=AXIS2_PLACEMENT_3D ( 'NONE', #92253, #104578, #39345 ) ;
#71317=CARTESIAN_POINT ( 'NONE',  ( 21.46453280170069888, 2.055000000000001048, 2.516649172247811554E-16 ) ) ;
#71323=CARTESIAN_POINT ( 'NONE',  ( 9.994118527364397764, 4.584330080086930965E-16, 0.000000000000000000 ) ) ;
#71335=CARTESIAN_POINT ( 'NONE',  ( 11.25346039003969523, 4.202752102959690472E-16, 0.000000000000000000 ) ) ;
#71354=CARTESIAN_POINT ( 'NONE',  ( 3.872664058232598183, 3.821174125832445049E-16, 0.000000000000000000 ) ) ;
#71386=CYLINDRICAL_SURFACE ( 'NONE', #66333, 2.500000000000000444 ) ;
#71397=DIRECTION ( 'NONE',  ( 0.000000000000000000, -1.000000000000000000, 0.000000000000000000 ) ) ;
#71420=CARTESIAN_POINT ( 'NONE',  ( 14.39532882439692862, 2.055000000000001048, 2.516649172247811554E-16 ) ) ;
#71445=DIRECTION ( 'NONE',  ( 0.000000000000000000, -1.000000000000000000, 0.000000000000000000 ) ) ;
#71514=AXIS2_PLACEMENT_3D ( 'NONE', #119652, #20348, #97175 ) ;
#71537=FACE_OUTER_BOUND ( 'NONE', #17455, .T. ) ;
#71583=VERTEX_POINT ( 'NONE', #30664 ) ;
#71617=EDGE_CURVE ( 'NONE', #80430, #121119, #99699, .T. ) ;
#71622=EDGE_CURVE ( 'NONE', #12905, #73407, #55744, .T. ) ;
#71642=FACE_OUTER_BOUND ( 'NONE', #141409, .T. ) ;
#71648=FACE_OUTER_BOUND ( 'NONE', #93628, .T. ) ;
#71650=ORIENTED_EDGE ( 'NONE', *, *, #49564, .T. ) ;
#71715=DIRECTION ( 'NONE',  ( -1.000000000000000000, -0.000000000000000000, -0.000000000000000000 ) ) ;
#71773=DIRECTION ( 'NONE',  ( 0.000000000000000000, -1.000000000000000000, 0.000000000000000000 ) ) ;
#71790=VECTOR ( 'NONE', #84185, 1000.000000000000000 ) ;
#71899=EDGE_LOOP ( 'NONE', ( #68221, #110035, #38221, #67122, #69144, #56077, #2962, #69559 ) ) ;
#71904=ORIENTED_EDGE ( 'NONE', *, *, #123998, .F. ) ;
#71909=AXIS2_PLACEMENT_3D ( 'NONE', #37599, #4904, #26707 ) ;
#71972=DIRECTION ( 'NONE',  ( 0.000000000000000000, 0.000000000000000000, 1.000000000000000000 ) ) ;
#72022=DIRECTION ( 'NONE',  ( -1.000000000000000000, -0.000000000000000000, -0.000000000000000000 ) ) ;
#72045=AXIS2_PLACEMENT_3D ( 'NONE', #82468, #51812, #106869 ) ;
#72062=ORIENTED_EDGE ( 'NONE', *, *, #131248, .F. ) ;
#72128=DIRECTION ( 'NONE',  ( -1.000000000000000000, -1.224606353822377258E-16, -0.000000000000000000 ) ) ;
#72150=FACE_OUTER_BOUND ( 'NONE', #66864, .T. ) ;
#72195=CIRCLE ( 'NONE', #14183, 2.055000000000000604 ) ;
#72211=EDGE_LOOP ( 'NONE', ( #29319, #70618, #119926, #133036, #74430, #127738 ) ) ;
#72216=AXIS2_PLACEMENT_3D ( 'NONE', #93939, #138173, #27978 ) ;
#72271=ORIENTED_EDGE ( 'NONE', *, *, #87199, .F. ) ;
#72297=CARTESIAN_POINT ( 'NONE',  ( 11.25346039003969523, -2.055000000000000160, 0.000000000000000000 ) ) ;
#72330=CONICAL_SURFACE ( 'NONE', #141729, 2.500000000000000444, 0.9599310885968830309 ) ;
#72341=B_SPLINE_CURVE_WITH_KNOTS ( 'NONE', 3,
 ( #26270, #94361, #70533, #105245 ),
 .UNSPECIFIED., .F., .F.,
 ( 4, 4 ),
 ( 0.008519363277820955760, 0.008755597426397563471 ),
 .UNSPECIFIED. ) ;
#72352=ORIENTED_EDGE ( 'NONE', *, *, #143117, .F. ) ;
#72373=CARTESIAN_POINT ( 'NONE',  ( 4.969723521325230209, 4.202752102959690472E-16, 0.000000000000000000 ) ) ;
#72374=ORIENTED_EDGE ( 'NONE', *, *, #64819, .T. ) ;
#72382=DIRECTION ( 'NONE',  ( 1.000000000000000000, 1.224606353822377258E-16, 0.000000000000000000 ) ) ;
#72417=CIRCLE ( 'NONE', #19181, 2.500000000000000444 ) ;
#72421=CIRCLE ( 'NONE', #83905, 2.500000000000000444 ) ;
#72496=FACE_OUTER_BOUND ( 'NONE', #85926, .T. ) ;
#72501=EDGE_LOOP ( 'NONE', ( #76811, #12310, #82550, #47161, #80945 ) ) ;
#72517=ORIENTED_EDGE ( 'NONE', *, *, #93795, .F. ) ;
#72579=FACE_OUTER_BOUND ( 'NONE', #27797, .T. ) ;
#72588=DIRECTION ( 'NONE',  ( -0.5735764363510501562, 0.8191520442889890230, 1.003171929053521419E-16 ) ) ;
#72635=ORIENTED_EDGE ( 'NONE', *, *, #117257, .F. ) ;
#72664=VECTOR ( 'NONE', #2850, 1000.000000000000000 ) ;
#72666=ORIENTED_EDGE ( 'NONE', *, *, #49930, .T. ) ;
#72698=AXIS2_PLACEMENT_3D ( 'NONE', #115077, #15749, #78957 ) ;
#72701=VERTEX_POINT ( 'NONE', #110675 ) ;
#72721=FACE_OUTER_BOUND ( 'NONE', #54938, .T. ) ;
#72826=PLANE ( 'NONE',  #81623 ) ;
#72829=DIRECTION ( 'NONE',  ( -1.000000000000000000, -1.224606353822377258E-16, -0.000000000000000000 ) ) ;
#72883=DIRECTION ( 'NONE',  ( -1.000000000000000000, -0.000000000000000000, -0.000000000000000000 ) ) ;
#72885=EDGE_CURVE ( 'NONE', #17540, #12905, #95384, .T. ) ;
#72898=ORIENTED_EDGE ( 'NONE', *, *, #8206, .T. ) ;
#72939=ORIENTED_EDGE ( 'NONE', *, *, #101437, .F. ) ;
#72980=EDGE_CURVE ( 'NONE', #22872, #11920, #123116, .T. ) ;
#72982=ORIENTED_EDGE ( 'NONE', *, *, #3398, .T. ) ;
#72990=AXIS2_PLACEMENT_3D ( 'NONE', #74325, #143129, #109788 ) ;
#73007=DIRECTION ( 'NONE',  ( -0.5735764363510499342, -0.8191520442889891340, 0.000000000000000000 ) ) ;
#73012=EDGE_CURVE ( 'NONE', #108385, #33386, #32547, .T. ) ;
#73075=AXIS2_PLACEMENT_3D ( 'NONE', #14484, #124671, #24638 ) ;
#73076=CONICAL_SURFACE ( 'NONE', #38282, 2.500000000000000444, 0.9599310885968830309 ) ;
#73086=ORIENTED_EDGE ( 'NONE', *, *, #32196, .F. ) ;
#73093=ORIENTED_EDGE ( 'NONE', *, *, #61221, .T. ) ;
#73116=CARTESIAN_POINT ( 'NONE',  ( 12.82439460721831104, 4.202752102959690472E-16, 0.000000000000000000 ) ) ;
#73144=DIRECTION ( 'NONE',  ( 0.000000000000000000, -1.000000000000000000, 0.000000000000000000 ) ) ;
#73171=DIRECTION ( 'NONE',  ( 0.5735764363510448272, -0.8191520442889927978, 1.003171929053526103E-16 ) ) ;
#73201=DIRECTION ( 'NONE',  ( 0.000000000000000000, 0.000000000000000000, 1.000000000000000000 ) ) ;
#73206=EDGE_CURVE ( 'NONE', #34286, #108094, #16010, .T. ) ;
#73242=ADVANCED_FACE ( 'NONE', ( #137851 ), #30252, .T. ) ;
#73260=CARTESIAN_POINT ( 'NONE',  ( -12.69999999999998153, 3.061616997868383634E-16, -2.500000000000000444 ) ) ;
#73287=VERTEX_POINT ( 'NONE', #798 ) ;
#73316=VERTEX_POINT ( 'NONE', #36833 ) ;
#73321=AXIS2_PLACEMENT_3D ( 'NONE', #122858, #56224, #80795 ) ;
#73324=ORIENTED_EDGE ( 'NONE', *, *, #42802, .T. ) ;
#73378=EDGE_CURVE ( 'NONE', #44903, #59504, #62672, .T. ) ;
#73381=VERTEX_POINT ( 'NONE', #136150 ) ;
#73407=VERTEX_POINT ( 'NONE', #114397 ) ;
#73409=VECTOR ( 'NONE', #3180, 1000.000000000000000 ) ;
#73427=FACE_OUTER_BOUND ( 'NONE', #29109, .T. ) ;
#73442=ORIENTED_EDGE ( 'NONE', *, *, #70512, .T. ) ;
#73501=DIRECTION ( 'NONE',  ( 0.000000000000000000, -1.000000000000000000, 0.000000000000000000 ) ) ;
#73519=CARTESIAN_POINT ( 'NONE',  ( -12.69999999999998153, 0.000000000000000000, 0.000000000000000000 ) ) ;
#73566=ORIENTED_EDGE ( 'NONE', *, *, #121981, .T. ) ;
#73586=ORIENTED_EDGE ( 'NONE', *, *, #106256, .T. ) ;
#73617=CARTESIAN_POINT ( 'NONE',  ( 12.03892749862900402, 4.202752102959690472E-16, 0.000000000000000000 ) ) ;
#73647=ORIENTED_EDGE ( 'NONE', *, *, #22906, .T. ) ;
#73650=VERTEX_POINT ( 'NONE', #17432 ) ;
#73700=DIRECTION ( 'NONE',  ( 0.000000000000000000, 0.000000000000000000, 1.000000000000000000 ) ) ;
#73702=ORIENTED_EDGE ( 'NONE', *, *, #9613, .F. ) ;
#73708=EDGE_LOOP ( 'NONE', ( #137061, #93200, #32978, #139252, #131056 ) ) ;
#73740=VECTOR ( 'NONE', #52321, 999.9999999999998863 ) ;
#73752=AXIS2_PLACEMENT_3D ( 'NONE', #72373, #29512, #117222 ) ;
#73762=CARTESIAN_POINT ( 'NONE',  ( 11.72733514412567857, -2.500000000000001776, 0.000000000000000000 ) ) ;
#73787=AXIS2_PLACEMENT_3D ( 'NONE', #62985, #62256, #73144 ) ;
#73809=CARTESIAN_POINT ( 'NONE',  ( 13.60986171580761805, 4.202752102959690472E-16, 0.000000000000000000 ) ) ;
#73846=CIRCLE ( 'NONE', #59993, 2.055000000000000604 ) ;
#73871=DIRECTION ( 'NONE',  ( 0.5735764363510444941, 0.8191520442889929088, 0.000000000000000000 ) ) ;
#73912=CARTESIAN_POINT ( 'NONE',  ( 5.281315875828549444, 4.584330080086930965E-16, 0.000000000000000000 ) ) ;
#73947=CONICAL_SURFACE ( 'NONE', #136443, 2.500000000000000444, 0.9599310885968830309 ) ;
#74011=CONICAL_SURFACE ( 'NONE', #39359, 2.500000000000000444, 0.9599310885968830309 ) ;
#74043=VERTEX_POINT ( 'NONE', #131036 ) ;
#74100=CIRCLE ( 'NONE', #11550, 2.500000000000000444 ) ;
#74124=CARTESIAN_POINT ( 'NONE',  ( 18.63425672184678916, -2.500000000000000000, 3.061616997868383634E-16 ) ) ;
#74147=VERTEX_POINT ( 'NONE', #91119 ) ;
#74171=DIRECTION ( 'NONE',  ( 0.000000000000000000, 0.000000000000000000, -1.000000000000000000 ) ) ;
#74258=EDGE_CURVE ( 'NONE', #69001, #101876, #121564, .T. ) ;
#74274=CARTESIAN_POINT ( 'NONE',  ( -12.69999999999998153, 3.061616997868383634E-16, -2.500000000000000444 ) ) ;
#74276=CARTESIAN_POINT ( 'NONE',  ( 1.353980332882009252, 0.4000000000000001887, -2.467792535850613866 ) ) ;
#74290=EDGE_CURVE ( 'NONE', #87033, #117239, #95238, .T. ) ;
#74295=CIRCLE ( 'NONE', #132264, 2.055000000000000604 ) ;
#74299=VECTOR ( 'NONE', #67468, 1000.000000000000000 ) ;
#74325=CARTESIAN_POINT ( 'NONE',  ( 5.755190629914537226, 4.202752102959690472E-16, 0.000000000000000000 ) ) ;
#74330=EDGE_LOOP ( 'NONE', ( #85344, #69456, #48819, #26198, #140485 ) ) ;
#74348=EDGE_CURVE ( 'NONE', #139436, #18445, #15618, .T. ) ;
#74393=FACE_OUTER_BOUND ( 'NONE', #16981, .T. ) ;
#74430=ORIENTED_EDGE ( 'NONE', *, *, #36954, .F. ) ;
#74434=AXIS2_PLACEMENT_3D ( 'NONE', #11975, #103111, #92211 ) ;
#74446=DIRECTION ( 'NONE',  ( -1.000000000000000000, -0.000000000000000000, -0.000000000000000000 ) ) ;
#74455=EDGE_CURVE ( 'NONE', #124291, #18445, #134708, .T. ) ;
#74478=VECTOR ( 'NONE', #102185, 999.9999999999998863 ) ;
#74486=ORIENTED_EDGE ( 'NONE', *, *, #93418, .F. ) ;
#74488=ORIENTED_EDGE ( 'NONE', *, *, #128045, .F. ) ;
#74495=B_SPLINE_CURVE_WITH_KNOTS ( 'NONE', 3,
 ( #67175, #20795, #65047, #32410 ),
 .UNSPECIFIED., .F., .F.,
 ( 4, 4 ),
 ( 0.003785693138453204761, 0.004021000868919195545 ),
 .UNSPECIFIED. ) ;
#74523=CIRCLE ( 'NONE', #60688, 2.500000000000000444 ) ;
#74566=VECTOR ( 'NONE', #133452, 999.9999999999998863 ) ;
#74573=CIRCLE ( 'NONE', #104657, 2.055000000000000604 ) ;
#74590=ORIENTED_EDGE ( 'NONE', *, *, #52543, .T. ) ;
#74672=VECTOR ( 'NONE', #68480, 999.9999999999998863 ) ;
#74719=DIRECTION ( 'NONE',  ( 0.000000000000000000, -1.000000000000000000, 0.000000000000000000 ) ) ;
#74741=FACE_OUTER_BOUND ( 'NONE', #92839, .T. ) ;
#74758=ORIENTED_EDGE ( 'NONE', *, *, #43307, .T. ) ;
#74827=DIRECTION ( 'NONE',  ( -1.734723475976806848E-16, 1.000000000000000000, 0.000000000000000000 ) ) ;
#74884=AXIS2_PLACEMENT_3D ( 'NONE', #6525, #93601, #18878 ) ;
#74965=ORIENTED_EDGE ( 'NONE', *, *, #125848, .F. ) ;
#75002=ADVANCED_FACE ( 'NONE', ( #97307 ), #5065, .T. ) ;
#75042=ORIENTED_EDGE ( 'NONE', *, *, #58617, .F. ) ;
#75058=ORIENTED_EDGE ( 'NONE', *, *, #81486, .F. ) ;
#75071=CARTESIAN_POINT ( 'NONE',  ( 18.79653912142945060, 3.821174125832445049E-16, 0.000000000000000000 ) ) ;
#75100=ORIENTED_EDGE ( 'NONE', *, *, #120601, .T. ) ;
#75113=ORIENTED_EDGE ( 'NONE', *, *, #142595, .T. ) ;
#75125=ADVANCED_FACE ( 'NONE', ( #860 ), #88534, .T. ) ;
#75126=CIRCLE ( 'NONE', #70777, 2.055000000000000604 ) ;
#75189=ORIENTED_EDGE ( 'NONE', *, *, #77304, .F. ) ;
#75196=DIRECTION ( 'NONE',  ( 1.734723475976806848E-16, -1.000000000000000000, 0.000000000000000000 ) ) ;
#75201=ORIENTED_EDGE ( 'NONE', *, *, #18214, .T. ) ;
#75223=CARTESIAN_POINT ( 'NONE',  ( 19.58200623001875940, 3.821174125832445049E-16, 0.000000000000000000 ) ) ;
#75276=DIRECTION ( 'NONE',  ( 2.110369192185896011E-16, -1.000000000000000000, 0.000000000000000000 ) ) ;
#75285=DIRECTION ( 'NONE',  ( -1.000000000000000000, -1.224606353822377258E-16, -0.000000000000000000 ) ) ;
#75302=CARTESIAN_POINT ( 'NONE',  ( 1.353980332882009252, 0.3999999999999995226, 2.467792535850613866 ) ) ;
#75327=DIRECTION ( 'NONE',  ( -1.000000000000000000, -1.224606353822377258E-16, -0.000000000000000000 ) ) ;
#75341=CONICAL_SURFACE ( 'NONE', #12793, 2.055000000000000604, 0.9599310885968764806 ) ;
#75363=CARTESIAN_POINT ( 'NONE',  ( 1.554198602559970332, 0.4000000000000001887, -2.412907414356850300 ) ) ;
#75395=EDGE_CURVE ( 'NONE', #126332, #126491, #16806, .T. ) ;
#75396=CONICAL_SURFACE ( 'NONE', #12863, 2.500000000000000444, 0.9599310885968830309 ) ;
#75421=LINE ( 'NONE', #94992, #28069 ) ;
#75427=ORIENTED_EDGE ( 'NONE', *, *, #29156, .F. ) ;
#75451=ORIENTED_EDGE ( 'NONE', *, *, #83173, .F. ) ;
#75461=DIRECTION ( 'NONE',  ( -1.000000000000000000, -1.224606353822377258E-16, -0.000000000000000000 ) ) ;
#75559=ORIENTED_EDGE ( 'NONE', *, *, #16759, .T. ) ;
#75567=CARTESIAN_POINT ( 'NONE',  ( 19.10813147593277250, 4.202752102959690472E-16, 0.000000000000000000 ) ) ;
#75589=CARTESIAN_POINT ( 'NONE',  ( 15.49238828748955576, 4.584330080086930965E-16, 0.000000000000000000 ) ) ;
#75604=AXIS2_PLACEMENT_3D ( 'NONE', #4677, #48977, #104765 ) ;
#75666=CARTESIAN_POINT ( 'NONE',  ( 17.06332250466817158, 4.584330080086930965E-16, 0.000000000000000000 ) ) ;
#75670=CARTESIAN_POINT ( 'NONE',  ( 0.000000000000000000, -0.4000000000000003553, 2.015694669338588429 ) ) ;
#75688=EDGE_CURVE ( 'NONE', #53690, #122791, #84547, .T. ) ;
#75707=AXIS2_PLACEMENT_3D ( 'NONE', #58110, #23268, #21862 ) ;
#75718=DIRECTION ( 'NONE',  ( 1.000000000000000000, 1.224606353822377258E-16, 0.000000000000000000 ) ) ;
#75772=ORIENTED_EDGE ( 'NONE', *, *, #52834, .F. ) ;
#75808=LINE ( 'NONE', #52606, #44967 ) ;
#75811=DIRECTION ( 'NONE',  ( -1.000000000000000000, -1.224606353822377258E-16, -0.000000000000000000 ) ) ;
#75845=AXIS2_PLACEMENT_3D ( 'NONE', #102107, #13631, #112268 ) ;
#75855=FACE_OUTER_BOUND ( 'NONE', #26930, .T. ) ;
#75913=CARTESIAN_POINT ( 'NONE',  ( 7.326124847093153925, 4.202752102959690472E-16, 0.000000000000000000 ) ) ;
#75916=AXIS2_PLACEMENT_3D ( 'NONE', #35739, #35006, #125578 ) ;
#75950=VERTEX_POINT ( 'NONE', #67816 ) ;
#75974=CARTESIAN_POINT ( 'NONE',  ( 18.01107201284014536, 4.333342374871280669E-31, 2.500000000000000444 ) ) ;
#75992=VERTEX_POINT ( 'NONE', #27106 ) ;
#76042=ADVANCED_FACE ( 'NONE', ( #48165 ), #62656, .T. ) ;
#76144=VECTOR ( 'NONE', #87893, 1000.000000000000000 ) ;
#76176=DIRECTION ( 'NONE',  ( -1.000000000000000000, -1.224606353822377258E-16, -0.000000000000000000 ) ) ;
#76184=FACE_OUTER_BOUND ( 'NONE', #8072, .T. ) ;
#76190=VERTEX_POINT ( 'NONE', #64037 ) ;
#76256=DIRECTION ( 'NONE',  ( -1.000000000000000000, -0.000000000000000000, -0.000000000000000000 ) ) ;
#76278=DIRECTION ( 'NONE',  ( -1.000000000000000000, -0.000000000000000000, -0.000000000000000000 ) ) ;
#76286=DIRECTION ( 'NONE',  ( -1.000000000000000000, -1.224606353822377258E-16, -0.000000000000000000 ) ) ;
#76308=CARTESIAN_POINT ( 'NONE',  ( 6.852250093007166143, 3.061616997868383634E-16, -2.500000000000000444 ) ) ;
#76332=ORIENTED_EDGE ( 'NONE', *, *, #130789, .F. ) ;
#76336=CIRCLE ( 'NONE', #111062, 2.500000000000000444 ) ;
#76338=ORIENTED_EDGE ( 'NONE', *, *, #101258, .F. ) ;
#76366=CIRCLE ( 'NONE', #92472, 2.500000000000000444 ) ;
#76383=ADVANCED_FACE ( 'NONE', ( #12490 ), #18626, .T. ) ;
#76389=CARTESIAN_POINT ( 'NONE',  ( 17.22560490425083657, -2.499999999999996447, 0.000000000000000000 ) ) ;
#76426=FACE_OUTER_BOUND ( 'NONE', #95916, .T. ) ;
#76515=CARTESIAN_POINT ( 'NONE',  ( 8.897059064271770623, 2.055000000000001048, 0.000000000000000000 ) ) ;
#76523=VECTOR ( 'NONE', #78984, 1000.000000000000000 ) ;
#76525=VERTEX_POINT ( 'NONE', #131263 ) ;
#76551=ORIENTED_EDGE ( 'NONE', *, *, #42812, .F. ) ;
#76597=CARTESIAN_POINT ( 'NONE',  ( 1.353980332882009252, -0.3999999999999997446, -2.467792535850613866 ) ) ;
#76604=CONICAL_SURFACE ( 'NONE', #4798, 2.500000000000000444, 0.9599310885968830309 ) ;
#76605=DIRECTION ( 'NONE',  ( 0.000000000000000000, 1.000000000000000000, 0.000000000000000000 ) ) ;
#76615=ORIENTED_EDGE ( 'NONE', *, *, #97105, .F. ) ;
#76665=CARTESIAN_POINT ( 'NONE',  ( 8.423184310185783730, 4.584330080086930965E-16, 0.000000000000000000 ) ) ;
#76679=EDGE_LOOP ( 'NONE', ( #127850, #80687, #140853, #34235 ) ) ;
#76691=LINE ( 'NONE', #21573, #106783 ) ;
#76748=ORIENTED_EDGE ( 'NONE', *, *, #3398, .F. ) ;
#76755=LINE ( 'NONE', #120934, #40851 ) ;
#76802=DIRECTION ( 'NONE',  ( -1.000000000000000000, -0.000000000000000000, -0.000000000000000000 ) ) ;
#76811=ORIENTED_EDGE ( 'NONE', *, *, #131432, .F. ) ;
#76874=CONICAL_SURFACE ( 'NONE', #86050, 2.500000000000000444, 0.9599310885968830309 ) ;
#76906=AXIS2_PLACEMENT_3D ( 'NONE', #82013, #47264, #94263 ) ;
#76915=ORIENTED_EDGE ( 'NONE', *, *, #140662, .F. ) ;
#76929=FACE_OUTER_BOUND ( 'NONE', #109746, .T. ) ;
#76954=EDGE_CURVE ( 'NONE', #62751, #66606, #107872, .T. ) ;
#76972=EDGE_CURVE ( 'NONE', #56350, #140092, #109085, .T. ) ;
#76998=CARTESIAN_POINT ( 'NONE',  ( 1.042387978378689573, 4.202752102959690472E-16, 0.000000000000000000 ) ) ;
#77000=CIRCLE ( 'NONE', #14470, 2.500000000000000444 ) ;
#77003=ORIENTED_EDGE ( 'NONE', *, *, #24289, .F. ) ;
#77032=ORIENTED_EDGE ( 'NONE', *, *, #85898, .F. ) ;
#77050=CARTESIAN_POINT ( 'NONE',  ( 17.22560490425083657, 3.821174125832445049E-16, 0.000000000000000000 ) ) ;
#77064=AXIS2_PLACEMENT_3D ( 'NONE', #122778, #12583, #23465 ) ;
#77087=LINE ( 'NONE', #9629, #93160 ) ;
#77103=ADVANCED_FACE ( 'NONE', ( #33767 ), #30457, .T. ) ;
#77119=DIRECTION ( 'NONE',  ( 0.000000000000000000, 1.000000000000000000, 0.000000000000000000 ) ) ;
#77124=CARTESIAN_POINT ( 'NONE',  ( 14.70692117890024697, 4.584330080086930965E-16, 0.000000000000000000 ) ) ;
#77132=LINE ( 'NONE', #66239, #27885 ) ;
#77139=CARTESIAN_POINT ( 'NONE',  ( 9.370933818357753964, 3.821174125832445049E-16, 0.000000000000000000 ) ) ;
#77150=CARTESIAN_POINT ( 'NONE',  ( 0.9387690737794645024, 0.3999999999999995781, 2.166563419957292957 ) ) ;
#77154=CIRCLE ( 'NONE', #88731, 2.500000000000000444 ) ;
#77196=EDGE_CURVE ( 'NONE', #111882, #15565, #112029, .T. ) ;
#77216=DIRECTION ( 'NONE',  ( 1.000000000000000000, 1.224606353822377258E-16, 0.000000000000000000 ) ) ;
#77224=EDGE_CURVE ( 'NONE', #33411, #19554, #14830, .T. ) ;
#77229=ORIENTED_EDGE ( 'NONE', *, *, #35869, .T. ) ;
#77234=EDGE_CURVE ( 'NONE', #111457, #103339, #26434, .T. ) ;
#77304=EDGE_CURVE ( 'NONE', #96600, #41872, #7357, .T. ) ;
#77315=VERTEX_POINT ( 'NONE', #114832 ) ;
#77332=VECTOR ( 'NONE', #84125, 999.9999999999998863 ) ;
#77333=DIRECTION ( 'NONE',  ( 1.000000000000000000, 1.224606353822377258E-16, 0.000000000000000000 ) ) ;
#77427=DIRECTION ( 'NONE',  ( 1.201410254241279878E-16, -1.000000000000000000, 0.000000000000000000 ) ) ;
#77431=FACE_OUTER_BOUND ( 'NONE', #63099, .T. ) ;
#77455=ADVANCED_FACE ( 'NONE', ( #41360 ), #106803, .T. ) ;
#77471=DIRECTION ( 'NONE',  ( -1.000000000000000000, -0.000000000000000000, -0.000000000000000000 ) ) ;
#77480=CARTESIAN_POINT ( 'NONE',  ( 6.540657738503846907, 4.202752102959690472E-16, 0.000000000000000000 ) ) ;
#77516=ORIENTED_EDGE ( 'NONE', *, *, #141495, .T. ) ;
#77587=ORIENTED_EDGE ( 'NONE', *, *, #123480, .F. ) ;
#77612=CARTESIAN_POINT ( 'NONE',  ( 22.25000000000000000, 0.000000000000000000, 1.749999999999999778 ) ) ;
#77615=CARTESIAN_POINT ( 'NONE',  ( 2.924914550060625285, 4.584330080086930965E-16, 0.000000000000000000 ) ) ;
#77662=CARTESIAN_POINT ( 'NONE',  ( 0.1630955410174104447, 0.4000000000000001332, -2.152173700565807479 ) ) ;
#77670=EDGE_CURVE ( 'NONE', #95691, #3259, #118503, .T. ) ;
#77710=CIRCLE ( 'NONE', #29159, 2.500000000000000444 ) ;
#77725=ORIENTED_EDGE ( 'NONE', *, *, #81155, .T. ) ;
#77726=VECTOR ( 'NONE', #130350, 999.9999999999998863 ) ;
#77742=DIRECTION ( 'NONE',  ( 0.5735764363510444941, 0.8191520442889929088, 0.000000000000000000 ) ) ;
#77804=CARTESIAN_POINT ( 'NONE',  ( 9.208651418775088970, 2.500000000000000444, 0.000000000000000000 ) ) ;
#77878=CARTESIAN_POINT ( 'NONE',  ( 0.7307956238753654521, -0.4000000000000004108, 2.467792535850613866 ) ) ;
#77930=AXIS2_PLACEMENT_3D ( 'NONE', #106418, #71715, #139109 ) ;
#77938=ORIENTED_EDGE ( 'NONE', *, *, #128523, .F. ) ;
#77954=EDGE_CURVE ( 'NONE', #61275, #24150, #88945, .T. ) ;
#77959=CARTESIAN_POINT ( 'NONE',  ( 17.06332250466817158, 2.500000000000000444, 0.000000000000000000 ) ) ;
#78004=CARTESIAN_POINT ( 'NONE',  ( 21.15294044719737698, 3.061616997868383634E-16, -2.500000000000000444 ) ) ;
#78013=EDGE_CURVE ( 'NONE', #73316, #58598, #77087, .T. ) ;
#78015=DIRECTION ( 'NONE',  ( -1.000000000000000000, -1.224606353822377258E-16, -0.000000000000000000 ) ) ;
#78040=CARTESIAN_POINT ( 'NONE',  ( 1.629999999999999893, 4.202752102959690472E-16, -4.330509084666861676E-16 ) ) ;
#78070=ADVANCED_FACE ( 'NONE', ( #104508 ), #83984, .T. ) ;
#78090=ORIENTED_EDGE ( 'NONE', *, *, #9532, .F. ) ;
#78118=CARTESIAN_POINT ( 'NONE',  ( 7.637717201596474048, 4.584330080086930965E-16, 0.000000000000000000 ) ) ;
#78120=ORIENTED_EDGE ( 'NONE', *, *, #8760, .T. ) ;
#78146=VERTEX_POINT ( 'NONE', #35005 ) ;
#78169=AXIS2_PLACEMENT_3D ( 'NONE', #65729, #88156, #107735 ) ;
#78175=DIRECTION ( 'NONE',  ( 0.000000000000000000, 0.000000000000000000, 1.000000000000000000 ) ) ;
#78222=EDGE_CURVE ( 'NONE', #129512, #53690, #58554, .T. ) ;
#78255=CIRCLE ( 'NONE', #15687, 2.500000000000000444 ) ;
#78278=CARTESIAN_POINT ( 'NONE',  ( 10.46799328145038821, -2.055000000000000160, 0.000000000000000000 ) ) ;
#78329=DIRECTION ( 'NONE',  ( -1.000000000000000000, -1.224606353822377258E-16, -0.000000000000000000 ) ) ;
#78371=ADVANCED_FACE ( 'NONE', ( #76184 ), #54451, .T. ) ;
#78385=EDGE_LOOP ( 'NONE', ( #131251, #70472, #79107, #43262, #5667 ) ) ;
#78472=ORIENTED_EDGE ( 'NONE', *, *, #68580, .T. ) ;
#78512=CIRCLE ( 'NONE', #46141, 1.749999999999999778 ) ;
#78554=EDGE_CURVE ( 'NONE', #71583, #10019, #102495, .T. ) ;
#78570=ORIENTED_EDGE ( 'NONE', *, *, #139969, .T. ) ;
#78613=DIRECTION ( 'NONE',  ( 1.000000000000000000, 1.224606353822377258E-16, 0.000000000000000000 ) ) ;
#78695=EDGE_CURVE ( 'NONE', #16173, #36972, #77154, .T. ) ;
#78725=CYLINDRICAL_SURFACE ( 'NONE', #38778, 2.500000000000000444 ) ;
#78739=DIRECTION ( 'NONE',  ( -1.000000000000000000, -1.224606353822377258E-16, -0.000000000000000000 ) ) ;
#78755=CARTESIAN_POINT ( 'NONE',  ( -12.69999999999998153, 0.000000000000000000, 0.000000000000000000 ) ) ;
#78761=VECTOR ( 'NONE', #58948, 1000.000000000000000 ) ;
#78779=FACE_OUTER_BOUND ( 'NONE', #78783, .T. ) ;
#78783=EDGE_LOOP ( 'NONE', ( #45270, #129420, #62929, #65198, #72939, #18747 ) ) ;
#78813=DIRECTION ( 'NONE',  ( -1.000000000000000000, -0.000000000000000000, -0.000000000000000000 ) ) ;
#78817=DIRECTION ( 'NONE',  ( 0.000000000000000000, 0.000000000000000000, 1.000000000000000000 ) ) ;
#78892=CARTESIAN_POINT ( 'NONE',  ( -12.69999999999998153, 3.061616997868383634E-16, -2.500000000000000444 ) ) ;
#78903=DIRECTION ( 'NONE',  ( -1.000000000000000000, -1.224606353822377258E-16, -0.000000000000000000 ) ) ;
#78933=DIRECTION ( 'NONE',  ( 1.000000000000000000, 1.224606353822377258E-16, 0.000000000000000000 ) ) ;
#78957=DIRECTION ( 'NONE',  ( 0.000000000000000000, 0.000000000000000000, 1.000000000000000000 ) ) ;
#78972=AXIS2_PLACEMENT_3D ( 'NONE', #18629, #62910, #107087 ) ;
#78982=B_SPLINE_CURVE_WITH_KNOTS ( 'NONE', 3,
 ( #69921, #82907, #81497, #35860 ),
 .UNSPECIFIED., .F., .F.,
 ( 4, 4 ),
 ( 0.003913914403404828747, 0.004162342877716045109 ),
 .UNSPECIFIED. ) ;
#78984=DIRECTION ( 'NONE',  ( -1.000000000000000000, -0.000000000000000000, -0.000000000000000000 ) ) ;
#78997=VERTEX_POINT ( 'NONE', #25905 ) ;
#78998=DIRECTION ( 'NONE',  ( -1.000000000000000000, -1.224606353822377258E-16, -0.000000000000000000 ) ) ;
#78999=DIRECTION ( 'NONE',  ( -1.000000000000000000, -1.224606353822377258E-16, -0.000000000000000000 ) ) ;
#79038=DIRECTION ( 'NONE',  ( 2.110369192185896011E-16, -1.000000000000000000, 0.000000000000000000 ) ) ;
#79054=CARTESIAN_POINT ( 'NONE',  ( 11.72733514412567857, 3.821174125832445049E-16, 0.000000000000000000 ) ) ;
#79061=VECTOR ( 'NONE', #19037, 1000.000000000000000 ) ;
#79107=ORIENTED_EDGE ( 'NONE', *, *, #35662, .T. ) ;
#79111=AXIS2_PLACEMENT_3D ( 'NONE', #62430, #142828, #130541 ) ;
#79116=AXIS2_PLACEMENT_3D ( 'NONE', #2785, #47084, #91265 ) ;
#79154=ORIENTED_EDGE ( 'NONE', *, *, #132332, .F. ) ;
#79228=ORIENTED_EDGE ( 'NONE', *, *, #132332, .T. ) ;
#79241=DIRECTION ( 'NONE',  ( 1.055184596092948005E-16, -1.000000000000000000, 0.000000000000000000 ) ) ;
#79281=DIRECTION ( 'NONE',  ( 0.5735764363510448272, -0.8191520442889927978, 1.003171929053526103E-16 ) ) ;
#79315=CARTESIAN_POINT ( 'NONE',  ( 8.423184310185783730, 3.061616997868383634E-16, -2.500000000000000444 ) ) ;
#79316=ORIENTED_EDGE ( 'NONE', *, *, #42410, .T. ) ;
#79362=DIRECTION ( 'NONE',  ( -1.000000000000000000, -1.224606353822377258E-16, -0.000000000000000000 ) ) ;
#79368=CARTESIAN_POINT ( 'NONE',  ( 1.353980332882009252, -0.4000000000000004108, 2.467792535850613866 ) ) ;
#79373=DIRECTION ( 'NONE',  ( -1.000000000000000000, -0.000000000000000000, -0.000000000000000000 ) ) ;
#79426=CARTESIAN_POINT ( 'NONE',  ( 14.39532882439692862, -2.055000000000000160, 2.789133085058097101E-16 ) ) ;
#79482=EDGE_CURVE ( 'NONE', #66625, #9950, #79967, .T. ) ;
#79508=CARTESIAN_POINT ( 'NONE',  ( 19.10813147593277250, 4.202752102959690472E-16, 0.000000000000000000 ) ) ;
#79522=VECTOR ( 'NONE', #101441, 1000.000000000000000 ) ;
#79583=EDGE_CURVE ( 'NONE', #33411, #122222, #141645, .T. ) ;
#79596=CARTESIAN_POINT ( 'NONE',  ( -12.69999999999998153, 0.000000000000000000, 0.000000000000000000 ) ) ;
#79621=CIRCLE ( 'NONE', #35615, 2.500000000000000444 ) ;
#79653=ORIENTED_EDGE ( 'NONE', *, *, #130028, .F. ) ;
#79677=FACE_OUTER_BOUND ( 'NONE', #37050, .T. ) ;
#79678=DIRECTION ( 'NONE',  ( 0.000000000000000000, -1.000000000000000000, 0.000000000000000000 ) ) ;
#79680=VERTEX_POINT ( 'NONE', #133623 ) ;
#79687=ORIENTED_EDGE ( 'NONE', *, *, #29576, .F. ) ;
#79690=VERTEX_POINT ( 'NONE', #12533 ) ;
#79754=VERTEX_POINT ( 'NONE', #127549 ) ;
#79803=CIRCLE ( 'NONE', #21881, 2.500000000000000444 ) ;
#79856=EDGE_CURVE ( 'NONE', #14269, #117065, #123615, .T. ) ;
#79893=DIRECTION ( 'NONE',  ( 0.000000000000000000, -1.000000000000000000, 0.000000000000000000 ) ) ;
#79933=ADVANCED_FACE ( 'NONE', ( #44120 ), #137242, .T. ) ;
#79967=B_SPLINE_CURVE_WITH_KNOTS ( 'NONE', 3,
 ( #97380, #98138, #40897, #106846 ),
 .UNSPECIFIED., .F., .F.,
 ( 4, 4 ),
 ( 0.009196836153558695173, 0.009397116448368620506 ),
 .UNSPECIFIED. ) ;
#79971=ADVANCED_FACE ( 'NONE', ( #92586 ), #123119, .T. ) ;
#79984=CARTESIAN_POINT ( 'NONE',  ( 6.066782984417857350, -2.500000000000000000, 3.061616997868383634E-16 ) ) ;
#80100=CARTESIAN_POINT ( 'NONE',  ( 20.99065804761471199, 4.584330080086930965E-16, 0.000000000000000000 ) ) ;
#80101=ORIENTED_EDGE ( 'NONE', *, *, #27711, .F. ) ;
#80102=CARTESIAN_POINT ( 'NONE',  ( 11.25346039003969523, 2.055000000000001048, 2.516649172247811554E-16 ) ) ;
#80112=DIRECTION ( 'NONE',  ( 0.000000000000000000, -1.000000000000000000, 0.000000000000000000 ) ) ;
#80114=CIRCLE ( 'NONE', #17554, 2.055000000000000604 ) ;
#80135=VERTEX_POINT ( 'NONE', #27331 ) ;
#80186=EDGE_CURVE ( 'NONE', #141894, #140092, #49131, .T. ) ;
#80237=ORIENTED_EDGE ( 'NONE', *, *, #43304, .F. ) ;
#80256=DIRECTION ( 'NONE',  ( -1.000000000000000000, -1.224606353822377258E-16, -0.000000000000000000 ) ) ;
#80289=ORIENTED_EDGE ( 'NONE', *, *, #13381, .F. ) ;
#80384=DIRECTION ( 'NONE',  ( 0.000000000000000000, -1.000000000000000000, 0.000000000000000000 ) ) ;
#80388=LINE ( 'NONE', #81091, #5327 ) ;
#80430=VERTEX_POINT ( 'NONE', #56292 ) ;
#80546=DIRECTION ( 'NONE',  ( 0.000000000000000000, 0.000000000000000000, 1.000000000000000000 ) ) ;
#80687=ORIENTED_EDGE ( 'NONE', *, *, #15657, .T. ) ;
#80698=CIRCLE ( 'NONE', #101473, 2.055000000000000604 ) ;
#80708=FACE_OUTER_BOUND ( 'NONE', #23449, .T. ) ;
#80725=LINE ( 'NONE', #69868, #77332 ) ;
#80767=CARTESIAN_POINT ( 'NONE',  ( 17.84878961325748037, 4.584330080086930965E-16, 0.000000000000000000 ) ) ;
#80795=DIRECTION ( 'NONE',  ( 0.000000000000000000, 1.000000000000000000, 0.000000000000000000 ) ) ;
#80796=AXIS2_PLACEMENT_3D ( 'NONE', #34347, #26151, #80546 ) ;
#80867=EDGE_CURVE ( 'NONE', #102793, #43279, #105041, .T. ) ;
#80905=CIRCLE ( 'NONE', #64753, 2.500000000000000444 ) ;
#80945=ORIENTED_EDGE ( 'NONE', *, *, #29920, .F. ) ;
#80975=EDGE_CURVE ( 'NONE', #119393, #108094, #63385, .T. ) ;
#80982=CARTESIAN_POINT ( 'NONE',  ( 19.41972383043609440, 2.500000000000000444, 0.000000000000000000 ) ) ;
#81037=EDGE_CURVE ( 'NONE', #79690, #124291, #121286, .T. ) ;
#81043=ORIENTED_EDGE ( 'NONE', *, *, #8329, .T. ) ;
#81045=AXIS2_PLACEMENT_3D ( 'NONE', #90716, #56691, #32769 ) ;
#81076=ORIENTED_EDGE ( 'NONE', *, *, #115252, .T. ) ;
#81091=CARTESIAN_POINT ( 'NONE',  ( 16.75173015016484968, 2.055000000000001048, 2.516649172247811554E-16 ) ) ;
#81147=UNCERTAINTY_MEASURE_WITH_UNIT (LENGTH_MEASURE( 1.000000000000000082E-05 ), #13492, 'distance_accuracy_value', 'NONE');
#81151=EDGE_CURVE ( 'NONE', #83013, #101443, #120957, .T. ) ;
#81155=EDGE_CURVE ( 'NONE', #123895, #9541, #12619, .T. ) ;
#81156=DIRECTION ( 'NONE',  ( -1.000000000000000000, -1.224606353822377258E-16, -0.000000000000000000 ) ) ;
#81171=EDGE_LOOP ( 'NONE', ( #118613, #141248, #59727, #96978, #170 ) ) ;
#81224=CIRCLE ( 'NONE', #22, 2.055000000000000604 ) ;
#81278=LINE ( 'NONE', #134957, #93443 ) ;
#81422=DIRECTION ( 'NONE',  ( -1.000000000000000000, -0.000000000000000000, -0.000000000000000000 ) ) ;
#81485=CARTESIAN_POINT ( 'NONE',  ( 9.370933818357753964, -2.499999999999999112, 0.000000000000000000 ) ) ;
#81486=EDGE_CURVE ( 'NONE', #90821, #51507, #56569, .T. ) ;
#81497=CARTESIAN_POINT ( 'NONE',  ( 0.2100385686636480065, -0.3999999999999998002, -2.083955130345452211 ) ) ;
#81601=ORIENTED_EDGE ( 'NONE', *, *, #140222, .F. ) ;
#81609=AXIS2_PLACEMENT_3D ( 'NONE', #73617, #19926, #81850 ) ;
#81616=DIRECTION ( 'NONE',  ( -1.000000000000000000, -0.000000000000000000, -0.000000000000000000 ) ) ;
#81623=AXIS2_PLACEMENT_3D ( 'NONE', #139495, #84388, #86517 ) ;
#81630=ORIENTED_EDGE ( 'NONE', *, *, #117441, .F. ) ;
#81653=EDGE_CURVE ( 'NONE', #13056, #140226, #86648, .T. ) ;
#81673=DIRECTION ( 'NONE',  ( -0.5735764363510499342, -0.8191520442889891340, 0.000000000000000000 ) ) ;
#81711=DIRECTION ( 'NONE',  ( -1.000000000000000000, -1.224606353822377258E-16, -0.000000000000000000 ) ) ;
#81747=DIRECTION ( 'NONE',  ( -1.000000000000000000, -1.224606353822377258E-16, -0.000000000000000000 ) ) ;
#81850=DIRECTION ( 'NONE',  ( 0.000000000000000000, -1.000000000000000000, 0.000000000000000000 ) ) ;
#81893=CARTESIAN_POINT ( 'NONE',  ( 20.36747333860806819, -2.499999999999996447, 0.000000000000000000 ) ) ;
#81902=DIRECTION ( 'NONE',  ( -1.000000000000000000, -1.224606353822377258E-16, -0.000000000000000000 ) ) ;
#81982=ORIENTED_EDGE ( 'NONE', *, *, #60749, .T. ) ;
#81985=CIRCLE ( 'NONE', #105122, 2.500000000000000444 ) ;
#82013=CARTESIAN_POINT ( 'NONE',  ( 8.111591955682463606, 4.202752102959690472E-16, 0.000000000000000000 ) ) ;
#82068=DIRECTION ( 'NONE',  ( 0.5735764363510444941, 0.8191520442889929088, 0.000000000000000000 ) ) ;
#82115=EDGE_CURVE ( 'NONE', #141895, #5194, #125100, .T. ) ;
#82120=DIRECTION ( 'NONE',  ( -1.000000000000000000, -0.000000000000000000, -0.000000000000000000 ) ) ;
#82131=ORIENTED_EDGE ( 'NONE', *, *, #25530, .T. ) ;
#82139=CIRCLE ( 'NONE', #89058, 2.055000000000000604 ) ;
#82192=ORIENTED_EDGE ( 'NONE', *, *, #27489, .F. ) ;
#82210=VERTEX_POINT ( 'NONE', #23523 ) ;
#82227=ORIENTED_EDGE ( 'NONE', *, *, #11221, .T. ) ;
#82243=EDGE_LOOP ( 'NONE', ( #52333, #13177, #136313, #60428, #123603 ) ) ;
#82321=DIRECTION ( 'NONE',  ( 0.000000000000000000, -1.000000000000000000, 0.000000000000000000 ) ) ;
#82329=CARTESIAN_POINT ( 'NONE',  ( 1.629999999999999893, 4.202752102959690472E-16, -4.330509084666861676E-16 ) ) ;
#82338=ADVANCED_FACE ( 'NONE', ( #127109 ), #76604, .T. ) ;
#82372=CARTESIAN_POINT ( 'NONE',  ( 9.682526172861077640, 4.202752102959690472E-16, 0.000000000000000000 ) ) ;
#82429=CARTESIAN_POINT ( 'NONE',  ( 5.755190629914537226, 4.202752102959690472E-16, 0.000000000000000000 ) ) ;
#82430=DIRECTION ( 'NONE',  ( -1.000000000000000000, -1.224606353822377258E-16, -0.000000000000000000 ) ) ;
#82441=ORIENTED_EDGE ( 'NONE', *, *, #28788, .F. ) ;
#82450=ORIENTED_EDGE ( 'NONE', *, *, #130588, .T. ) ;
#82468=CARTESIAN_POINT ( 'NONE',  ( 12.03892749862900402, 4.202752102959690472E-16, 0.000000000000000000 ) ) ;
#82486=EDGE_LOOP ( 'NONE', ( #87146, #7633, #66094, #122991, #128867 ) ) ;
#82507=EDGE_CURVE ( 'NONE', #114653, #38444, #96591, .T. ) ;
#82511=VERTEX_POINT ( 'NONE', #3019 ) ;
#82523=ORIENTED_EDGE ( 'NONE', *, *, #41510, .T. ) ;
#82550=ORIENTED_EDGE ( 'NONE', *, *, #91892, .T. ) ;
#82553=VERTEX_POINT ( 'NONE', #13875 ) ;
#82570=CARTESIAN_POINT ( 'NONE',  ( 6.229065384000522343, 2.500000000000001776, 3.061616997868385113E-16 ) ) ;
#82793=ORIENTED_EDGE ( 'NONE', *, *, #11221, .F. ) ;
#82814=CYLINDRICAL_SURFACE ( 'NONE', #132147, 2.500000000000000444 ) ;
#82820=CARTESIAN_POINT ( 'NONE',  ( 9.370933818357753964, 3.821174125832445049E-16, 0.000000000000000000 ) ) ;
#82861=VECTOR ( 'NONE', #24810, 999.9999999999998863 ) ;
#82874=ORIENTED_EDGE ( 'NONE', *, *, #59307, .T. ) ;
#82889=FACE_OUTER_BOUND ( 'NONE', #136708, .T. ) ;
#82904=ORIENTED_EDGE ( 'NONE', *, *, #127289, .T. ) ;
#82907=CARTESIAN_POINT ( 'NONE',  ( 0.1630955763144141257, -0.3999999999999998002, -2.152173649344992334 ) ) ;
#82909=FACE_OUTER_BOUND ( 'NONE', #104624, .T. ) ;
#82930=ORIENTED_EDGE ( 'NONE', *, *, #97143, .T. ) ;
#82932=ORIENTED_EDGE ( 'NONE', *, *, #9532, .T. ) ;
#82983=ORIENTED_EDGE ( 'NONE', *, *, #131432, .T. ) ;
#82985=DIRECTION ( 'NONE',  ( -1.000000000000000000, -1.224606353822377258E-16, -0.000000000000000000 ) ) ;
#82989=VERTEX_POINT ( 'NONE', #697 ) ;
#83013=VERTEX_POINT ( 'NONE', #96789 ) ;
#83044=ORIENTED_EDGE ( 'NONE', *, *, #24785, .T. ) ;
#83073=CONICAL_SURFACE ( 'NONE', #73752, 2.055000000000000604, 0.9599310885968764806 ) ;
#83157=LINE ( 'NONE', #7711, #102371 ) ;
#83173=EDGE_CURVE ( 'NONE', #92014, #118128, #16195, .T. ) ;
#83191=CARTESIAN_POINT ( 'NONE',  ( 10.46799328145038821, 4.202752102959690472E-16, 0.000000000000000000 ) ) ;
#83199=CONICAL_SURFACE ( 'NONE', #108610, 2.500000000000000444, 0.9599310885968830309 ) ;
#83234=FACE_OUTER_BOUND ( 'NONE', #63371, .T. ) ;
#83256=DIRECTION ( 'NONE',  ( -1.000000000000000000, -1.224606353822377258E-16, -0.000000000000000000 ) ) ;
#83288=AXIS2_PLACEMENT_3D ( 'NONE', #108748, #31943, #140686 ) ;
#83311=CARTESIAN_POINT ( 'NONE',  ( 10.15640092694706453, 3.821174125832445049E-16, 0.000000000000000000 ) ) ;
#83315=CARTESIAN_POINT ( 'NONE',  ( -12.69999999999998153, 0.000000000000000000, 2.500000000000000444 ) ) ;
#83320=CARTESIAN_POINT ( 'NONE',  ( 20.20519093902540320, -2.500000000000000000, 3.061616997868383634E-16 ) ) ;
#83358=B_SPLINE_CURVE_WITH_KNOTS ( 'NONE', 3,
 ( #122742, #45924, #90859, #100987 ),
 .UNSPECIFIED., .F., .F.,
 ( 4, 4 ),
 ( 0.003609336753060590330, 0.003809496093231038664 ),
 .UNSPECIFIED. ) ;
#83369=AXIS2_PLACEMENT_3D ( 'NONE', #57248, #78999, #89829 ) ;
#83370=CARTESIAN_POINT ( 'NONE',  ( 14.08373646989360317, 2.500000000000003109, 3.061616997868386592E-16 ) ) ;
#83433=ORIENTED_EDGE ( 'NONE', *, *, #133355, .T. ) ;
#83477=EDGE_CURVE ( 'NONE', #67994, #59910, #60235, .T. ) ;
#83522=VERTEX_POINT ( 'NONE', #116975 ) ;
#83582=CARTESIAN_POINT ( 'NONE',  ( -12.69999999999998153, 0.000000000000000000, 0.000000000000000000 ) ) ;
#83588=VECTOR ( 'NONE', #63504, 1000.000000000000000 ) ;
#83589=VERTEX_POINT ( 'NONE', #53901 ) ;
#83594=CIRCLE ( 'NONE', #106614, 2.500000000000000444 ) ;
#83608=LINE ( 'NONE', #114063, #17103 ) ;
#83617=CARTESIAN_POINT ( 'NONE',  ( 1.042387978378689573, -0.4000000000000003553, 2.015694669338588429 ) ) ;
#83621=ADVANCED_FACE ( 'NONE', ( #108206 ), #64751, .T. ) ;
#83635=VECTOR ( 'NONE', #39253, 1000.000000000000000 ) ;
#83645=CARTESIAN_POINT ( 'NONE',  ( 12.35051985313232237, 2.500000000000000444, 0.000000000000000000 ) ) ;
#83655=DIRECTION ( 'NONE',  ( -1.000000000000000000, -1.224606353822377258E-16, -0.000000000000000000 ) ) ;
#83700=DIRECTION ( 'NONE',  ( 0.000000000000000000, -1.000000000000000000, 0.000000000000000000 ) ) ;
#83707=LINE ( 'NONE', #94523, #141880 ) ;
#83712=EDGE_CURVE ( 'NONE', #93815, #101443, #115844, .T. ) ;
#83836=AXIS2_PLACEMENT_3D ( 'NONE', #101877, #12719, #103291 ) ;
#83873=EDGE_CURVE ( 'NONE', #74043, #57414, #48745, .T. ) ;
#83905=AXIS2_PLACEMENT_3D ( 'NONE', #35119, #79362, #101768 ) ;
#83984=CONICAL_SURFACE ( 'NONE', #132627, 2.055000000000000604, 0.9599310885968764806 ) ;
#84085=VERTEX_POINT ( 'NONE', #118950 ) ;
#84093=EDGE_CURVE ( 'NONE', #18713, #133133, #135562, .T. ) ;
#84125=DIRECTION ( 'NONE',  ( 0.5735764363510448272, -0.8191520442889927978, 1.003171929053526103E-16 ) ) ;
#84139=ORIENTED_EDGE ( 'NONE', *, *, #139969, .F. ) ;
#84144=ORIENTED_EDGE ( 'NONE', *, *, #100503, .T. ) ;
#84185=DIRECTION ( 'NONE',  ( -0.5735764363510499342, -0.8191520442889891340, 0.000000000000000000 ) ) ;
#84308=FACE_OUTER_BOUND ( 'NONE', #110187, .T. ) ;
#84315=DIRECTION ( 'NONE',  ( 0.5735764363510448272, -0.8191520442889927978, 1.003171929053526103E-16 ) ) ;
#84356=ORIENTED_EDGE ( 'NONE', *, *, #12057, .T. ) ;
#84383=EDGE_CURVE ( 'NONE', #104716, #13272, #24535, .T. ) ;
#84386=ORIENTED_EDGE ( 'NONE', *, *, #51529, .T. ) ;
#84388=DIRECTION ( 'NONE',  ( 0.000000000000000000, 1.000000000000000000, 1.301042606982605074E-16 ) ) ;
#84418=ORIENTED_EDGE ( 'NONE', *, *, #83873, .F. ) ;
#84443=ORIENTED_EDGE ( 'NONE', *, *, #67139, .F. ) ;
#84488=EDGE_CURVE ( 'NONE', #48215, #112363, #2543, .T. ) ;
#84547=LINE ( 'NONE', #14964, #111145 ) ;
#84562=DIRECTION ( 'NONE',  ( 0.000000000000000000, -1.000000000000000000, 0.000000000000000000 ) ) ;
#84579=DIRECTION ( 'NONE',  ( 0.000000000000000000, -1.000000000000000000, 0.000000000000000000 ) ) ;
#84591=DIRECTION ( 'NONE',  ( -1.000000000000000000, -0.000000000000000000, -0.000000000000000000 ) ) ;
#84599=DIRECTION ( 'NONE',  ( -1.000000000000000000, -0.000000000000000000, -0.000000000000000000 ) ) ;
#84628=CARTESIAN_POINT ( 'NONE',  ( 0.03865102804815064713, -0.4000000000000003553, 2.083945628037807030 ) ) ;
#84629=VERTEX_POINT ( 'NONE', #11311 ) ;
#84630=CARTESIAN_POINT ( 'NONE',  ( 3.398789304146613510, 2.055000000000001048, 0.000000000000000000 ) ) ;
#84662=ADVANCED_FACE ( 'NONE', ( #5969 ), #123710, .T. ) ;
#84677=CARTESIAN_POINT ( 'NONE',  ( 17.84878961325748037, -2.500000000000000444, 3.061616997868384127E-16 ) ) ;
#84682=DIRECTION ( 'NONE',  ( 0.000000000000000000, -1.000000000000000000, 0.000000000000000000 ) ) ;
#84785=CIRCLE ( 'NONE', #57083, 2.500000000000000444 ) ;
#84814=DIRECTION ( 'NONE',  ( -1.000000000000000000, -1.224606353822377258E-16, -0.000000000000000000 ) ) ;
#84881=DIRECTION ( 'NONE',  ( -1.301042606982605074E-16, 1.000000000000000000, 0.000000000000000000 ) ) ;
#84885=ORIENTED_EDGE ( 'NONE', *, *, #61737, .T. ) ;
#84891=FACE_OUTER_BOUND ( 'NONE', #130869, .T. ) ;
#84893=CARTESIAN_POINT ( 'NONE',  ( 15.18079593298623564, 4.202752102959690472E-16, 0.000000000000000000 ) ) ;
#84907=CIRCLE ( 'NONE', #75707, 2.500000000000000444 ) ;
#84926=ORIENTED_EDGE ( 'NONE', *, *, #30094, .T. ) ;
#84966=CARTESIAN_POINT ( 'NONE',  ( 16.75173015016484968, -2.055000000000000160, 0.000000000000000000 ) ) ;
#85005=CARTESIAN_POINT ( 'NONE',  ( -12.69999999999998153, -0.4000000000000004108, 2.467792535850613866 ) ) ;
#85022=DIRECTION ( 'NONE',  ( -1.000000000000000000, -1.224606353822377258E-16, -0.000000000000000000 ) ) ;
#85075=EDGE_LOOP ( 'NONE', ( #15888, #128090, #48493, #134400, #136804, #70630 ) ) ;
#85097=EDGE_CURVE ( 'NONE', #8017, #139436, #104596, .T. ) ;
#85098=CARTESIAN_POINT ( 'NONE',  ( 1.629999999999999893, 0.3999999999999995226, 2.303088455023526215 ) ) ;
#85100=EDGE_LOOP ( 'NONE', ( #65900, #19919, #115296, #71650, #98515 ) ) ;
#85143=CARTESIAN_POINT ( 'NONE',  ( 18.01107201284014536, 2.499999999999998224, 3.061616997868380183E-16 ) ) ;
#85170=ORIENTED_EDGE ( 'NONE', *, *, #68662, .T. ) ;
#85214=EDGE_LOOP ( 'NONE', ( #74965, #101048, #142522, #84356, #133869 ) ) ;
#85215=DIRECTION ( 'NONE',  ( 0.000000000000000000, -1.000000000000000000, 0.000000000000000000 ) ) ;
#85219=DIRECTION ( 'NONE',  ( -0.5735764363510499342, -0.8191520442889891340, 0.000000000000000000 ) ) ;
#85243=EDGE_LOOP ( 'NONE', ( #19225, #135096, #34910, #41966, #103616, #88477 ) ) ;
#85258=DIRECTION ( 'NONE',  ( 0.000000000000000000, -1.000000000000000000, 0.000000000000000000 ) ) ;
#85265=B_SPLINE_CURVE_WITH_KNOTS ( 'NONE', 3,
 ( #123611, #24265, #68512, #88100 ),
 .UNSPECIFIED., .F., .F.,
 ( 4, 4 ),
 ( 0.003615568590623256025, 0.004164643302645746128 ),
 .UNSPECIFIED. ) ;
#85306=CIRCLE ( 'NONE', #22783, 2.500000000000000444 ) ;
#85344=ORIENTED_EDGE ( 'NONE', *, *, #35578, .F. ) ;
#85358=ADVANCED_FACE ( 'NONE', ( #110821 ), #99235, .T. ) ;
#85367=DIRECTION ( 'NONE',  ( -1.000000000000000000, -1.224606353822377258E-16, -0.000000000000000000 ) ) ;
#85378=DIRECTION ( 'NONE',  ( -1.000000000000000000, -1.224606353822377258E-16, -0.000000000000000000 ) ) ;
#85404=ORIENTED_EDGE ( 'NONE', *, *, #136043, .F. ) ;
#85417=LINE ( 'NONE', #143385, #92776 ) ;
#85432=ORIENTED_EDGE ( 'NONE', *, *, #121301, .F. ) ;
#85439=CARTESIAN_POINT ( 'NONE',  ( 5.281315875828549444, 3.061616997868382648E-16, -2.500000000000000444 ) ) ;
#85442=ORIENTED_EDGE ( 'NONE', *, *, #126407, .T. ) ;
#85494=DIRECTION ( 'NONE',  ( 0.000000000000000000, -1.000000000000000000, 0.000000000000000000 ) ) ;
#85523=AXIS2_PLACEMENT_3D ( 'NONE', #80767, #78613, #124957 ) ;
#85544=DIRECTION ( 'NONE',  ( -1.000000000000000000, -1.224606353822377258E-16, -0.000000000000000000 ) ) ;
#85604=EDGE_CURVE ( 'NONE', #98637, #764, #88479, .T. ) ;
#85618=ORIENTED_EDGE ( 'NONE', *, *, #5537, .T. ) ;
#85634=DIRECTION ( 'NONE',  ( -1.000000000000000000, -0.000000000000000000, -0.000000000000000000 ) ) ;
#85659=VECTOR ( 'NONE', #102048, 1000.000000000000000 ) ;
#85729=AXIS2_PLACEMENT_3D ( 'NONE', #126296, #39305, #47371 ) ;
#85734=ORIENTED_EDGE ( 'NONE', *, *, #118294, .T. ) ;
#85756=CARTESIAN_POINT ( 'NONE',  ( 19.10813147593277250, -2.055000000000000160, 2.789133085058097101E-16 ) ) ;
#85758=ORIENTED_EDGE ( 'NONE', *, *, #73012, .F. ) ;
#85797=DIRECTION ( 'NONE',  ( 0.000000000000000000, 0.000000000000000000, 1.000000000000000000 ) ) ;
#85812=CARTESIAN_POINT ( 'NONE',  ( 15.96626304157554266, 2.055000000000001048, 2.516649172247811554E-16 ) ) ;
#85822=EDGE_LOOP ( 'NONE', ( #55934, #111538, #47720, #99450, #54532, #77003 ) ) ;
#85862=AXIS2_PLACEMENT_3D ( 'NONE', #75666, #32153, #43740 ) ;
#85898=EDGE_CURVE ( 'NONE', #18445, #42023, #134856, .T. ) ;
#85900=ORIENTED_EDGE ( 'NONE', *, *, #71106, .F. ) ;
#85926=EDGE_LOOP ( 'NONE', ( #67322, #28135, #47818, #56076, #102996, #112516 ) ) ;
#85951=LINE ( 'NONE', #29415, #4369 ) ;
#85980=CARTESIAN_POINT ( 'NONE',  ( 9.682526172861077640, -2.055000000000000160, 0.000000000000000000 ) ) ;
#85994=CARTESIAN_POINT ( 'NONE',  ( 10.46799328145038821, 4.202752102959690472E-16, 0.000000000000000000 ) ) ;
#85995=ORIENTED_EDGE ( 'NONE', *, *, #60532, .F. ) ;
#86008=CARTESIAN_POINT ( 'NONE',  ( -12.69999999999998153, 0.3999999999999995226, 2.467792535850613866 ) ) ;
#86025=VECTOR ( 'NONE', #101123, 999.9999999999998863 ) ;
#86043=DIRECTION ( 'NONE',  ( 0.000000000000000000, -1.000000000000000000, 0.000000000000000000 ) ) ;
#86044=DIRECTION ( 'NONE',  ( 1.734723475976806848E-16, -1.000000000000000000, 0.000000000000000000 ) ) ;
#86050=AXIS2_PLACEMENT_3D ( 'NONE', #127363, #61448, #28063 ) ;
#86072=EDGE_CURVE ( 'NONE', #45062, #2478, #77000, .T. ) ;
#86095=ORIENTED_EDGE ( 'NONE', *, *, #13381, .T. ) ;
#86096=CIRCLE ( 'NONE', #23586, 1.749999999999999778 ) ;
#86117=VERTEX_POINT ( 'NONE', #94627 ) ;
#86152=AXIS2_PLACEMENT_3D ( 'NONE', #87109, #119695, #41447 ) ;
#86220=CARTESIAN_POINT ( 'NONE',  ( 7.799999601179139042, -2.500000000000000444, 0.000000000000000000 ) ) ;
#86222=DIRECTION ( 'NONE',  ( -1.000000000000000000, -1.224606353822377258E-16, -0.000000000000000000 ) ) ;
#86225=VECTOR ( 'NONE', #42087, 1000.000000000000000 ) ;
#86230=ORIENTED_EDGE ( 'NONE', *, *, #31670, .F. ) ;
#86240=EDGE_LOOP ( 'NONE', ( #111483, #101566, #15897, #29705, #58404 ) ) ;
#86247=CARTESIAN_POINT ( 'NONE',  ( 17.84878961325748037, 4.584330080086930965E-16, 0.000000000000000000 ) ) ;
#86265=AXIS2_PLACEMENT_3D ( 'NONE', #113404, #125006, #80112 ) ;
#86269=EDGE_CURVE ( 'NONE', #13745, #78997, #5332, .T. ) ;
#86274=ORIENTED_EDGE ( 'NONE', *, *, #19290, .T. ) ;
#86279=CIRCLE ( 'NONE', #40050, 2.500000000000000444 ) ;
#86312=CARTESIAN_POINT ( 'NONE',  ( 25.00000000000000000, 0.000000000000000000, 0.000000000000000000 ) ) ;
#86457=EDGE_CURVE ( 'NONE', #103754, #73407, #12623, .T. ) ;
#86470=DIRECTION ( 'NONE',  ( -0.5735764363510499342, -0.8191520442889891340, 0.000000000000000000 ) ) ;
#86482=DIRECTION ( 'NONE',  ( 1.000000000000000000, 0.000000000000000000, 0.000000000000000000 ) ) ;
#86505=CARTESIAN_POINT ( 'NONE',  ( 20.20519093902540320, 4.584330080086930965E-16, 0.000000000000000000 ) ) ;
#86517=DIRECTION ( 'NONE',  ( 0.000000000000000000, -1.301042606982605074E-16, 1.000000000000000000 ) ) ;
#86557=EDGE_CURVE ( 'NONE', #20222, #57263, #38676, .T. ) ;
#86560=DIRECTION ( 'NONE',  ( 0.000000000000000000, -1.000000000000000000, 0.000000000000000000 ) ) ;
#86572=ADVANCED_FACE ( 'NONE', ( #93768 ), #67909, .T. ) ;
#86592=VECTOR ( 'NONE', #24107, 1000.000000000000000 ) ;
#86616=ORIENTED_EDGE ( 'NONE', *, *, #24406, .F. ) ;
#86648=CIRCLE ( 'NONE', #70431, 2.055000000000000604 ) ;
#86651=LINE ( 'NONE', #43141, #777 ) ;
#86694=DIRECTION ( 'NONE',  ( 0.000000000000000000, 0.000000000000000000, 1.000000000000000000 ) ) ;
#86734=CARTESIAN_POINT ( 'NONE',  ( -12.69999999999998153, 0.000000000000000000, 0.000000000000000000 ) ) ;
#86792=CARTESIAN_POINT ( 'NONE',  ( 2.301729841053981929, -2.500000000000000444, 0.000000000000000000 ) ) ;
#86829=CARTESIAN_POINT ( 'NONE',  ( 0.2100385299584287269, -0.4000000000000003553, 2.083955186700111373 ) ) ;
#86879=CARTESIAN_POINT ( 'NONE',  ( 18.63425672184678916, 0.000000000000000000, 2.500000000000000444 ) ) ;
#86996=DIRECTION ( 'NONE',  ( 1.055184596092948005E-16, -1.000000000000000000, 0.000000000000000000 ) ) ;
#86999=EDGE_CURVE ( 'NONE', #38008, #57414, #61868, .T. ) ;
#87033=VERTEX_POINT ( 'NONE', #81485 ) ;
#87070=ADVANCED_FACE ( 'NONE', ( #9570 ), #31031, .T. ) ;
#87109=CARTESIAN_POINT ( 'NONE',  ( 0.5685132242927012358, 4.584330080086930965E-16, 0.000000000000000000 ) ) ;
#87146=ORIENTED_EDGE ( 'NONE', *, *, #81486, .T. ) ;
#87169=CARTESIAN_POINT ( 'NONE',  ( 6.229065384000522343, -2.500000000000000444, 0.000000000000000000 ) ) ;
#87197=ORIENTED_EDGE ( 'NONE', *, *, #55482, .F. ) ;
#87199=EDGE_CURVE ( 'NONE', #75992, #52878, #51833, .T. ) ;
#87201=AXIS2_PLACEMENT_3D ( 'NONE', #25767, #23630, #135963 ) ;
#87217=DIRECTION ( 'NONE',  ( 0.5735764363510448272, -0.8191520442889927978, 1.003171929053526103E-16 ) ) ;
#87222=LINE ( 'NONE', #65503, #1769 ) ;
#87259=VECTOR ( 'NONE', #127181, 999.9999999999998863 ) ;
#87330=DIRECTION ( 'NONE',  ( -0.5735764363510499342, -0.8191520442889891340, 0.000000000000000000 ) ) ;
#87356=ORIENTED_EDGE ( 'NONE', *, *, #11999, .F. ) ;
#87362=ORIENTED_EDGE ( 'NONE', *, *, #85097, .T. ) ;
#87371=ADVANCED_FACE ( 'NONE', ( #134248 ), #134984, .T. ) ;
#87390=ORIENTED_EDGE ( 'NONE', *, *, #68662, .F. ) ;
#87411=DIRECTION ( 'NONE',  ( -1.000000000000000000, -1.224606353822377258E-16, -0.000000000000000000 ) ) ;
#87438=ORIENTED_EDGE ( 'NONE', *, *, #27291, .T. ) ;
#87447=AXIS2_PLACEMENT_3D ( 'NONE', #36100, #141455, #2719 ) ;
#87456=CARTESIAN_POINT ( 'NONE',  ( 1.249915201643648111, -0.3999999999999997446, -2.317232462839658780 ) ) ;
#87500=DIRECTION ( 'NONE',  ( 0.000000000000000000, -1.000000000000000000, 0.000000000000000000 ) ) ;
#87505=ORIENTED_EDGE ( 'NONE', *, *, #137949, .F. ) ;
#87508=ORIENTED_EDGE ( 'NONE', *, *, #25530, .F. ) ;
#87540=ORIENTED_EDGE ( 'NONE', *, *, #138891, .T. ) ;
#87541=DIRECTION ( 'NONE',  ( -1.000000000000000000, -1.224606353822377258E-16, -0.000000000000000000 ) ) ;
#87564=CARTESIAN_POINT ( 'NONE',  ( 11.72733514412567857, 2.500000000000003109, 3.061616997868386592E-16 ) ) ;
#87611=CIRCLE ( 'NONE', #59887, 2.500000000000000444 ) ;
#87644=DIRECTION ( 'NONE',  ( -1.000000000000000000, -1.224606353822377258E-16, -0.000000000000000000 ) ) ;
#87751=FACE_OUTER_BOUND ( 'NONE', #132061, .T. ) ;
#87755=AXIS2_PLACEMENT_3D ( 'NONE', #130186, #119273, #19963 ) ;
#87767=FACE_OUTER_BOUND ( 'NONE', #102541, .T. ) ;
#87794=ORIENTED_EDGE ( 'NONE', *, *, #9105, .F. ) ;
#87797=VERTEX_POINT ( 'NONE', #4186 ) ;
#87889=ORIENTED_EDGE ( 'NONE', *, *, #103725, .T. ) ;
#87893=DIRECTION ( 'NONE',  ( -1.000000000000000000, -0.000000000000000000, -0.000000000000000000 ) ) ;
#87896=EDGE_CURVE ( 'NONE', #104418, #75992, #112136, .T. ) ;
#87910=AXIS2_PLACEMENT_3D ( 'NONE', #45109, #111756, #12422 ) ;
#87912=AXIS2_PLACEMENT_3D ( 'NONE', #46661, #101691, #58251 ) ;
#87916=AXIS2_PLACEMENT_3D ( 'NONE', #63447, #62007, #259 ) ;
#87951=AXIS2_PLACEMENT_3D ( 'NONE', #96822, #141067, #122901 ) ;
#88032=AXIS2_PLACEMENT_3D ( 'NONE', #107702, #18528, #131623 ) ;
#88050=VECTOR ( 'NONE', #106838, 1000.000000000000000 ) ;
#88091=DIRECTION ( 'NONE',  ( 0.000000000000000000, -1.000000000000000000, 0.000000000000000000 ) ) ;
#88100=CARTESIAN_POINT ( 'NONE',  ( 1.042387978378689350, 0.4000000000000001332, -2.015694669338588429 ) ) ;
#88115=DIRECTION ( 'NONE',  ( -1.000000000000000000, -1.224606353822377258E-16, -0.000000000000000000 ) ) ;
#88156=DIRECTION ( 'NONE',  ( -1.000000000000000000, -1.224606353822377258E-16, -0.000000000000000000 ) ) ;
#88270=ORIENTED_EDGE ( 'NONE', *, *, #94131, .F. ) ;
#88271=CARTESIAN_POINT ( 'NONE',  ( 18.63425672184678916, 4.584330080086930965E-16, 0.000000000000000000 ) ) ;
#88331=FACE_OUTER_BOUND ( 'NONE', #112518, .T. ) ;
#88338=VECTOR ( 'NONE', #84315, 999.9999999999998863 ) ;
#88360=ORIENTED_EDGE ( 'NONE', *, *, #40272, .F. ) ;
#88367=EDGE_CURVE ( 'NONE', #36502, #50807, #112258, .T. ) ;
#88383=ORIENTED_EDGE ( 'NONE', *, *, #97915, .T. ) ;
#88394=FACE_OUTER_BOUND ( 'NONE', #134360, .T. ) ;
#88408=EDGE_CURVE ( 'NONE', #59855, #133129, #128407, .T. ) ;
#88421=LINE ( 'NONE', #109432, #76523 ) ;
#88477=ORIENTED_EDGE ( 'NONE', *, *, #64009, .F. ) ;
#88479=CIRCLE ( 'NONE', #25955, 2.500000000000000444 ) ;
#88494=CARTESIAN_POINT ( 'NONE',  ( 5.755190629914537226, 4.202752102959690472E-16, 0.000000000000000000 ) ) ;
#88508=AXIS2_PLACEMENT_3D ( 'NONE', #1236, #44824, #22267 ) ;
#88534=CONICAL_SURFACE ( 'NONE', #111698, 2.500000000000000444, 0.9599310885968830309 ) ;
#88639=DIRECTION ( 'NONE',  ( -1.000000000000000000, -1.224606353822377258E-16, -0.000000000000000000 ) ) ;
#88647=CIRCLE ( 'NONE', #646, 2.500000000000000444 ) ;
#88673=ORIENTED_EDGE ( 'NONE', *, *, #48969, .F. ) ;
#88683=VECTOR ( 'NONE', #61875, 1000.000000000000000 ) ;
#88708=DIRECTION ( 'NONE',  ( 0.000000000000000000, -1.000000000000000000, 0.000000000000000000 ) ) ;
#88731=AXIS2_PLACEMENT_3D ( 'NONE', #49983, #107189, #138406 ) ;
#88753=ORIENTED_EDGE ( 'NONE', *, *, #85097, .F. ) ;
#88761=VERTEX_POINT ( 'NONE', #139991 ) ;
#88783=VERTEX_POINT ( 'NONE', #52237 ) ;
#88798=EDGE_LOOP ( 'NONE', ( #105581, #7489, #12261, #91959, #39556 ) ) ;
#88892=ORIENTED_EDGE ( 'NONE', *, *, #51443, .T. ) ;
#88922=DIRECTION ( 'NONE',  ( 1.000000000000000000, 1.224606353822377258E-16, 0.000000000000000000 ) ) ;
#88945=B_SPLINE_CURVE_WITH_KNOTS ( 'NONE', 3,
 ( #64756, #111838, #99491, #32864 ),
 .UNSPECIFIED., .F., .F.,
 ( 4, 4 ),
 ( 0.008853860144884172223, 0.009403245473020183098 ),
 .UNSPECIFIED. ) ;
#88970=CARTESIAN_POINT ( 'NONE',  ( 19.41972383043609440, 4.584330080086930965E-16, 0.000000000000000000 ) ) ;
#88974=CIRCLE ( 'NONE', #38368, 2.500000000000000444 ) ;
#88990=EDGE_LOOP ( 'NONE', ( #132891, #143178, #68897, #10415 ) ) ;
#89002=CARTESIAN_POINT ( 'NONE',  ( 0.1161069444170876597, 0.000000000000000000, 0.000000000000000000 ) ) ;
#89015=EDGE_CURVE ( 'NONE', #47310, #89141, #3532, .T. ) ;
#89032=ORIENTED_EDGE ( 'NONE', *, *, #24236, .F. ) ;
#89041=ORIENTED_EDGE ( 'NONE', *, *, #131390, .F. ) ;
#89042=DIRECTION ( 'NONE',  ( -1.000000000000000000, -1.224606353822377258E-16, -0.000000000000000000 ) ) ;
#89058=AXIS2_PLACEMENT_3D ( 'NONE', #34719, #123165, #25249 ) ;
#89069=CIRCLE ( 'NONE', #139689, 2.500000000000000444 ) ;
#89101=ORIENTED_EDGE ( 'NONE', *, *, #110101, .F. ) ;
#89105=CYLINDRICAL_SURFACE ( 'NONE', #92291, 2.500000000000000444 ) ;
#89141=VERTEX_POINT ( 'NONE', #128907 ) ;
#89202=CARTESIAN_POINT ( 'NONE',  ( -12.69999999999998153, 0.000000000000000000, 2.500000000000000444 ) ) ;
#89206=CARTESIAN_POINT ( 'NONE',  ( -12.69999999999998153, 0.3999999999999995226, 2.467792535850613866 ) ) ;
#89233=ORIENTED_EDGE ( 'NONE', *, *, #30767, .T. ) ;
#89281=ORIENTED_EDGE ( 'NONE', *, *, #58443, .F. ) ;
#89287=CARTESIAN_POINT ( 'NONE',  ( 20.36747333860806819, 3.821174125832445049E-16, 0.000000000000000000 ) ) ;
#89296=ADVANCED_FACE ( 'NONE', ( #77431 ), #63834, .T. ) ;
#89319=ORIENTED_EDGE ( 'NONE', *, *, #12683, .T. ) ;
#89361=AXIS2_PLACEMENT_3D ( 'NONE', #103627, #28242, #127546 ) ;
#89388=CARTESIAN_POINT ( 'NONE',  ( 19.41972383043609440, -2.500000000000000000, 3.061616997868383634E-16 ) ) ;
#89398=CARTESIAN_POINT ( 'NONE',  ( 10.94186803553636977, 0.000000000000000000, 2.500000000000000444 ) ) ;
#89446=EDGE_CURVE ( 'NONE', #37203, #69267, #88974, .T. ) ;
#89477=CARTESIAN_POINT ( 'NONE',  ( 3.087196949643289834, 3.821174125832445049E-16, 0.000000000000000000 ) ) ;
#89490=VECTOR ( 'NONE', #32715, 1000.000000000000000 ) ;
#89531=EDGE_LOOP ( 'NONE', ( #136594, #30217, #22512, #98392, #90777, #77587 ) ) ;
#89547=CARTESIAN_POINT ( 'NONE',  ( 4.969723521325230209, -2.055000000000000160, 2.789133085058097101E-16 ) ) ;
#89559=ADVANCED_FACE ( 'NONE', ( #74393 ), #106987, .T. ) ;
#89566=CARTESIAN_POINT ( 'NONE',  ( 4.969723521325230209, 4.202752102959690472E-16, 0.000000000000000000 ) ) ;
#89586=CARTESIAN_POINT ( 'NONE',  ( 2.139447441471317379, 4.584330080086930965E-16, 0.000000000000000000 ) ) ;
#89599=FACE_OUTER_BOUND ( 'NONE', #29339, .T. ) ;
#89600=EDGE_CURVE ( 'NONE', #29556, #14737, #75126, .T. ) ;
#89635=CARTESIAN_POINT ( 'NONE',  ( 10.94186803553636977, 3.821174125832445049E-16, 0.000000000000000000 ) ) ;
#89657=DIRECTION ( 'NONE',  ( 1.000000000000000000, 0.000000000000000000, 0.000000000000000000 ) ) ;
#89716=LINE ( 'NONE', #123079, #114594 ) ;
#89717=CARTESIAN_POINT ( 'NONE',  ( 0.5685132242927012358, -0.4000000000000004108, 2.467792535850613866 ) ) ;
#89732=ORIENTED_EDGE ( 'NONE', *, *, #29576, .T. ) ;
#89744=DIRECTION ( 'NONE',  ( -1.000000000000000000, -0.000000000000000000, -0.000000000000000000 ) ) ;
#89762=EDGE_LOOP ( 'NONE', ( #131247, #39571, #34758, #85170, #91961 ) ) ;
#89773=CIRCLE ( 'NONE', #34323, 2.500000000000000444 ) ;
#89791=EDGE_CURVE ( 'NONE', #121119, #73381, #63633, .T. ) ;
#89829=DIRECTION ( 'NONE',  ( 0.000000000000000000, -1.000000000000000000, 0.000000000000000000 ) ) ;
#89925=ORIENTED_EDGE ( 'NONE', *, *, #35869, .F. ) ;
#89961=CARTESIAN_POINT ( 'NONE',  ( 15.96626304157554266, 4.202752102959690472E-16, 0.000000000000000000 ) ) ;
#89962=EDGE_CURVE ( 'NONE', #24150, #127065, #102940, .T. ) ;
#89994=AXIS2_PLACEMENT_3D ( 'NONE', #86312, #120307, #10150 ) ;
#90067=CARTESIAN_POINT ( 'NONE',  ( 2.139447441471317379, 4.584330080086930965E-16, 0.000000000000000000 ) ) ;
#90085=DIRECTION ( 'NONE',  ( 0.000000000000000000, -1.000000000000000000, 0.000000000000000000 ) ) ;
#90118=CIRCLE ( 'NONE', #87755, 2.500000000000000444 ) ;
#90148=DIRECTION ( 'NONE',  ( -1.000000000000000000, -1.224606353822377258E-16, -0.000000000000000000 ) ) ;
#90171=ORIENTED_EDGE ( 'NONE', *, *, #113116, .T. ) ;
#90197=DIRECTION ( 'NONE',  ( -1.000000000000000000, -1.224606353822377258E-16, -0.000000000000000000 ) ) ;
#90203=DIRECTION ( 'NONE',  ( 0.000000000000000000, 0.000000000000000000, 1.000000000000000000 ) ) ;
#90220=DIRECTION ( 'NONE',  ( -0.5735764363510501562, 0.8191520442889890230, 1.003171929053521419E-16 ) ) ;
#90244=DIRECTION ( 'NONE',  ( -1.000000000000000000, -0.000000000000000000, -0.000000000000000000 ) ) ;
#90253=CARTESIAN_POINT ( 'NONE',  ( 4.969723521325230209, 4.202752102959690472E-16, 0.000000000000000000 ) ) ;
#90301=EDGE_LOOP ( 'NONE', ( #43084, #7849, #23966, #69601, #136504 ) ) ;
#90323=ADVANCED_FACE ( 'NONE', ( #39276 ), #18180, .T. ) ;
#90324=LINE ( 'NONE', #1152, #63534 ) ;
#90325=DIRECTION ( 'NONE',  ( -0.5735764363510499342, -0.8191520442889891340, 0.000000000000000000 ) ) ;
#90362=VERTEX_POINT ( 'NONE', #138583 ) ;
#90372=EDGE_CURVE ( 'NONE', #110816, #119393, #89716, .T. ) ;
#90374=ORIENTED_EDGE ( 'NONE', *, *, #53543, .T. ) ;
#90420=CARTESIAN_POINT ( 'NONE',  ( -12.69999999999998153, 0.000000000000000000, 0.000000000000000000 ) ) ;
#90466=DIRECTION ( 'NONE',  ( 1.055184596092948005E-16, -1.000000000000000000, 0.000000000000000000 ) ) ;
#90469=CYLINDRICAL_SURFACE ( 'NONE', #90507, 2.500000000000000444 ) ;
#90491=ORIENTED_EDGE ( 'NONE', *, *, #73206, .F. ) ;
#90507=AXIS2_PLACEMENT_3D ( 'NONE', #134715, #89744, #78175 ) ;
#90523=CARTESIAN_POINT ( 'NONE',  ( 21.77612515620402078, -2.500000000000000000, 3.061616997868383634E-16 ) ) ;
#90531=DIRECTION ( 'NONE',  ( 0.5735764363510448272, -0.8191520442889927978, 1.003171929053526103E-16 ) ) ;
#90535=DIRECTION ( 'NONE',  ( -0.5735764363510501562, 0.8191520442889890230, 1.003171929053521419E-16 ) ) ;
#90565=ORIENTED_EDGE ( 'NONE', *, *, #99126, .F. ) ;
#90572=AXIS2_PLACEMENT_3D ( 'NONE', #36038, #138731, #117637 ) ;
#90583=CARTESIAN_POINT ( 'NONE',  ( 12.35051985313232237, 3.061616997868383634E-16, -2.500000000000000444 ) ) ;
#90595=CARTESIAN_POINT ( 'NONE',  ( 8.111591955682463606, 2.055000000000001048, 0.000000000000000000 ) ) ;
#90621=AXIS2_PLACEMENT_3D ( 'NONE', #60908, #115914, #62300 ) ;
#90637=DIRECTION ( 'NONE',  ( -1.000000000000000000, -1.224606353822377258E-16, -0.000000000000000000 ) ) ;
#90662=CARTESIAN_POINT ( 'NONE',  ( 1.827855086967997478, 2.055000000000001048, 0.000000000000000000 ) ) ;
#90688=EDGE_CURVE ( 'NONE', #104746, #117017, #96140, .T. ) ;
#90695=CARTESIAN_POINT ( 'NONE',  ( 19.10813147593277250, 2.055000000000001048, 2.516649172247811554E-16 ) ) ;
#90699=ORIENTED_EDGE ( 'NONE', *, *, #90812, .T. ) ;
#90716=CARTESIAN_POINT ( 'NONE',  ( 2.613322195557305605, 4.202752102959690472E-16, 0.000000000000000000 ) ) ;
#90736=DIRECTION ( 'NONE',  ( 0.000000000000000000, -1.000000000000000000, 0.000000000000000000 ) ) ;
#90777=ORIENTED_EDGE ( 'NONE', *, *, #141001, .F. ) ;
#90812=EDGE_CURVE ( 'NONE', #68516, #44903, #57688, .T. ) ;
#90820=ADVANCED_FACE ( 'NONE', ( #100456 ), #59185, .T. ) ;
#90821=VERTEX_POINT ( 'NONE', #12706 ) ;
#90833=CARTESIAN_POINT ( 'NONE',  ( 1.146007053337370074, 0.3999999999999995781, 2.166563668000046849 ) ) ;
#90842=CARTESIAN_POINT ( 'NONE',  ( 8.111591955682463606, 4.202752102959690472E-16, 0.000000000000000000 ) ) ;
#90845=LINE ( 'NONE', #79984, #142 ) ;
#90859=CARTESIAN_POINT ( 'NONE',  ( 1.592112687295236251, -0.3999999999999997446, -2.358007167714499364 ) ) ;
#90918=DIRECTION ( 'NONE',  ( -1.000000000000000000, -1.224606353822377258E-16, -0.000000000000000000 ) ) ;
#90939=DIRECTION ( 'NONE',  ( 0.000000000000000000, -1.000000000000000000, 0.000000000000000000 ) ) ;
#90997=EDGE_CURVE ( 'NONE', #82989, #37103, #36096, .T. ) ;
#91012=ORIENTED_EDGE ( 'NONE', *, *, #13072, .T. ) ;
#91066=VECTOR ( 'NONE', #5990, 1000.000000000000000 ) ;
#91082=MECHANICAL_DESIGN_GEOMETRIC_PRESENTATION_REPRESENTATION('',(#56340),#128124);
#91113=CARTESIAN_POINT ( 'NONE',  ( 1.042387978378689573, 4.202752102959690472E-16, 0.000000000000000000 ) ) ;
#91119=CARTESIAN_POINT ( 'NONE',  ( 0.7307956238753654521, 0.3999999999999995226, 2.467792535850613866 ) ) ;
#91130=AXIS2_PLACEMENT_3D ( 'NONE', #41469, #20419, #131348 ) ;
#91134=CARTESIAN_POINT ( 'NONE',  ( 20.99065804761471199, 4.584330080086930965E-16, 0.000000000000000000 ) ) ;
#91190=CYLINDRICAL_SURFACE ( 'NONE', #62525, 2.500000000000000444 ) ;
#91199=VERTEX_POINT ( 'NONE', #89398 ) ;
#91228=FILL_AREA_STYLE_COLOUR ( '', #127981 ) ;
#91230=CONICAL_SURFACE ( 'NONE', #47272, 2.500000000000000444, 0.9599310885968830309 ) ;
#91237=CIRCLE ( 'NONE', #51804, 2.055000000000000604 ) ;
#91240=CARTESIAN_POINT ( 'NONE',  ( 0.7307956238753654521, 0.4000000000000001887, -2.467792535850613866 ) ) ;
#91242=DIRECTION ( 'NONE',  ( -1.000000000000000000, -1.224606353822377258E-16, -0.000000000000000000 ) ) ;
#91265=DIRECTION ( 'NONE',  ( 0.000000000000000000, 1.000000000000000000, 0.000000000000000000 ) ) ;
#91287=VECTOR ( 'NONE', #72588, 999.9999999999998863 ) ;
#91288=EDGE_CURVE ( 'NONE', #59073, #73381, #50716, .T. ) ;
#91292=ORIENTED_EDGE ( 'NONE', *, *, #121981, .F. ) ;
#91379=FACE_OUTER_BOUND ( 'NONE', #27701, .T. ) ;
#91381=ORIENTED_EDGE ( 'NONE', *, *, #11425, .T. ) ;
#91420=DIRECTION ( 'NONE',  ( -1.000000000000000000, -1.224606353822377258E-16, -0.000000000000000000 ) ) ;
#91439=CARTESIAN_POINT ( 'NONE',  ( 0.3605397743886049056, 0.4000000000000001332, -2.166563419957293402 ) ) ;
#91503=DIRECTION ( 'NONE',  ( 0.000000000000000000, -1.000000000000000000, 0.000000000000000000 ) ) ;
#91517=CARTESIAN_POINT ( 'NONE',  ( 12.03892749862900402, 4.202752102959690472E-16, 0.000000000000000000 ) ) ;
#91577=CIRCLE ( 'NONE', #10525, 2.500000000000000444 ) ;
#91686=ORIENTED_EDGE ( 'NONE', *, *, #125848, .T. ) ;
#91705=DIRECTION ( 'NONE',  ( -1.000000000000000000, -0.000000000000000000, -0.000000000000000000 ) ) ;
#91737=DIRECTION ( 'NONE',  ( 0.000000000000000000, -1.000000000000000000, 0.000000000000000000 ) ) ;
#91746=CARTESIAN_POINT ( 'NONE',  ( 8.585466709768445170, 3.821174125832445049E-16, 0.000000000000000000 ) ) ;
#91751=AXIS2_PLACEMENT_3D ( 'NONE', #21639, #66579, #132575 ) ;
#91762=EDGE_CURVE ( 'NONE', #24475, #94208, #9877, .T. ) ;
#91769=EDGE_LOOP ( 'NONE', ( #64328, #66994, #135298, #12268, #76551 ) ) ;
#91785=ADVANCED_FACE ( 'NONE', ( #109909 ), #107944, .T. ) ;
#91852=DIRECTION ( 'NONE',  ( -1.000000000000000000, -1.224606353822377258E-16, -0.000000000000000000 ) ) ;
#91878=ORIENTED_EDGE ( 'NONE', *, *, #91762, .F. ) ;
#91892=EDGE_CURVE ( 'NONE', #37103, #92014, #50256, .T. ) ;
#91896=CARTESIAN_POINT ( 'NONE',  ( 12.82439460721831104, -2.055000000000000160, 2.789133085058097101E-16 ) ) ;
#91899=PRESENTATION_STYLE_ASSIGNMENT (( #68757 ) ) ;
#91918=CARTESIAN_POINT ( 'NONE',  ( 19.89359858452208130, 4.202752102959690472E-16, 0.000000000000000000 ) ) ;
#91945=DIRECTION ( 'NONE',  ( -1.000000000000000000, -1.224606353822377258E-16, -0.000000000000000000 ) ) ;
#91959=ORIENTED_EDGE ( 'NONE', *, *, #34004, .F. ) ;
#91961=ORIENTED_EDGE ( 'NONE', *, *, #25164, .F. ) ;
#91991=EDGE_CURVE ( 'NONE', #54699, #16019, #142865, .T. ) ;
#92014=VERTEX_POINT ( 'NONE', #5404 ) ;
#92048=LINE ( 'NONE', #26105, #107849 ) ;
#92211=DIRECTION ( 'NONE',  ( 0.000000000000000000, -1.000000000000000000, 0.000000000000000000 ) ) ;
#92247=CARTESIAN_POINT ( 'NONE',  ( 0.7307956238753654521, -0.3999999999999997446, -2.467792535850613866 ) ) ;
#92253=CARTESIAN_POINT ( 'NONE',  ( 20.67906569311139009, 4.202752102959690472E-16, 0.000000000000000000 ) ) ;
#92291=AXIS2_PLACEMENT_3D ( 'NONE', #1335, #2030, #34716 ) ;
#92318=DIRECTION ( 'NONE',  ( -1.000000000000000000, -0.000000000000000000, -0.000000000000000000 ) ) ;
#92380=DIRECTION ( 'NONE',  ( -1.000000000000000000, -0.000000000000000000, -0.000000000000000000 ) ) ;
#92396=ADVANCED_FACE ( 'NONE', ( #72721 ), #92989, .T. ) ;
#92460=DIRECTION ( 'NONE',  ( -1.000000000000000000, -1.224606353822377258E-16, -0.000000000000000000 ) ) ;
#92464=VECTOR ( 'NONE', #56189, 1000.000000000000000 ) ;
#92472=AXIS2_PLACEMENT_3D ( 'NONE', #52629, #19994, #65713 ) ;
#92484=DIRECTION ( 'NONE',  ( -1.000000000000000000, -1.224606353822377258E-16, -0.000000000000000000 ) ) ;
#92492=DIRECTION ( 'NONE',  ( 1.055184596092948005E-16, -1.000000000000000000, 0.000000000000000000 ) ) ;
#92503=FACE_OUTER_BOUND ( 'NONE', #93547, .T. ) ;
#92532=CARTESIAN_POINT ( 'NONE',  ( 19.41972383043609440, -2.500000000000000444, 3.061616997868384127E-16 ) ) ;
#92561=AXIS2_PLACEMENT_3D ( 'NONE', #93642, #6571, #137871 ) ;
#92586=FACE_OUTER_BOUND ( 'NONE', #116713, .T. ) ;
#92643=ORIENTED_EDGE ( 'NONE', *, *, #24785, .F. ) ;
#92679=CIRCLE ( 'NONE', #32590, 2.055000000000000604 ) ;
#92727=VECTOR ( 'NONE', #50779, 1000.000000000000000 ) ;
#92754=CARTESIAN_POINT ( 'NONE',  ( 19.58200623001875940, 0.000000000000000000, 2.500000000000000444 ) ) ;
#92776=VECTOR ( 'NONE', #129643, 1000.000000000000000 ) ;
#92783=ORIENTED_EDGE ( 'NONE', *, *, #101437, .T. ) ;
#92820=VECTOR ( 'NONE', #551, 1000.000000000000000 ) ;
#92833=DIRECTION ( 'NONE',  ( -0.5735764363510499342, -0.8191520442889891340, 0.000000000000000000 ) ) ;
#92839=EDGE_LOOP ( 'NONE', ( #137823, #60895, #5382, #9544, #89101, #91292 ) ) ;
#92912=CIRCLE ( 'NONE', #46720, 2.500000000000000444 ) ;
#92939=AXIS2_PLACEMENT_3D ( 'NONE', #113554, #83655, #57795 ) ;
#92944=FACE_OUTER_BOUND ( 'NONE', #90301, .T. ) ;
#92953=LINE ( 'NONE', #38577, #23212 ) ;
#92965=EDGE_CURVE ( 'NONE', #17540, #19275, #438, .T. ) ;
#92989=CYLINDRICAL_SURFACE ( 'NONE', #43415, 2.500000000000000444 ) ;
#93024=VERTEX_POINT ( 'NONE', #108643 ) ;
#93054=ADVANCED_FACE ( 'NONE', ( #14181 ), #122143, .T. ) ;
#93082=ORIENTED_EDGE ( 'NONE', *, *, #38142, .F. ) ;
#93087=AXIS2_PLACEMENT_3D ( 'NONE', #78118, #68680, #123047 ) ;
#93160=VECTOR ( 'NONE', #121262, 1000.000000000000000 ) ;
#93200=ORIENTED_EDGE ( 'NONE', *, *, #121301, .T. ) ;
#93204=DIRECTION ( 'NONE',  ( -1.000000000000000000, -1.224606353822377258E-16, -0.000000000000000000 ) ) ;
#93237=VECTOR ( 'NONE', #112021, 999.9999999999998863 ) ;
#93248=VERTEX_POINT ( 'NONE', #62713 ) ;
#93293=FACE_OUTER_BOUND ( 'NONE', #115056, .T. ) ;
#93303=VERTEX_POINT ( 'NONE', #53989 ) ;
#93332=CARTESIAN_POINT ( 'NONE',  ( 10.77958563595370833, -2.500000000000000444, 3.061616997868384127E-16 ) ) ;
#93333=VECTOR ( 'NONE', #50819, 999.9999999999998863 ) ;
#93336=ORIENTED_EDGE ( 'NONE', *, *, #61737, .F. ) ;
#93364=ORIENTED_EDGE ( 'NONE', *, *, #116674, .F. ) ;
#93413=CIRCLE ( 'NONE', #132775, 2.500000000000000444 ) ;
#93418=EDGE_CURVE ( 'NONE', #34275, #53418, #22956, .T. ) ;
#93443=VECTOR ( 'NONE', #92833, 1000.000000000000000 ) ;
#93530=ORIENTED_EDGE ( 'NONE', *, *, #127874, .F. ) ;
#93547=EDGE_LOOP ( 'NONE', ( #96787, #27408, #54177, #8197 ) ) ;
#93571=ORIENTED_EDGE ( 'NONE', *, *, #94131, .T. ) ;
#93591=LINE ( 'NONE', #114602, #116461 ) ;
#93601=DIRECTION ( 'NONE',  ( -1.000000000000000000, -1.224606353822377258E-16, -0.000000000000000000 ) ) ;
#93628=EDGE_LOOP ( 'NONE', ( #111499, #29916, #90699, #86230, #72062, #23090 ) ) ;
#93642=CARTESIAN_POINT ( 'NONE',  ( 12.51280225271498736, 3.821174125832445049E-16, 0.000000000000000000 ) ) ;
#93686=CARTESIAN_POINT ( 'NONE',  ( 18.63425672184678916, 4.584330080086930965E-16, 0.000000000000000000 ) ) ;
#93687=CARTESIAN_POINT ( 'NONE',  ( 0.7307956238753657852, -2.500000000000000000, 0.000000000000000000 ) ) ;
#93711=ORIENTED_EDGE ( 'NONE', *, *, #6001, .F. ) ;
#93717=ORIENTED_EDGE ( 'NONE', *, *, #132882, .F. ) ;
#93731=CARTESIAN_POINT ( 'NONE',  ( 6.852250093007166143, 2.500000000000000888, 0.000000000000000000 ) ) ;
#93739=CARTESIAN_POINT ( 'NONE',  ( 11.72733514412567857, 3.821174125832445049E-16, 0.000000000000000000 ) ) ;
#93744=CONICAL_SURFACE ( 'NONE', #31264, 2.055000000000000604, 0.9599310885968764806 ) ;
#93751=LINE ( 'NONE', #85005, #79061 ) ;
#93768=FACE_OUTER_BOUND ( 'NONE', #119343, .T. ) ;
#93770=CARTESIAN_POINT ( 'NONE',  ( 12.35051985313232237, 4.584330080086930965E-16, 0.000000000000000000 ) ) ;
#93785=DIRECTION ( 'NONE',  ( 1.000000000000000000, 1.224606353822377258E-16, 0.000000000000000000 ) ) ;
#93788=DIRECTION ( 'NONE',  ( 0.000000000000000000, -1.000000000000000000, 0.000000000000000000 ) ) ;
#93795=EDGE_CURVE ( 'NONE', #117989, #123895, #32401, .T. ) ;
#93811=EDGE_CURVE ( 'NONE', #20222, #17540, #134225, .T. ) ;
#93815=VERTEX_POINT ( 'NONE', #47253 ) ;
#93831=CARTESIAN_POINT ( 'NONE',  ( -12.69999999999998153, 0.000000000000000000, 2.500000000000000444 ) ) ;
#93875=EDGE_CURVE ( 'NONE', #125896, #130467, #13828, .T. ) ;
#93938=EDGE_CURVE ( 'NONE', #110962, #14269, #69690, .T. ) ;
#93939=CARTESIAN_POINT ( 'NONE',  ( 8.423184310185783730, 4.584330080086930965E-16, 0.000000000000000000 ) ) ;
#93942=ORIENTED_EDGE ( 'NONE', *, *, #116300, .F. ) ;
#93967=ORIENTED_EDGE ( 'NONE', *, *, #39427, .T. ) ;
#93989=ORIENTED_EDGE ( 'NONE', *, *, #25486, .T. ) ;
#93991=CARTESIAN_POINT ( 'NONE',  ( 2.613322195557305605, 4.202752102959690472E-16, 0.000000000000000000 ) ) ;
#93992=DIRECTION ( 'NONE',  ( -1.000000000000000000, -1.224606353822377258E-16, -0.000000000000000000 ) ) ;
#94020=ORIENTED_EDGE ( 'NONE', *, *, #23362, .F. ) ;
#94022=EDGE_CURVE ( 'NONE', #52416, #118938, #133271, .T. ) ;
#94026=EDGE_CURVE ( 'NONE', #141895, #94686, #102773, .T. ) ;
#94032=AXIS2_PLACEMENT_3D ( 'NONE', #93686, #115381, #104544 ) ;
#94065=ADVANCED_FACE ( 'NONE', ( #33952 ), #101825, .T. ) ;
#94093=ORIENTED_EDGE ( 'NONE', *, *, #89015, .F. ) ;
#94101=ORIENTED_EDGE ( 'NONE', *, *, #103071, .T. ) ;
#94131=EDGE_CURVE ( 'NONE', #5092, #111882, #118027, .T. ) ;
#94134=CARTESIAN_POINT ( 'NONE',  ( 9.370933818357753964, 3.821174125832445049E-16, 0.000000000000000000 ) ) ;
#94138=DIRECTION ( 'NONE',  ( 0.000000000000000000, 0.000000000000000000, 1.000000000000000000 ) ) ;
#94173=AXIS2_PLACEMENT_3D ( 'NONE', #4164, #3491, #6322 ) ;
#94176=CARTESIAN_POINT ( 'NONE',  ( 21.66240673564756491, -2.337593264352435085, 2.862726108897622684E-16 ) ) ;
#94205=ADVANCED_FACE ( 'NONE', ( #38328 ), #4582, .T. ) ;
#94208=VERTEX_POINT ( 'NONE', #7072 ) ;
#94222=DIRECTION ( 'NONE',  ( 0.000000000000000000, -1.000000000000000000, 0.000000000000000000 ) ) ;
#94246=CIRCLE ( 'NONE', #64154, 2.500000000000000444 ) ;
#94259=DIRECTION ( 'NONE',  ( 1.000000000000000000, 1.224606353822377258E-16, 0.000000000000000000 ) ) ;
#94263=DIRECTION ( 'NONE',  ( 0.000000000000000000, -1.000000000000000000, 0.000000000000000000 ) ) ;
#94361=CARTESIAN_POINT ( 'NONE',  ( 0.03865117921958852176, 0.3999999999999995781, 2.083945894980139268 ) ) ;
#94374=CARTESIAN_POINT ( 'NONE',  ( 12.82439460721831104, 4.202752102959690472E-16, 0.000000000000000000 ) ) ;
#94523=CARTESIAN_POINT ( 'NONE',  ( 13.60986171580761805, 2.055000000000001048, 2.516649172247811554E-16 ) ) ;
#94524=CIRCLE ( 'NONE', #62273, 2.500000000000000444 ) ;
#94533=CARTESIAN_POINT ( 'NONE',  ( 13.60986171580761805, -2.055000000000000160, 2.789133085058097101E-16 ) ) ;
#94558=ORIENTED_EDGE ( 'NONE', *, *, #46004, .T. ) ;
#94627=CARTESIAN_POINT ( 'NONE',  ( 16.27785539607886633, 0.000000000000000000, 2.500000000000000444 ) ) ;
#94638=DIRECTION ( 'NONE',  ( -1.000000000000000000, -1.224606353822377258E-16, -0.000000000000000000 ) ) ;
#94648=DIRECTION ( 'NONE',  ( -1.000000000000000000, -1.224606353822377258E-16, -0.000000000000000000 ) ) ;
#94654=CARTESIAN_POINT ( 'NONE',  ( 2.924914550060625729, -2.500000000000000000, 3.061616997868383634E-16 ) ) ;
#94686=VERTEX_POINT ( 'NONE', #15633 ) ;
#94735=ORIENTED_EDGE ( 'NONE', *, *, #93795, .T. ) ;
#94754=AXIS2_PLACEMENT_3D ( 'NONE', #111246, #22101, #66358 ) ;
#94814=CIRCLE ( 'NONE', #87912, 2.500000000000000444 ) ;
#94833=DIRECTION ( 'NONE',  ( 0.000000000000000000, -1.000000000000000000, 0.000000000000000000 ) ) ;
#94834=AXIS2_PLACEMENT_3D ( 'NONE', #35130, #79373, #123576 ) ;
#94844=CIRCLE ( 'NONE', #113377, 2.055000000000000604 ) ;
#94864=DIRECTION ( 'NONE',  ( -1.000000000000000000, -1.224606353822377258E-16, -0.000000000000000000 ) ) ;
#94873=DIRECTION ( 'NONE',  ( 1.000000000000000000, 1.224606353822377258E-16, 0.000000000000000000 ) ) ;
#94927=CARTESIAN_POINT ( 'NONE',  ( 5.281315875828549444, 4.584330080086930965E-16, 0.000000000000000000 ) ) ;
#94944=FACE_OUTER_BOUND ( 'NONE', #55225, .T. ) ;
#94947=CARTESIAN_POINT ( 'NONE',  ( 4.184256412735922304, -2.055000000000000160, 2.789133085058097101E-16 ) ) ;
#94962=VECTOR ( 'NONE', #17116, 1000.000000000000000 ) ;
#94966=DIRECTION ( 'NONE',  ( 0.000000000000000000, 0.000000000000000000, -1.000000000000000000 ) ) ;
#94990=EDGE_CURVE ( 'NONE', #2478, #22757, #48684, .T. ) ;
#94992=CARTESIAN_POINT ( 'NONE',  ( -12.69999999999998153, 0.000000000000000000, 2.500000000000000444 ) ) ;
#94999=EDGE_CURVE ( 'NONE', #53690, #129512, #11444, .T. ) ;
#95004=ORIENTED_EDGE ( 'NONE', *, *, #22815, .F. ) ;
#95005=DIRECTION ( 'NONE',  ( -1.000000000000000000, -1.224606353822377258E-16, -0.000000000000000000 ) ) ;
#95019=ADVANCED_FACE ( 'NONE', ( #140666 ), #83199, .T. ) ;
#95043=DIRECTION ( 'NONE',  ( 0.000000000000000000, -1.000000000000000000, 0.000000000000000000 ) ) ;
#95067=CARTESIAN_POINT ( 'NONE',  ( 9.370933818357753964, 2.500000000000000444, 3.061616997868383634E-16 ) ) ;
#95088=DIRECTION ( 'NONE',  ( 0.000000000000000000, -1.000000000000000000, 0.000000000000000000 ) ) ;
#95089=CARTESIAN_POINT ( 'NONE',  ( 12.51280225271498736, 3.821174125832445049E-16, 0.000000000000000000 ) ) ;
#95098=ORIENTED_EDGE ( 'NONE', *, *, #57252, .F. ) ;
#95154=AXIS2_PLACEMENT_3D ( 'NONE', #16413, #4074, #48359 ) ;
#95158=ORIENTED_EDGE ( 'NONE', *, *, #51564, .F. ) ;
#95187=DIRECTION ( 'NONE',  ( -1.000000000000000000, -1.224606353822377258E-16, -0.000000000000000000 ) ) ;
#95212=CONICAL_SURFACE ( 'NONE', #16550, 2.055000000000000604, 0.9599310885968764806 ) ;
#95238=CIRCLE ( 'NONE', #99906, 2.500000000000000444 ) ;
#95276=CYLINDRICAL_SURFACE ( 'NONE', #58526, 2.500000000000000444 ) ;
#95292=DIRECTION ( 'NONE',  ( -0.5735764363510499342, -0.8191520442889891340, 0.000000000000000000 ) ) ;
#95316=AXIS2_PLACEMENT_3D ( 'NONE', #99442, #108, #22584 ) ;
#95343=VECTOR ( 'NONE', #68255, 1000.000000000000000 ) ;
#95346=ORIENTED_EDGE ( 'NONE', *, *, #35669, .T. ) ;
#95350=CARTESIAN_POINT ( 'NONE',  ( 14.86920357848291196, 3.821174125832445049E-16, 0.000000000000000000 ) ) ;
#95384=LINE ( 'NONE', #94654, #130032 ) ;
#95390=ORIENTED_EDGE ( 'NONE', *, *, #4391, .T. ) ;
#95435=VERTEX_POINT ( 'NONE', #81893 ) ;
#95476=AXIS2_PLACEMENT_3D ( 'NONE', #76665, #98395, #133874 ) ;
#95487=ORIENTED_EDGE ( 'NONE', *, *, #13226, .F. ) ;
#95534=AXIS2_PLACEMENT_3D ( 'NONE', #28528, #40139, #108168 ) ;
#95615=VERTEX_POINT ( 'NONE', #129620 ) ;
#95691=VERTEX_POINT ( 'NONE', #102730 ) ;
#95708=CARTESIAN_POINT ( 'NONE',  ( 8.423184310185783730, -2.500000000000000000, 3.061616997868383634E-16 ) ) ;
#95724=CARTESIAN_POINT ( 'NONE',  ( 20.36747333860806819, 3.061616997868387579E-16, -2.500000000000000444 ) ) ;
#95768=CARTESIAN_POINT ( 'NONE',  ( 5.755190629914537226, -2.055000000000000160, 2.789133085058097101E-16 ) ) ;
#95772=DIRECTION ( 'NONE',  ( -1.000000000000000000, -1.224606353822377258E-16, -0.000000000000000000 ) ) ;
#95803=AXIS2_PLACEMENT_3D ( 'NONE', #128300, #5761, #7178 ) ;
#95837=DIRECTION ( 'NONE',  ( -0.5735764363510499342, -0.8191520442889891340, 0.000000000000000000 ) ) ;
#95839=ORIENTED_EDGE ( 'NONE', *, *, #53298, .F. ) ;
#95870=CONICAL_SURFACE ( 'NONE', #107459, 2.500000000000000444, 0.9599310885968830309 ) ;
#95899=CARTESIAN_POINT ( 'NONE',  ( 2.613322195557305161, 2.055000000000001048, 2.516649172247811554E-16 ) ) ;
#95916=EDGE_LOOP ( 'NONE', ( #63043, #22037, #112403, #77032, #136280, #60801 ) ) ;
#95925=EDGE_LOOP ( 'NONE', ( #47001, #99588, #136638, #117693, #46819, #113168 ) ) ;
#95948=ORIENTED_EDGE ( 'NONE', *, *, #132588, .T. ) ;
#95959=FACE_OUTER_BOUND ( 'NONE', #116453, .T. ) ;
#95980=DIRECTION ( 'NONE',  ( -1.000000000000000000, -0.000000000000000000, -0.000000000000000000 ) ) ;
#96006=EDGE_CURVE ( 'NONE', #3259, #89141, #8929, .T. ) ;
#96040=ORIENTED_EDGE ( 'NONE', *, *, #91288, .F. ) ;
#96079=CARTESIAN_POINT ( 'NONE',  ( 8.897059064271770623, 4.202752102959690472E-16, 0.000000000000000000 ) ) ;
#96096=DIRECTION ( 'NONE',  ( 1.000000000000000000, 1.224606353822377258E-16, 0.000000000000000000 ) ) ;
#96107=CONICAL_SURFACE ( 'NONE', #72990, 2.055000000000000604, 0.9599310885968764806 ) ;
#96111=VERTEX_POINT ( 'NONE', #77959 ) ;
#96136=ORIENTED_EDGE ( 'NONE', *, *, #40527, .T. ) ;
#96140=LINE ( 'NONE', #140377, #110047 ) ;
#96148=LINE ( 'NONE', #5573, #25743 ) ;
#96155=CARTESIAN_POINT ( 'NONE',  ( 7.637717201596474048, 4.584330080086930965E-16, 0.000000000000000000 ) ) ;
#96159=DIRECTION ( 'NONE',  ( -1.000000000000000000, -1.224606353822377258E-16, -0.000000000000000000 ) ) ;
#96166=ADVANCED_FACE ( 'NONE', ( #46803 ), #36813, .T. ) ;
#96218=ORIENTED_EDGE ( 'NONE', *, *, #78013, .T. ) ;
#96246=CARTESIAN_POINT ( 'NONE',  ( 3.872664058232598183, 3.821174125832445049E-16, 0.000000000000000000 ) ) ;
#96258=CARTESIAN_POINT ( 'NONE',  ( 1.516262732464673579, 3.821174125832445049E-16, 0.000000000000000000 ) ) ;
#96329=DIRECTION ( 'NONE',  ( 0.000000000000000000, -1.000000000000000000, 0.000000000000000000 ) ) ;
#96333=DIRECTION ( 'NONE',  ( -1.000000000000000000, -1.224606353822377258E-16, -0.000000000000000000 ) ) ;
#96341=DIRECTION ( 'NONE',  ( -1.000000000000000000, -1.224606353822377258E-16, -0.000000000000000000 ) ) ;
#96401=DIRECTION ( 'NONE',  ( 0.000000000000000000, -1.000000000000000000, 0.000000000000000000 ) ) ;
#96405=ORIENTED_EDGE ( 'NONE', *, *, #140335, .F. ) ;
#96414=ORIENTED_EDGE ( 'NONE', *, *, #127373, .T. ) ;
#96415=ORIENTED_EDGE ( 'NONE', *, *, #18869, .F. ) ;
#96444=FACE_OUTER_BOUND ( 'NONE', #42693, .T. ) ;
#96450=ADVANCED_FACE ( 'NONE', ( #128587 ), #31422, .T. ) ;
#96483=AXIS2_PLACEMENT_3D ( 'NONE', #39869, #140563, #71773 ) ;
#96499=ORIENTED_EDGE ( 'NONE', *, *, #120889, .F. ) ;
#96501=CIRCLE ( 'NONE', #38698, 2.500000000000000444 ) ;
#96521=AXIS2_PLACEMENT_3D ( 'NONE', #60614, #92460, #135989 ) ;
#96546=EDGE_LOOP ( 'NONE', ( #113318, #47605, #43244, #33272, #59303, #112458 ) ) ;
#96568=DIRECTION ( 'NONE',  ( -1.000000000000000000, -1.224606353822377258E-16, -0.000000000000000000 ) ) ;
#96571=DIRECTION ( 'NONE',  ( -1.000000000000000000, -1.224606353822377258E-16, -0.000000000000000000 ) ) ;
#96587=CIRCLE ( 'NONE', #36417, 2.500000000000000444 ) ;
#96591=LINE ( 'NONE', #30685, #109043 ) ;
#96600=VERTEX_POINT ( 'NONE', #55322 ) ;
#96619=CARTESIAN_POINT ( 'NONE',  ( 0.5685132242927012358, 4.584330080086930965E-16, 0.000000000000000000 ) ) ;
#96623=ADVANCED_FACE ( 'NONE', ( #57476 ), #32870, .T. ) ;
#96627=ORIENTED_EDGE ( 'NONE', *, *, #42410, .F. ) ;
#96639=CARTESIAN_POINT ( 'NONE',  ( 15.65467068707222076, 3.821174125832445049E-16, 0.000000000000000000 ) ) ;
#96667=DIRECTION ( 'NONE',  ( 0.000000000000000000, -1.000000000000000000, 0.000000000000000000 ) ) ;
#96718=VECTOR ( 'NONE', #76256, 1000.000000000000000 ) ;
#96731=EDGE_CURVE ( 'NONE', #126491, #97154, #61076, .T. ) ;
#96740=ORIENTED_EDGE ( 'NONE', *, *, #15291, .T. ) ;
#96754=EDGE_LOOP ( 'NONE', ( #115969, #48730, #5907, #59544, #93364 ) ) ;
#96787=ORIENTED_EDGE ( 'NONE', *, *, #59713, .F. ) ;
#96789=CARTESIAN_POINT ( 'NONE',  ( 1.353980332882009252, -0.4000000000000004108, 2.467792535850613866 ) ) ;
#96822=CARTESIAN_POINT ( 'NONE',  ( 12.35051985313232237, 4.584330080086930965E-16, 0.000000000000000000 ) ) ;
#96837=DIRECTION ( 'NONE',  ( 0.5735764363510444941, 0.8191520442889929088, 0.000000000000000000 ) ) ;
#96850=ORIENTED_EDGE ( 'NONE', *, *, #51564, .T. ) ;
#96923=AXIS2_PLACEMENT_3D ( 'NONE', #68178, #124641, #79038 ) ;
#96960=EDGE_CURVE ( 'NONE', #34275, #25809, #129521, .T. ) ;
#96978=ORIENTED_EDGE ( 'NONE', *, *, #121526, .F. ) ;
#97024=AXIS2_PLACEMENT_3D ( 'NONE', #12772, #122987, #23668 ) ;
#97037=CARTESIAN_POINT ( 'NONE',  ( 1.353980332882009252, -0.3999999999999997446, -2.467792535850613866 ) ) ;
#97045=CARTESIAN_POINT ( 'NONE',  ( 16.27785539607886633, 4.584330080086930965E-16, 0.000000000000000000 ) ) ;
#97060=CARTESIAN_POINT ( 'NONE',  ( 4.495848767239241539, 4.584330080086930965E-16, 0.000000000000000000 ) ) ;
#97073=CIRCLE ( 'NONE', #39301, 2.500000000000000444 ) ;
#97101=CIRCLE ( 'NONE', #134208, 2.500000000000000444 ) ;
#97105=EDGE_CURVE ( 'NONE', #12477, #48215, #76366, .T. ) ;
#97135=DIRECTION ( 'NONE',  ( -1.000000000000000000, -1.224606353822377258E-16, -0.000000000000000000 ) ) ;
#97143=EDGE_CURVE ( 'NONE', #15589, #106919, #20513, .T. ) ;
#97154=VERTEX_POINT ( 'NONE', #98985 ) ;
#97175=DIRECTION ( 'NONE',  ( 0.000000000000000000, -1.000000000000000000, 0.000000000000000000 ) ) ;
#97185=CARTESIAN_POINT ( 'NONE',  ( 16.44013779566152778, 3.821174125832445049E-16, 0.000000000000000000 ) ) ;
#97192=CIRCLE ( 'NONE', #83369, 2.500000000000000444 ) ;
#97193=LINE ( 'NONE', #18958, #89490 ) ;
#97217=VERTEX_POINT ( 'NONE', #19302 ) ;
#97233=AXIS2_PLACEMENT_3D ( 'NONE', #97939, #118232, #21074 ) ;
#97262=EDGE_LOOP ( 'NONE', ( #49005, #36390, #58470, #78090, #50384 ) ) ;
#97270=EDGE_CURVE ( 'NONE', #61548, #60360, #13929, .T. ) ;
#97284=VECTOR ( 'NONE', #95980, 1000.000000000000000 ) ;
#97294=DIRECTION ( 'NONE',  ( 0.000000000000000000, -1.000000000000000000, 0.000000000000000000 ) ) ;
#97307=FACE_OUTER_BOUND ( 'NONE', #81171, .T. ) ;
#97350=ORIENTED_EDGE ( 'NONE', *, *, #72885, .F. ) ;
#97356=VECTOR ( 'NONE', #120915, 999.9999999999998863 ) ;
#97366=EDGE_CURVE ( 'NONE', #59073, #117931, #134322, .T. ) ;
#97380=CARTESIAN_POINT ( 'NONE',  ( 1.629999999999999893, -0.4000000000000004108, 2.303088455023526215 ) ) ;
#97415=CARTESIAN_POINT ( 'NONE',  ( -12.69999999999998153, 3.061616997868383634E-16, -2.500000000000000444 ) ) ;
#97452=EDGE_CURVE ( 'NONE', #104716, #109980, #6775, .T. ) ;
#97523=AXIS2_PLACEMENT_3D ( 'NONE', #15188, #59465, #134887 ) ;
#97539=DIRECTION ( 'NONE',  ( -1.000000000000000000, -0.000000000000000000, -0.000000000000000000 ) ) ;
#97565=CARTESIAN_POINT ( 'NONE',  ( 19.10813147593277250, -2.055000000000000160, 0.000000000000000000 ) ) ;
#97609=CIRCLE ( 'NONE', #65168, 2.256103126841972895 ) ;
#97652=AXIS2_PLACEMENT_3D ( 'NONE', #91746, #1150, #35273 ) ;
#97689=EDGE_CURVE ( 'NONE', #139436, #8017, #92679, .T. ) ;
#97699=LINE ( 'NONE', #121581, #77726 ) ;
#97718=DIRECTION ( 'NONE',  ( -1.000000000000000000, -1.224606353822377258E-16, -0.000000000000000000 ) ) ;
#97755=ORIENTED_EDGE ( 'NONE', *, *, #131248, .T. ) ;
#97796=ADVANCED_FACE ( 'NONE', ( #28426 ), #82814, .T. ) ;
#97836=VERTEX_POINT ( 'NONE', #137192 ) ;
#97842=( GEOMETRIC_REPRESENTATION_CONTEXT ( 3 ) GLOBAL_UNCERTAINTY_ASSIGNED_CONTEXT ( ( #53291 ) ) GLOBAL_UNIT_ASSIGNED_CONTEXT ( ( #101351, #34687, #26649 ) ) REPRESENTATION_CONTEXT ( 'NONE', 'WORKASPACE' ) );
#97910=ORIENTED_EDGE ( 'NONE', *, *, #113116, .F. ) ;
#97915=EDGE_CURVE ( 'NONE', #106463, #121849, #9478, .T. ) ;
#97939=CARTESIAN_POINT ( 'NONE',  ( 13.13598696172163116, 4.584330080086930965E-16, 0.000000000000000000 ) ) ;
#97972=ORIENTED_EDGE ( 'NONE', *, *, #5130, .T. ) ;
#98014=ORIENTED_EDGE ( 'NONE', *, *, #141059, .T. ) ;
#98031=DIRECTION ( 'NONE',  ( -1.000000000000000000, -1.224606353822377258E-16, -0.000000000000000000 ) ) ;
#98048=VERTEX_POINT ( 'NONE', #20921 ) ;
#98082=B_SPLINE_CURVE_WITH_KNOTS ( 'NONE', 3,
 ( #50041, #138473, #75363, #61646 ),
 .UNSPECIFIED., .F., .F.,
 ( 4, 4 ),
 ( 0.009196836153558695173, 0.009397116448368620506 ),
 .UNSPECIFIED. ) ;
#98089=CIRCLE ( 'NONE', #95803, 2.500000000000000444 ) ;
#98138=CARTESIAN_POINT ( 'NONE',  ( 1.592112669765240796, -0.4000000000000004108, 2.358007193124715073 ) ) ;
#98186=DIRECTION ( 'NONE',  ( -1.000000000000000000, -1.224606353822377258E-16, -0.000000000000000000 ) ) ;
#98232=ORIENTED_EDGE ( 'NONE', *, *, #70512, .F. ) ;
#98285=AXIS2_PLACEMENT_3D ( 'NONE', #96619, #61922, #140859 ) ;
#98337=CARTESIAN_POINT ( 'NONE',  ( -12.69999999999998153, 3.061616997868383634E-16, -2.500000000000000444 ) ) ;
#98358=DIRECTION ( 'NONE',  ( 0.5735764363510448272, -0.8191520442889927978, 1.003171929053526103E-16 ) ) ;
#98372=VERTEX_POINT ( 'NONE', #93332 ) ;
#98382=DIRECTION ( 'NONE',  ( 1.734723475976806848E-16, -1.000000000000000000, 0.000000000000000000 ) ) ;
#98383=EDGE_CURVE ( 'NONE', #111457, #132148, #106752, .T. ) ;
#98392=ORIENTED_EDGE ( 'NONE', *, *, #28608, .T. ) ;
#98395=DIRECTION ( 'NONE',  ( -1.000000000000000000, -1.224606353822377258E-16, -0.000000000000000000 ) ) ;
#98454=CARTESIAN_POINT ( 'NONE',  ( 3.872664058232597739, 2.500000000000001776, 3.061616997868385113E-16 ) ) ;
#98515=ORIENTED_EDGE ( 'NONE', *, *, #29587, .T. ) ;
#98556=EDGE_CURVE ( 'NONE', #74147, #97217, #30553, .T. ) ;
#98637=VERTEX_POINT ( 'NONE', #92247 ) ;
#98684=ORIENTED_EDGE ( 'NONE', *, *, #59300, .F. ) ;
#98700=CIRCLE ( 'NONE', #40876, 2.500000000000000444 ) ;
#98740=CONICAL_SURFACE ( 'NONE', #43208, 2.500000000000000444, 0.9599310885968830309 ) ;
#98773=CARTESIAN_POINT ( 'NONE',  ( 0.1161069444170876042, 0.3999999999999995781, 2.220360628129161906 ) ) ;
#98818=DIRECTION ( 'NONE',  ( -1.000000000000000000, -1.224606353822377258E-16, -0.000000000000000000 ) ) ;
#98835=DIRECTION ( 'NONE',  ( -0.5735764363510499342, -0.8191520442889891340, 0.000000000000000000 ) ) ;
#98845=CARTESIAN_POINT ( 'NONE',  ( 1.042387978378689573, -0.3999999999999998002, -2.015694669338588429 ) ) ;
#98886=VECTOR ( 'NONE', #95292, 1000.000000000000000 ) ;
#98931=CARTESIAN_POINT ( 'NONE',  ( 1.353980332882009030, 2.500000000000000888, 0.000000000000000000 ) ) ;
#98974=CIRCLE ( 'NONE', #140681, 2.055000000000000604 ) ;
#98985=CARTESIAN_POINT ( 'NONE',  ( 4.495848767239241539, 0.000000000000000000, 2.500000000000000444 ) ) ;
#99014=ORIENTED_EDGE ( 'NONE', *, *, #79482, .T. ) ;
#99021=EDGE_CURVE ( 'NONE', #88761, #58598, #23456, .T. ) ;
#99045=ORIENTED_EDGE ( 'NONE', *, *, #15934, .T. ) ;
#99054=ORIENTED_EDGE ( 'NONE', *, *, #89600, .T. ) ;
#99060=CIRCLE ( 'NONE', #136128, 2.500000000000000444 ) ;
#99089=EDGE_CURVE ( 'NONE', #142779, #124724, #67487, .T. ) ;
#99111=VERTEX_POINT ( 'NONE', #83370 ) ;
#99126=EDGE_CURVE ( 'NONE', #17542, #22488, #42002, .T. ) ;
#99156=ADVANCED_FACE ( 'NONE', ( #142050 ), #67340, .T. ) ;
#99223=AXIS2_PLACEMENT_3D ( 'NONE', #19233, #77216, #63489 ) ;
#99235=CYLINDRICAL_SURFACE ( 'NONE', #56107, 2.500000000000000444 ) ;
#99242=ORIENTED_EDGE ( 'NONE', *, *, #137486, .T. ) ;
#99252=ORIENTED_EDGE ( 'NONE', *, *, #34013, .T. ) ;
#99308=CARTESIAN_POINT ( 'NONE',  ( 9.208651418775088970, 4.584330080086930965E-16, 0.000000000000000000 ) ) ;
#99309=LINE ( 'NONE', #10865, #48734 ) ;
#99312=CARTESIAN_POINT ( 'NONE',  ( 3.872664058232598183, 3.821174125832445049E-16, 0.000000000000000000 ) ) ;
#99330=ORIENTED_EDGE ( 'NONE', *, *, #24406, .T. ) ;
#99341=DIRECTION ( 'NONE',  ( 0.000000000000000000, -1.000000000000000000, 0.000000000000000000 ) ) ;
#99350=CARTESIAN_POINT ( 'NONE',  ( -12.69999999999998153, 3.061616997868383634E-16, -2.500000000000000444 ) ) ;
#99432=EDGE_LOOP ( 'NONE', ( #96136, #18481 ) ) ;
#99442=CARTESIAN_POINT ( 'NONE',  ( 16.44013779566152778, 3.821174125832445049E-16, 0.000000000000000000 ) ) ;
#99450=ORIENTED_EDGE ( 'NONE', *, *, #8329, .F. ) ;
#99466=VERTEX_POINT ( 'NONE', #6284 ) ;
#99491=CARTESIAN_POINT ( 'NONE',  ( 0.4644480930543400943, -0.3999999999999997446, -2.317232462839659224 ) ) ;
#99504=CARTESIAN_POINT ( 'NONE',  ( 7.014532492589830248, 2.500000000000000444, 3.061616997868383634E-16 ) ) ;
#99588=ORIENTED_EDGE ( 'NONE', *, *, #57629, .T. ) ;
#99589=EDGE_CURVE ( 'NONE', #110816, #75950, #19361, .T. ) ;
#99597=DIRECTION ( 'NONE',  ( -1.000000000000000000, -1.224606353822377258E-16, -0.000000000000000000 ) ) ;
#99603=DIRECTION ( 'NONE',  ( -1.000000000000000000, -1.224606353822377258E-16, -0.000000000000000000 ) ) ;
#99659=EDGE_CURVE ( 'NONE', #121565, #38043, #104591, .T. ) ;
#99685=EDGE_CURVE ( 'NONE', #57414, #93303, #116183, .T. ) ;
#99699=CIRCLE ( 'NONE', #129822, 2.500000000000000444 ) ;
#99710=ORIENTED_EDGE ( 'NONE', *, *, #135299, .F. ) ;
#99728=DIRECTION ( 'NONE',  ( 1.000000000000000000, 0.000000000000000000, 0.000000000000000000 ) ) ;
#99739=CONICAL_SURFACE ( 'NONE', #136790, 2.500000000000000444, 0.9599310885968830309 ) ;
#99772=FACE_OUTER_BOUND ( 'NONE', #86240, .T. ) ;
#99776=ORIENTED_EDGE ( 'NONE', *, *, #17042, .T. ) ;
#99779=ORIENTED_EDGE ( 'NONE', *, *, #69462, .F. ) ;
#99791=EDGE_CURVE ( 'NONE', #48215, #142779, #57022, .T. ) ;
#99793=AXIS2_PLACEMENT_3D ( 'NONE', #82329, #70752, #126511 ) ;
#99800=B_SPLINE_CURVE_WITH_KNOTS ( 'NONE', 3,
 ( #18061, #15220, #6462, #48600 ),
 .UNSPECIFIED., .F., .F.,
 ( 4, 4 ),
 ( 0.008853860144884201713, 0.009403245473020212589 ),
 .UNSPECIFIED. ) ;
#99814=DIRECTION ( 'NONE',  ( 0.000000000000000000, -1.000000000000000000, 0.000000000000000000 ) ) ;
#99873=CARTESIAN_POINT ( 'NONE',  ( 18.32266436734346726, 2.055000000000001048, 0.000000000000000000 ) ) ;
#99884=CARTESIAN_POINT ( 'NONE',  ( 13.60986171580761805, -2.055000000000000160, 0.000000000000000000 ) ) ;
#99902=CYLINDRICAL_SURFACE ( 'NONE', #68868, 2.500000000000000444 ) ;
#99906=AXIS2_PLACEMENT_3D ( 'NONE', #132498, #66500, #110664 ) ;
#100025=CARTESIAN_POINT ( 'NONE',  ( 8.111591955682463606, 4.202752102959690472E-16, 0.000000000000000000 ) ) ;
#100030=AXIS2_PLACEMENT_3D ( 'NONE', #46050, #67821, #100417 ) ;
#100115=CIRCLE ( 'NONE', #141721, 2.055000000000000604 ) ;
#100125=CIRCLE ( 'NONE', #86265, 2.500000000000000444 ) ;
#100219=CARTESIAN_POINT ( 'NONE',  ( 12.51280225271498736, 3.821174125832445049E-16, 0.000000000000000000 ) ) ;
#100237=DIRECTION ( 'NONE',  ( 0.000000000000000000, 0.000000000000000000, 1.000000000000000000 ) ) ;
#100290=CARTESIAN_POINT ( 'NONE',  ( 15.18079593298623564, -2.055000000000000160, 0.000000000000000000 ) ) ;
#100322=AXIS2_PLACEMENT_3D ( 'NONE', #89961, #134214, #57380 ) ;
#100329=CARTESIAN_POINT ( 'NONE',  ( 9.682526172861077640, 4.202752102959690472E-16, 0.000000000000000000 ) ) ;
#100339=ORIENTED_EDGE ( 'NONE', *, *, #5206, .F. ) ;
#100370=FACE_OUTER_BOUND ( 'NONE', #134737, .T. ) ;
#100372=DIRECTION ( 'NONE',  ( 0.000000000000000000, -1.000000000000000000, 0.000000000000000000 ) ) ;
#100405=AXIS2_PLACEMENT_3D ( 'NONE', #9001, #54032, #32248 ) ;
#100415=ORIENTED_EDGE ( 'NONE', *, *, #22440, .T. ) ;
#100416=CARTESIAN_POINT ( 'NONE',  ( 14.70692117890024697, 4.584330080086930965E-16, 0.000000000000000000 ) ) ;
#100417=DIRECTION ( 'NONE',  ( 0.000000000000000000, -1.000000000000000000, 0.000000000000000000 ) ) ;
#100456=FACE_OUTER_BOUND ( 'NONE', #22491, .T. ) ;
#100503=EDGE_CURVE ( 'NONE', #14737, #137211, #80388, .T. ) ;
#100508=DIRECTION ( 'NONE',  ( 1.000000000000000000, 1.224606353822377258E-16, 0.000000000000000000 ) ) ;
#100570=CARTESIAN_POINT ( 'NONE',  ( -12.69999999999998153, 0.000000000000000000, 0.000000000000000000 ) ) ;
#100629=EDGE_CURVE ( 'NONE', #71583, #122249, #8459, .T. ) ;
#100735=CARTESIAN_POINT ( 'NONE',  ( 8.897059064271770623, -2.055000000000000160, 2.789133085058097101E-16 ) ) ;
#100736=ORIENTED_EDGE ( 'NONE', *, *, #60935, .T. ) ;
#100742=CARTESIAN_POINT ( 'NONE',  ( 4.184256412735922304, -2.055000000000000160, 0.000000000000000000 ) ) ;
#100777=CARTESIAN_POINT ( 'NONE',  ( -12.69999999999998153, 3.061616997868383634E-16, -2.500000000000000444 ) ) ;
#100784=FACE_OUTER_BOUND ( 'NONE', #56134, .T. ) ;
#100788=ORIENTED_EDGE ( 'NONE', *, *, #65154, .F. ) ;
#100880=CARTESIAN_POINT ( 'NONE',  ( 19.10813147593277250, 2.055000000000001048, 0.000000000000000000 ) ) ;
#100894=ORIENTED_EDGE ( 'NONE', *, *, #99685, .T. ) ;
#100897=FACE_OUTER_BOUND ( 'NONE', #57953, .T. ) ;
#100906=DIRECTION ( 'NONE',  ( -1.000000000000000000, -1.224606353822377258E-16, -0.000000000000000000 ) ) ;
#100923=ORIENTED_EDGE ( 'NONE', *, *, #10751, .T. ) ;
#100987=CARTESIAN_POINT ( 'NONE',  ( 1.629999999999999893, -0.3999999999999997446, -2.303088455023527104 ) ) ;
#101016=CARTESIAN_POINT ( 'NONE',  ( 1.629999999999999893, 0.3999999999999995226, 2.303088455023526215 ) ) ;
#101019=LINE ( 'NONE', #56863, #127969 ) ;
#101022=AXIS2_PLACEMENT_3D ( 'NONE', #101094, #123608, #58375 ) ;
#101048=ORIENTED_EDGE ( 'NONE', *, *, #35578, .T. ) ;
#101055=CARTESIAN_POINT ( 'NONE',  ( -12.69999999999998153, 0.000000000000000000, 2.500000000000000444 ) ) ;
#101094=CARTESIAN_POINT ( 'NONE',  ( 3.087196949643289834, 3.821174125832445049E-16, 0.000000000000000000 ) ) ;
#101123=DIRECTION ( 'NONE',  ( 0.5735764363510448272, -0.8191520442889927978, 1.003171929053526103E-16 ) ) ;
#101127=ORIENTED_EDGE ( 'NONE', *, *, #40098, .T. ) ;
#101148=DIRECTION ( 'NONE',  ( 0.000000000000000000, -1.000000000000000000, 0.000000000000000000 ) ) ;
#101181=ORIENTED_EDGE ( 'NONE', *, *, #71622, .T. ) ;
#101250=ADVANCED_FACE ( 'NONE', ( #68467 ), #12372, .T. ) ;
#101258=EDGE_CURVE ( 'NONE', #118938, #119988, #93413, .T. ) ;
#101261=DIRECTION ( 'NONE',  ( 0.000000000000000000, 0.000000000000000000, 1.000000000000000000 ) ) ;
#101266=ORIENTED_EDGE ( 'NONE', *, *, #77670, .T. ) ;
#101282=DIRECTION ( 'NONE',  ( 1.000000000000000000, 1.224606353822377258E-16, 0.000000000000000000 ) ) ;
#101287=ORIENTED_EDGE ( 'NONE', *, *, #30985, .T. ) ;
#101305=FACE_OUTER_BOUND ( 'NONE', #17410, .T. ) ;
#101322=ORIENTED_EDGE ( 'NONE', *, *, #47590, .T. ) ;
#101351=( LENGTH_UNIT ( ) NAMED_UNIT ( * ) SI_UNIT ( .MILLI., .METRE. ) );
#101415=ADVANCED_FACE ( 'NONE', ( #35114 ), #142180, .T. ) ;
#101421=ORIENTED_EDGE ( 'NONE', *, *, #132071, .T. ) ;
#101433=DIRECTION ( 'NONE',  ( 0.000000000000000000, -1.000000000000000000, 0.000000000000000000 ) ) ;
#101437=EDGE_CURVE ( 'NONE', #38444, #80430, #123664, .T. ) ;
#101441=DIRECTION ( 'NONE',  ( -0.5735764363510499342, -0.8191520442889891340, 0.000000000000000000 ) ) ;
#101443=VERTEX_POINT ( 'NONE', #83617 ) ;
#101472=AXIS2_PLACEMENT_3D ( 'NONE', #78040, #123694, #57013 ) ;
#101473=AXIS2_PLACEMENT_3D ( 'NONE', #136187, #112315, #102866 ) ;
#101498=DIRECTION ( 'NONE',  ( -1.000000000000000000, -1.224606353822377258E-16, -0.000000000000000000 ) ) ;
#101513=CARTESIAN_POINT ( 'NONE',  ( 22.25000000000000000, 0.000000000000000000, 1.749999999999999778 ) ) ;
#101516=EDGE_LOOP ( 'NONE', ( #107939, #4945, #75113, #33215 ) ) ;
#101518=CARTESIAN_POINT ( 'NONE',  ( 1.516262732464673579, 0.4000000000000001887, -2.467792535850613866 ) ) ;
#101539=ORIENTED_EDGE ( 'NONE', *, *, #102888, .F. ) ;
#101566=ORIENTED_EDGE ( 'NONE', *, *, #5281, .T. ) ;
#101577=ORIENTED_EDGE ( 'NONE', *, *, #93811, .T. ) ;
#101659=DIRECTION ( 'NONE',  ( -1.000000000000000000, -0.000000000000000000, -0.000000000000000000 ) ) ;
#101675=VECTOR ( 'NONE', #81616, 1000.000000000000000 ) ;
#101676=AXIS2_PLACEMENT_3D ( 'NONE', #136310, #36995, #130328 ) ;
#101691=DIRECTION ( 'NONE',  ( -1.000000000000000000, -1.224606353822377258E-16, -0.000000000000000000 ) ) ;
#101702=AXIS2_PLACEMENT_3D ( 'NONE', #90067, #58226, #24121 ) ;
#101719=CARTESIAN_POINT ( 'NONE',  ( 8.585466709768445170, 3.821174125832445049E-16, 0.000000000000000000 ) ) ;
#101725=ORIENTED_EDGE ( 'NONE', *, *, #81653, .F. ) ;
#101736=AXIS2_PLACEMENT_3D ( 'NONE', #849, #56735, #21908 ) ;
#101752=VERTEX_POINT ( 'NONE', #100880 ) ;
#101768=DIRECTION ( 'NONE',  ( 0.000000000000000000, -1.000000000000000000, 0.000000000000000000 ) ) ;
#101811=DIRECTION ( 'NONE',  ( -1.000000000000000000, -0.000000000000000000, -0.000000000000000000 ) ) ;
#101816=DIRECTION ( 'NONE',  ( 0.000000000000000000, 1.000000000000000000, 0.000000000000000000 ) ) ;
#101818=CONICAL_SURFACE ( 'NONE', #6771, 2.055000000000000604, 0.9599310885968764806 ) ;
#101825=CONICAL_SURFACE ( 'NONE', #106438, 2.500000000000000444, 0.9599310885968830309 ) ;
#101841=CYLINDRICAL_SURFACE ( 'NONE', #116912, 2.500000000000000444 ) ;
#101846=CARTESIAN_POINT ( 'NONE',  ( 6.066782984417857350, 4.584330080086930965E-16, 0.000000000000000000 ) ) ;
#101865=EDGE_LOOP ( 'NONE', ( #131277, #124914, #17267, #21932 ) ) ;
#101866=CARTESIAN_POINT ( 'NONE',  ( -12.69999999999998153, 3.061616997868383634E-16, -2.500000000000000444 ) ) ;
#101876=VERTEX_POINT ( 'NONE', #19948 ) ;
#101877=CARTESIAN_POINT ( 'NONE',  ( 5.281315875828549444, 4.584330080086930965E-16, 0.000000000000000000 ) ) ;
#101882=CIRCLE ( 'NONE', #39401, 2.500000000000000444 ) ;
#101898=ORIENTED_EDGE ( 'NONE', *, *, #29920, .T. ) ;
#101959=EDGE_LOOP ( 'NONE', ( #96627, #67238, #101287, #18286, #60212 ) ) ;
#101977=AXIS2_PLACEMENT_3D ( 'NONE', #142053, #107243, #42741 ) ;
#102015=FACE_OUTER_BOUND ( 'NONE', #91769, .T. ) ;
#102047=VERTEX_POINT ( 'NONE', #10494 ) ;
#102048=DIRECTION ( 'NONE',  ( 0.5735764363510444941, 0.8191520442889929088, 0.000000000000000000 ) ) ;
#102071=CONICAL_SURFACE ( 'NONE', #118178, 2.055000000000000604, 0.9599310885968764806 ) ;
#102075=EDGE_CURVE ( 'NONE', #72701, #38008, #86279, .T. ) ;
#102077=FILL_AREA_STYLE ('',( #91228 ) ) ;
#102107=CARTESIAN_POINT ( 'NONE',  ( 1.042387978378689573, 4.202752102959690472E-16, 0.000000000000000000 ) ) ;
#102132=DIRECTION ( 'NONE',  ( 0.000000000000000000, -1.000000000000000000, 0.000000000000000000 ) ) ;
#102172=CIRCLE ( 'NONE', #39680, 2.055000000000000604 ) ;
#102185=DIRECTION ( 'NONE',  ( -0.5735764363510501562, 0.8191520442889890230, 1.003171929053521419E-16 ) ) ;
#102214=CIRCLE ( 'NONE', #30488, 2.500000000000000444 ) ;
#102232=LINE ( 'NONE', #89202, #114823 ) ;
#102289=CARTESIAN_POINT ( 'NONE',  ( 0.2569208697893812232, 2.055000000000001048, 0.000000000000000000 ) ) ;
#102294=AXIS2_PLACEMENT_3D ( 'NONE', #103260, #16224, #70684 ) ;
#102309=DIRECTION ( 'NONE',  ( -1.000000000000000000, -1.224606353822377258E-16, -0.000000000000000000 ) ) ;
#102371=VECTOR ( 'NONE', #62852, 1000.000000000000000 ) ;
#102396=EDGE_LOOP ( 'NONE', ( #117551, #37928, #21549, #75189, #137399 ) ) ;
#102495=CIRCLE ( 'NONE', #114057, 2.500000000000000444 ) ;
#102519=DIRECTION ( 'NONE',  ( 0.5735764363510444941, 0.8191520442889929088, 0.000000000000000000 ) ) ;
#102522=VECTOR ( 'NONE', #1253, 1000.000000000000000 ) ;
#102531=EDGE_CURVE ( 'NONE', #76190, #66627, #57441, .T. ) ;
#102541=EDGE_LOOP ( 'NONE', ( #131431, #7994, #76915, #34552, #82441 ) ) ;
#102578=DIRECTION ( 'NONE',  ( -1.000000000000000000, -0.000000000000000000, -0.000000000000000000 ) ) ;
#102592=CARTESIAN_POINT ( 'NONE',  ( 10.46799328145038821, 4.202752102959690472E-16, 0.000000000000000000 ) ) ;
#102596=LINE ( 'NONE', #67854, #134126 ) ;
#102602=ORIENTED_EDGE ( 'NONE', *, *, #104229, .T. ) ;
#102619=ORIENTED_EDGE ( 'NONE', *, *, #122358, .F. ) ;
#102672=CONICAL_SURFACE ( 'NONE', #19351, 2.055000000000000604, 0.9599310885968764806 ) ;
#102677=CYLINDRICAL_SURFACE ( 'NONE', #97024, 2.500000000000000444 ) ;
#102704=AXIS2_PLACEMENT_3D ( 'NONE', #133308, #78933, #23059 ) ;
#102730=CARTESIAN_POINT ( 'NONE',  ( 13.92145407031093818, -2.500000000000000444, 3.061616997868384127E-16 ) ) ;
#102742=DIRECTION ( 'NONE',  ( 0.5735764363510448272, -0.8191520442889927978, 1.003171929053526103E-16 ) ) ;
#102743=VERTEX_POINT ( 'NONE', #126934 ) ;
#102748=CARTESIAN_POINT ( 'NONE',  ( -12.69999999999998153, 0.000000000000000000, 2.500000000000000444 ) ) ;
#102754=LINE ( 'NONE', #56436, #62807 ) ;
#102773=LINE ( 'NONE', #12169, #85659 ) ;
#102791=EDGE_CURVE ( 'NONE', #101876, #7107, #70275, .T. ) ;
#102793=VERTEX_POINT ( 'NONE', #40671 ) ;
#102866=DIRECTION ( 'NONE',  ( 0.000000000000000000, -1.000000000000000000, 0.000000000000000000 ) ) ;
#102888=EDGE_CURVE ( 'NONE', #23831, #60214, #35600, .T. ) ;
#102892=LINE ( 'NONE', #34786, #74478 ) ;
#102916=ORIENTED_EDGE ( 'NONE', *, *, #108372, .F. ) ;
#102940=CIRCLE ( 'NONE', #98285, 2.500000000000000444 ) ;
#102996=ORIENTED_EDGE ( 'NONE', *, *, #64819, .F. ) ;
#103021=CIRCLE ( 'NONE', #42818, 2.500000000000000444 ) ;
#103049=VERTEX_POINT ( 'NONE', #82570 ) ;
#103071=EDGE_CURVE ( 'NONE', #133129, #121565, #13005, .T. ) ;
#103111=DIRECTION ( 'NONE',  ( -1.000000000000000000, -1.224606353822377258E-16, -0.000000000000000000 ) ) ;
#103115=CARTESIAN_POINT ( 'NONE',  ( 1.353980332882009252, 0.3999999999999995226, 2.467792535850613866 ) ) ;
#103117=DIRECTION ( 'NONE',  ( 1.734723475976806848E-16, -1.000000000000000000, 0.000000000000000000 ) ) ;
#103124=DIRECTION ( 'NONE',  ( -1.000000000000000000, -1.224606353822377258E-16, -0.000000000000000000 ) ) ;
#103170=ORIENTED_EDGE ( 'NONE', *, *, #127229, .F. ) ;
#103171=EDGE_LOOP ( 'NONE', ( #88753, #136273, #130403, #67508, #39727 ) ) ;
#103187=DIRECTION ( 'NONE',  ( -1.734723475976806848E-16, 1.000000000000000000, 0.000000000000000000 ) ) ;
#103246=CONICAL_SURFACE ( 'NONE', #24498, 2.055000000000000604, 0.9599310885968764806 ) ;
#103260=CARTESIAN_POINT ( 'NONE',  ( 10.94186803553636977, 3.821174125832445049E-16, 0.000000000000000000 ) ) ;
#103276=EDGE_CURVE ( 'NONE', #89141, #51035, #966, .T. ) ;
#103286=VECTOR ( 'NONE', #73007, 1000.000000000000000 ) ;
#103291=DIRECTION ( 'NONE',  ( 0.000000000000000000, 1.000000000000000000, 0.000000000000000000 ) ) ;
#103293=DIRECTION ( 'NONE',  ( 0.000000000000000000, 1.000000000000000000, 0.000000000000000000 ) ) ;
#103339=VERTEX_POINT ( 'NONE', #87564 ) ;
#103360=ORIENTED_EDGE ( 'NONE', *, *, #43739, .T. ) ;
#103361=DIRECTION ( 'NONE',  ( -1.000000000000000000, -1.224606353822377258E-16, -0.000000000000000000 ) ) ;
#103375=CIRCLE ( 'NONE', #29304, 2.500000000000000444 ) ;
#103386=AXIS2_PLACEMENT_3D ( 'NONE', #142155, #140685, #108036 ) ;
#103464=VERTEX_POINT ( 'NONE', #80982 ) ;
#103493=ADVANCED_FACE ( 'NONE', ( #12833 ), #57109, .T. ) ;
#103502=ORIENTED_EDGE ( 'NONE', *, *, #39621, .F. ) ;
#103520=DIRECTION ( 'NONE',  ( 0.000000000000000000, 0.000000000000000000, 1.000000000000000000 ) ) ;
#103531=AXIS2_PLACEMENT_3D ( 'NONE', #28631, #72883, #51088 ) ;
#103538=EDGE_LOOP ( 'NONE', ( #99054, #84144, #113654, #61616, #473 ) ) ;
#103560=VERTEX_POINT ( 'NONE', #130007 ) ;
#103585=DIRECTION ( 'NONE',  ( -1.000000000000000000, -1.224606353822377258E-16, -0.000000000000000000 ) ) ;
#103607=CARTESIAN_POINT ( 'NONE',  ( 13.60986171580761805, 4.202752102959690472E-16, 0.000000000000000000 ) ) ;
#103616=ORIENTED_EDGE ( 'NONE', *, *, #69478, .F. ) ;
#103627=CARTESIAN_POINT ( 'NONE',  ( 15.49238828748955576, 4.584330080086930965E-16, 0.000000000000000000 ) ) ;
#103649=EDGE_CURVE ( 'NONE', #138500, #83589, #62623, .T. ) ;
#103660=CIRCLE ( 'NONE', #43574, 2.500000000000000444 ) ;
#103725=EDGE_CURVE ( 'NONE', #50807, #132555, #13192, .T. ) ;
#103746=CARTESIAN_POINT ( 'NONE',  ( 15.49238828748955576, 0.000000000000000000, 2.500000000000000444 ) ) ;
#103754=VERTEX_POINT ( 'NONE', #112534 ) ;
#103783=ORIENTED_EDGE ( 'NONE', *, *, #63946, .F. ) ;
#103820=CIRCLE ( 'NONE', #13593, 2.500000000000000444 ) ;
#103855=CIRCLE ( 'NONE', #111114, 2.055000000000000604 ) ;
#103876=CARTESIAN_POINT ( 'NONE',  ( 7.799999601179139042, 3.821174125832445049E-16, 0.000000000000000000 ) ) ;
#103955=AXIS2_PLACEMENT_3D ( 'NONE', #20505, #130013, #52436 ) ;
#103957=DIRECTION ( 'NONE',  ( 0.5735764363510444941, 0.8191520442889929088, 0.000000000000000000 ) ) ;
#104001=PRODUCT_CONTEXT ( 'NONE', #69885, 'mechanical' ) ;
#104015=CYLINDRICAL_SURFACE ( 'NONE', #75604, 2.500000000000000444 ) ;
#104053=AXIS2_PLACEMENT_3D ( 'NONE', #60712, #93992, #117165 ) ;
#104061=CONICAL_SURFACE ( 'NONE', #55477, 2.055000000000000604, 0.9599310885968764806 ) ;
#104083=PLANE ( 'NONE',  #68583 ) ;
#104157=CARTESIAN_POINT ( 'NONE',  ( 13.13598696172163116, 2.500000000000000888, 0.000000000000000000 ) ) ;
#104167=AXIS2_PLACEMENT_3D ( 'NONE', #39033, #83256, #128886 ) ;
#104178=ORIENTED_EDGE ( 'NONE', *, *, #36836, .T. ) ;
#104199=ORIENTED_EDGE ( 'NONE', *, *, #68580, .F. ) ;
#104200=EDGE_CURVE ( 'NONE', #129512, #25493, #68201, .T. ) ;
#104229=EDGE_CURVE ( 'NONE', #20849, #26888, #79803, .T. ) ;
#104254=CARTESIAN_POINT ( 'NONE',  ( 11.56505274454301357, 4.584330080086930965E-16, 0.000000000000000000 ) ) ;
#104401=CARTESIAN_POINT ( 'NONE',  ( 12.35051985313232237, 4.584330080086930965E-16, 0.000000000000000000 ) ) ;
#104406=AXIS2_PLACEMENT_3D ( 'NONE', #73809, #85378, #41168 ) ;
#104418=VERTEX_POINT ( 'NONE', #18733 ) ;
#104460=VERTEX_POINT ( 'NONE', #75302 ) ;
#104471=CARTESIAN_POINT ( 'NONE',  ( -12.69999999999998153, 3.061616997868383634E-16, -2.500000000000000444 ) ) ;
#104477=DIRECTION ( 'NONE',  ( 1.318980745116185161E-16, -1.000000000000000000, 0.000000000000000000 ) ) ;
#104482=AXIS2_PLACEMENT_3D ( 'NONE', #94927, #5767, #94222 ) ;
#104508=FACE_OUTER_BOUND ( 'NONE', #126498, .T. ) ;
#104517=ORIENTED_EDGE ( 'NONE', *, *, #142595, .F. ) ;
#104544=DIRECTION ( 'NONE',  ( 0.000000000000000000, -1.000000000000000000, 0.000000000000000000 ) ) ;
#104552=EDGE_CURVE ( 'NONE', #117065, #83522, #49856, .T. ) ;
#104555=ORIENTED_EDGE ( 'NONE', *, *, #89446, .F. ) ;
#104562=CARTESIAN_POINT ( 'NONE',  ( -12.69999999999998153, 0.000000000000000000, 0.000000000000000000 ) ) ;
#104564=CARTESIAN_POINT ( 'NONE',  ( 16.44013779566152778, -2.499999999999996447, 0.000000000000000000 ) ) ;
#104578=DIRECTION ( 'NONE',  ( -1.000000000000000000, -1.224606353822377258E-16, -0.000000000000000000 ) ) ;
#104591=CIRCLE ( 'NONE', #97652, 2.500000000000000444 ) ;
#104596=CIRCLE ( 'NONE', #76906, 2.055000000000000604 ) ;
#104605=ORIENTED_EDGE ( 'NONE', *, *, #117775, .T. ) ;
#104624=EDGE_LOOP ( 'NONE', ( #140757, #3623, #61420, #130527, #99252 ) ) ;
#104651=AXIS2_PLACEMENT_3D ( 'NONE', #141578, #100906, #133556 ) ;
#104653=VECTOR ( 'NONE', #8573, 1000.000000000000000 ) ;
#104657=AXIS2_PLACEMENT_3D ( 'NONE', #5935, #137219, #136482 ) ;
#104666=CIRCLE ( 'NONE', #132454, 2.500000000000000444 ) ;
#104671=CARTESIAN_POINT ( 'NONE',  ( 15.96626304157554266, 2.055000000000001048, 0.000000000000000000 ) ) ;
#104713=EDGE_CURVE ( 'NONE', #83589, #130990, #103021, .T. ) ;
#104716=VERTEX_POINT ( 'NONE', #69425 ) ;
#104722=DIRECTION ( 'NONE',  ( -0.5735764363510501562, 0.8191520442889890230, 1.003171929053521419E-16 ) ) ;
#104727=CARTESIAN_POINT ( 'NONE',  ( -12.69999999999998153, 0.000000000000000000, 0.000000000000000000 ) ) ;
#104746=VERTEX_POINT ( 'NONE', #125938 ) ;
#104765=DIRECTION ( 'NONE',  ( 0.000000000000000000, 0.000000000000000000, 1.000000000000000000 ) ) ;
#104803=ORIENTED_EDGE ( 'NONE', *, *, #11425, .F. ) ;
#104815=FACE_OUTER_BOUND ( 'NONE', #96754, .T. ) ;
#104842=ORIENTED_EDGE ( 'NONE', *, *, #29587, .F. ) ;
#104846=ORIENTED_EDGE ( 'NONE', *, *, #56937, .T. ) ;
#104892=VECTOR ( 'NONE', #121934, 1000.000000000000000 ) ;
#104897=CARTESIAN_POINT ( 'NONE',  ( 19.89359858452208130, 2.055000000000001048, 0.000000000000000000 ) ) ;
#104903=AXIS2_PLACEMENT_3D ( 'NONE', #137995, #116937, #62579 ) ;
#105012=CARTESIAN_POINT ( 'NONE',  ( -12.69999999999998153, 3.061616997868383634E-16, -2.500000000000000444 ) ) ;
#105023=DIRECTION ( 'NONE',  ( -1.000000000000000000, -0.000000000000000000, -0.000000000000000000 ) ) ;
#105041=CIRCLE ( 'NONE', #3202, 2.500000000000000444 ) ;
#105067=ORIENTED_EDGE ( 'NONE', *, *, #43304, .T. ) ;
#105086=CARTESIAN_POINT ( 'NONE',  ( -12.69999999999998153, 0.000000000000000000, 0.000000000000000000 ) ) ;
#105122=AXIS2_PLACEMENT_3D ( 'NONE', #86247, #130470, #64481 ) ;
#105139=AXIS2_PLACEMENT_3D ( 'NONE', #12270, #78998, #143498 ) ;
#105198=LINE ( 'NONE', #4390, #52952 ) ;
#105199=DIRECTION ( 'NONE',  ( -1.000000000000000000, -0.000000000000000000, -0.000000000000000000 ) ) ;
#105234=CARTESIAN_POINT ( 'NONE',  ( -12.69999999999998153, 0.000000000000000000, 2.500000000000000444 ) ) ;
#105245=CARTESIAN_POINT ( 'NONE',  ( 0.1161069444170876042, 0.3999999999999995781, 2.220360628129161906 ) ) ;
#105255=FACE_OUTER_BOUND ( 'NONE', #5758, .T. ) ;
#105366=ADVANCED_FACE ( 'NONE', ( #119839 ), #66095, .T. ) ;
#105369=VERTEX_POINT ( 'NONE', #90662 ) ;
#105390=ORIENTED_EDGE ( 'NONE', *, *, #111033, .F. ) ;
#105397=ORIENTED_EDGE ( 'NONE', *, *, #39277, .T. ) ;
#105420=ADVANCED_FACE ( 'NONE', ( #141640 ), #75396, .T. ) ;
#105467=ADVANCED_FACE ( 'NONE', ( #91379 ), #36091, .T. ) ;
#105507=EDGE_CURVE ( 'NONE', #140149, #37103, #92048, .T. ) ;
#105547=CARTESIAN_POINT ( 'NONE',  ( 6.229065384000522343, 3.821174125832445049E-16, 0.000000000000000000 ) ) ;
#105581=ORIENTED_EDGE ( 'NONE', *, *, #53298, .T. ) ;
#105645=FACE_OUTER_BOUND ( 'NONE', #10570, .T. ) ;
#105686=AXIS2_PLACEMENT_3D ( 'NONE', #34510, #78739, #122954 ) ;
#105703=CIRCLE ( 'NONE', #6139, 2.500000000000000444 ) ;
#105708=DIRECTION ( 'NONE',  ( -1.000000000000000000, -1.224606353822377258E-16, -0.000000000000000000 ) ) ;
#105755=ADVANCED_FACE ( 'NONE', ( #92503 ), #104083, .F. ) ;
#105828=CARTESIAN_POINT ( 'NONE',  ( 8.423184310185783730, 4.584330080086930965E-16, 0.000000000000000000 ) ) ;
#105836=ORIENTED_EDGE ( 'NONE', *, *, #55482, .T. ) ;
#105860=CARTESIAN_POINT ( 'NONE',  ( 1.516262732464673579, 0.3999999999999995226, 2.467792535850613866 ) ) ;
#105905=DIRECTION ( 'NONE',  ( -1.000000000000000000, -1.224606353822377258E-16, -0.000000000000000000 ) ) ;
#105942=CARTESIAN_POINT ( 'NONE',  ( -12.69999999999998153, 0.000000000000000000, 0.000000000000000000 ) ) ;
#105981=VECTOR ( 'NONE', #28281, 1000.000000000000000 ) ;
#105984=CARTESIAN_POINT ( 'NONE',  ( 11.56505274454301357, 2.500000000000000888, 0.000000000000000000 ) ) ;
#106025=CARTESIAN_POINT ( 'NONE',  ( -12.69999999999998153, 0.000000000000000000, 2.500000000000000444 ) ) ;
#106043=DIRECTION ( 'NONE',  ( 1.734723475976806848E-16, -1.000000000000000000, 0.000000000000000000 ) ) ;
#106097=VECTOR ( 'NONE', #131200, 1000.000000000000000 ) ;
#106152=CONICAL_SURFACE ( 'NONE', #99223, 2.500000000000000444, 0.9599310885968830309 ) ;
#106173=ADVANCED_FACE ( 'NONE', ( #106893 ), #104015, .T. ) ;
#106194=ORIENTED_EDGE ( 'NONE', *, *, #77196, .F. ) ;
#106240=DIRECTION ( 'NONE',  ( 1.734723475976806848E-16, -1.000000000000000000, 0.000000000000000000 ) ) ;
#106256=EDGE_CURVE ( 'NONE', #11616, #102743, #57099, .T. ) ;
#106263=ORIENTED_EDGE ( 'NONE', *, *, #72980, .T. ) ;
#106270=DIRECTION ( 'NONE',  ( 2.110369192185896011E-16, -1.000000000000000000, 0.000000000000000000 ) ) ;
#106296=CONICAL_SURFACE ( 'NONE', #124864, 2.500000000000000444, 0.9599310885968830309 ) ;
#106309=AXIS2_PLACEMENT_3D ( 'NONE', #131786, #119441, #75276 ) ;
#106344=VECTOR ( 'NONE', #106815, 1000.000000000000000 ) ;
#106353=CARTESIAN_POINT ( 'NONE',  ( 20.36747333860806819, 3.821174125832445049E-16, 0.000000000000000000 ) ) ;
#106357=VERTEX_POINT ( 'NONE', #57550 ) ;
#106418=CARTESIAN_POINT ( 'NONE',  ( -12.69999999999998153, 0.000000000000000000, 0.000000000000000000 ) ) ;
#106438=AXIS2_PLACEMENT_3D ( 'NONE', #34658, #113622, #25183 ) ;
#106445=CARTESIAN_POINT ( 'NONE',  ( 21.66240673564756491, 0.000000000000000000, 0.000000000000000000 ) ) ;
#106463=VERTEX_POINT ( 'NONE', #1668 ) ;
#106472=EDGE_LOOP ( 'NONE', ( #127428, #107813, #26321, #3145, #80289 ) ) ;
#106479=CYLINDRICAL_SURFACE ( 'NONE', #29448, 2.500000000000000444 ) ;
#106499=CONICAL_SURFACE ( 'NONE', #2295, 2.500000000000000444, 0.9599310885968830309 ) ;
#106554=ORIENTED_EDGE ( 'NONE', *, *, #91991, .T. ) ;
#106560=CARTESIAN_POINT ( 'NONE',  ( 4.658131166821905644, 3.821174125832445049E-16, 0.000000000000000000 ) ) ;
#106567=ORIENTED_EDGE ( 'NONE', *, *, #58918, .T. ) ;
#106575=CARTESIAN_POINT ( 'NONE',  ( 7.637717201596474048, 2.500000000000000888, 0.000000000000000000 ) ) ;
#106586=DIRECTION ( 'NONE',  ( -1.000000000000000000, -0.000000000000000000, -0.000000000000000000 ) ) ;
#106597=ORIENTED_EDGE ( 'NONE', *, *, #74348, .T. ) ;
#106601=AXIS2_PLACEMENT_3D ( 'NONE', #44507, #45225, #88708 ) ;
#106614=AXIS2_PLACEMENT_3D ( 'NONE', #9923, #23662, #98382 ) ;
#106667=DIRECTION ( 'NONE',  ( -1.000000000000000000, -1.224606353822377258E-16, -0.000000000000000000 ) ) ;
#106691=AXIS2_PLACEMENT_3D ( 'NONE', #29613, #28923, #62280 ) ;
#106705=CIRCLE ( 'NONE', #44263, 2.500000000000000444 ) ;
#106752=CIRCLE ( 'NONE', #72045, 2.055000000000000604 ) ;
#106762=AXIS2_PLACEMENT_3D ( 'NONE', #100219, #88639, #133566 ) ;
#106765=DIRECTION ( 'NONE',  ( 1.000000000000000000, 1.224606353822377258E-16, 0.000000000000000000 ) ) ;
#106769=EDGE_CURVE ( 'NONE', #29345, #103464, #84907, .T. ) ;
#106783=VECTOR ( 'NONE', #133210, 1000.000000000000000 ) ;
#106792=VECTOR ( 'NONE', #131947, 999.9999999999998863 ) ;
#106803=CONICAL_SURFACE ( 'NONE', #136934, 2.055000000000000604, 0.9599310885968764806 ) ;
#106815=DIRECTION ( 'NONE',  ( 0.5735764363510444941, 0.8191520442889929088, 0.000000000000000000 ) ) ;
#106838=DIRECTION ( 'NONE',  ( -0.5735764363510499342, -0.8191520442889891340, 0.000000000000000000 ) ) ;
#106846=CARTESIAN_POINT ( 'NONE',  ( 1.516262732464673579, -0.4000000000000004108, 2.467792535850613866 ) ) ;
#106869=DIRECTION ( 'NONE',  ( 0.000000000000000000, -1.000000000000000000, 0.000000000000000000 ) ) ;
#106873=DIRECTION ( 'NONE',  ( -1.000000000000000000, -0.000000000000000000, -0.000000000000000000 ) ) ;
#106893=FACE_OUTER_BOUND ( 'NONE', #2857, .T. ) ;
#106896=CONICAL_SURFACE ( 'NONE', #116116, 2.055000000000000604, 0.9599310885968764806 ) ;
#106919=VERTEX_POINT ( 'NONE', #125475 ) ;
#106987=CYLINDRICAL_SURFACE ( 'NONE', #12884, 2.500000000000000444 ) ;
#107021=DIRECTION ( 'NONE',  ( -1.000000000000000000, -1.224606353822377258E-16, -0.000000000000000000 ) ) ;
#107028=CYLINDRICAL_SURFACE ( 'NONE', #47970, 2.500000000000000444 ) ;
#107086=ORIENTED_EDGE ( 'NONE', *, *, #123480, .T. ) ;
#107087=DIRECTION ( 'NONE',  ( 0.000000000000000000, -1.000000000000000000, 0.000000000000000000 ) ) ;
#107103=ORIENTED_EDGE ( 'NONE', *, *, #8639, .F. ) ;
#107120=ORIENTED_EDGE ( 'NONE', *, *, #51031, .F. ) ;
#107126=CARTESIAN_POINT ( 'NONE',  ( 0.1161069444170889225, -0.4000000000000003553, 2.220360628129160130 ) ) ;
#107139=AXIS2_PLACEMENT_3D ( 'NONE', #22991, #47687, #12146 ) ;
#107160=CYLINDRICAL_SURFACE ( 'NONE', #15892, 2.500000000000000444 ) ;
#107164=CYLINDRICAL_SURFACE ( 'NONE', #77930, 2.500000000000000444 ) ;
#107165=ORIENTED_EDGE ( 'NONE', *, *, #24976, .F. ) ;
#107172=VECTOR ( 'NONE', #5998, 999.9999999999998863 ) ;
#107189=DIRECTION ( 'NONE',  ( -1.000000000000000000, -1.224606353822377258E-16, -0.000000000000000000 ) ) ;
#107227=ORIENTED_EDGE ( 'NONE', *, *, #22440, .F. ) ;
#107243=DIRECTION ( 'NONE',  ( -1.000000000000000000, -1.224606353822377258E-16, -0.000000000000000000 ) ) ;
#107273=DIRECTION ( 'NONE',  ( 0.000000000000000000, 1.000000000000000000, 0.000000000000000000 ) ) ;
#107295=ADVANCED_FACE ( 'NONE', ( #71642 ), #136165, .T. ) ;
#107300=DIRECTION ( 'NONE',  ( 0.000000000000000000, -1.000000000000000000, 0.000000000000000000 ) ) ;
#107313=LINE ( 'NONE', #139978, #25774 ) ;
#107317=ORIENTED_EDGE ( 'NONE', *, *, #17441, .T. ) ;
#107322=CARTESIAN_POINT ( 'NONE',  ( 22.25000000000000000, 0.000000000000000000, 0.000000000000000000 ) ) ;
#107352=CARTESIAN_POINT ( 'NONE',  ( 7.326124847093153925, -2.055000000000000160, 2.789133085058097101E-16 ) ) ;
#107371=AXIS2_PLACEMENT_3D ( 'NONE', #21030, #142138, #34794 ) ;
#107429=ORIENTED_EDGE ( 'NONE', *, *, #52077, .F. ) ;
#107459=AXIS2_PLACEMENT_3D ( 'NONE', #135294, #100508, #446 ) ;
#107471=CARTESIAN_POINT ( 'NONE',  ( -12.69999999999998153, 0.000000000000000000, 0.000000000000000000 ) ) ;
#107480=DIRECTION ( 'NONE',  ( 0.000000000000000000, -1.000000000000000000, 0.000000000000000000 ) ) ;
#107512=AXIS2_PLACEMENT_3D ( 'NONE', #17054, #137410, #38105 ) ;
#107529=DIRECTION ( 'NONE',  ( 0.000000000000000000, -1.000000000000000000, 0.000000000000000000 ) ) ;
#107545=AXIS2_PLACEMENT_3D ( 'NONE', #118110, #27546, #139928 ) ;
#107577=CARTESIAN_POINT ( 'NONE',  ( 3.087196949643289834, 3.821174125832445049E-16, 0.000000000000000000 ) ) ;
#107683=ADVANCED_FACE ( 'NONE', ( #87767 ), #93744, .T. ) ;
#107702=CARTESIAN_POINT ( 'NONE',  ( 7.637717201596474048, 4.584330080086930965E-16, 0.000000000000000000 ) ) ;
#107705=ORIENTED_EDGE ( 'NONE', *, *, #77196, .T. ) ;
#107735=DIRECTION ( 'NONE',  ( 0.000000000000000000, -1.000000000000000000, 0.000000000000000000 ) ) ;
#107737=CARTESIAN_POINT ( 'NONE',  ( 2.924914550060624840, 2.500000000000000888, 0.000000000000000000 ) ) ;
#107756=CARTESIAN_POINT ( 'NONE',  ( 0.5685132242927012358, 4.584330080086930965E-16, 0.000000000000000000 ) ) ;
#107769=DIRECTION ( 'NONE',  ( -1.000000000000000000, -1.224606353822377258E-16, -0.000000000000000000 ) ) ;
#107799=ADVANCED_FACE ( 'NONE', ( #132735 ), #73076, .T. ) ;
#107810=ADVANCED_FACE ( 'NONE', ( #100784 ), #57312, .T. ) ;
#107813=ORIENTED_EDGE ( 'NONE', *, *, #84383, .T. ) ;
#107849=VECTOR ( 'NONE', #126814, 999.9999999999998863 ) ;
#107872=LINE ( 'NONE', #52097, #58250 ) ;
#107879=DIRECTION ( 'NONE',  ( -1.000000000000000000, -1.224606353822377258E-16, -0.000000000000000000 ) ) ;
#107909=FACE_OUTER_BOUND ( 'NONE', #9684, .T. ) ;
#107939=ORIENTED_EDGE ( 'NONE', *, *, #93875, .F. ) ;
#107944=CONICAL_SURFACE ( 'NONE', #64015, 2.500000000000000444, 0.9599310885968830309 ) ;
#107991=AXIS2_PLACEMENT_3D ( 'NONE', #67251, #66541, #33232 ) ;
#108007=CARTESIAN_POINT ( 'NONE',  ( 0.2569208697893812232, 0.4000000000000001332, -2.015694669338588429 ) ) ;
#108019=LINE ( 'NONE', #53696, #134668 ) ;
#108029=ORIENTED_EDGE ( 'NONE', *, *, #68268, .F. ) ;
#108036=DIRECTION ( 'NONE',  ( 0.000000000000000000, -1.000000000000000000, 0.000000000000000000 ) ) ;
#108094=VERTEX_POINT ( 'NONE', #121456 ) ;
#108168=DIRECTION ( 'NONE',  ( 0.000000000000000000, -1.000000000000000000, 0.000000000000000000 ) ) ;
#108176=DIRECTION ( 'NONE',  ( 1.000000000000000000, 1.224606353822377258E-16, 0.000000000000000000 ) ) ;
#108206=FACE_OUTER_BOUND ( 'NONE', #63524, .T. ) ;
#108239=CARTESIAN_POINT ( 'NONE',  ( 20.99065804761471199, 4.584330080086930965E-16, 0.000000000000000000 ) ) ;
#108246=ADVANCED_FACE ( 'NONE', ( #46078 ), #75341, .T. ) ;
#108247=EDGE_LOOP ( 'NONE', ( #34478, #52737, #57382, #104555, #30981 ) ) ;
#108352=CARTESIAN_POINT ( 'NONE',  ( 7.014532492589830248, 3.821174125832445049E-16, 0.000000000000000000 ) ) ;
#108372=EDGE_CURVE ( 'NONE', #16482, #31359, #68525, .T. ) ;
#108384=CARTESIAN_POINT ( 'NONE',  ( 13.92145407031093818, 4.584330080086930965E-16, 0.000000000000000000 ) ) ;
#108385=VERTEX_POINT ( 'NONE', #77804 ) ;
#108404=CARTESIAN_POINT ( 'NONE',  ( 0.000000000000000000, -0.3999999999999998002, -2.015694669338588429 ) ) ;
#108445=DIRECTION ( 'NONE',  ( -1.000000000000000000, -1.224606353822377258E-16, -0.000000000000000000 ) ) ;
#108543=DIRECTION ( 'NONE',  ( -1.000000000000000000, -1.224606353822377258E-16, -0.000000000000000000 ) ) ;
#108586=ORIENTED_EDGE ( 'NONE', *, *, #97689, .T. ) ;
#108610=AXIS2_PLACEMENT_3D ( 'NONE', #28365, #116062, #118920 ) ;
#108619=CONICAL_SURFACE ( 'NONE', #22932, 2.055000000000000604, 0.9599310885968764806 ) ;
#108638=CARTESIAN_POINT ( 'NONE',  ( 9.208651418775088970, 4.584330080086930965E-16, 0.000000000000000000 ) ) ;
#108643=CARTESIAN_POINT ( 'NONE',  ( 17.06332250466817158, -2.500000000000000444, 3.061616997868384127E-16 ) ) ;
#108678=CARTESIAN_POINT ( 'NONE',  ( 0.000000000000000000, 0.000000000000000000, 0.000000000000000000 ) ) ;
#108697=FACE_OUTER_BOUND ( 'NONE', #74330, .T. ) ;
#108699=DIRECTION ( 'NONE',  ( 0.000000000000000000, -1.000000000000000000, 0.000000000000000000 ) ) ;
#108721=DIRECTION ( 'NONE',  ( -1.000000000000000000, -0.000000000000000000, -0.000000000000000000 ) ) ;
#108748=CARTESIAN_POINT ( 'NONE',  ( 13.13598696172163116, 4.584330080086930965E-16, 0.000000000000000000 ) ) ;
#108767=ORIENTED_EDGE ( 'NONE', *, *, #47495, .T. ) ;
#108776=FACE_OUTER_BOUND ( 'NONE', #88798, .T. ) ;
#108796=DIRECTION ( 'NONE',  ( 0.000000000000000000, -1.000000000000000000, 0.000000000000000000 ) ) ;
#108798=CIRCLE ( 'NONE', #92561, 2.500000000000000444 ) ;
#108817=AXIS2_PLACEMENT_3D ( 'NONE', #77615, #75461, #142158 ) ;
#108823=DIRECTION ( 'NONE',  ( 0.000000000000000000, -1.000000000000000000, 0.000000000000000000 ) ) ;
#108828=EDGE_CURVE ( 'NONE', #106357, #7107, #97193, .T. ) ;
#108879=CONICAL_SURFACE ( 'NONE', #106601, 2.055000000000000604, 0.9599310885968764806 ) ;
#108884=AXIS2_PLACEMENT_3D ( 'NONE', #60679, #6911, #106240 ) ;
#108885=CIRCLE ( 'NONE', #67338, 2.500000000000000444 ) ;
#108887=CONICAL_SURFACE ( 'NONE', #85729, 2.055000000000000604, 0.9599310885968764806 ) ;
#108920=AXIS2_PLACEMENT_3D ( 'NONE', #21237, #143019, #100237 ) ;
#108993=AXIS2_PLACEMENT_3D ( 'NONE', #78755, #56329, #43985 ) ;
#109017=ORIENTED_EDGE ( 'NONE', *, *, #100629, .F. ) ;
#109033=CARTESIAN_POINT ( 'NONE',  ( 19.41972383043609440, 3.061616997868383634E-16, -2.500000000000000444 ) ) ;
#109043=VECTOR ( 'NONE', #121930, 1000.000000000000000 ) ;
#109049=CIRCLE ( 'NONE', #273, 2.500000000000000444 ) ;
#109085=CIRCLE ( 'NONE', #106691, 2.500000000000000444 ) ;
#109112=EDGE_LOOP ( 'NONE', ( #66952, #100736, #45439, #27160, #87390, #29683 ) ) ;
#109142=DIRECTION ( 'NONE',  ( 0.000000000000000000, -1.000000000000000000, 0.000000000000000000 ) ) ;
#109222=CIRCLE ( 'NONE', #42093, 2.500000000000000444 ) ;
#109235=DIRECTION ( 'NONE',  ( 0.000000000000000000, -1.000000000000000000, 0.000000000000000000 ) ) ;
#109327=AXIS2_PLACEMENT_3D ( 'NONE', #134491, #114831, #70682 ) ;
#109337=CARTESIAN_POINT ( 'NONE',  ( 9.994118527364397764, 4.584330080086930965E-16, 0.000000000000000000 ) ) ;
#109432=CARTESIAN_POINT ( 'NONE',  ( -12.69999999999998153, 0.000000000000000000, 2.500000000000000444 ) ) ;
#109454=ORIENTED_EDGE ( 'NONE', *, *, #39977, .F. ) ;
#109461=VERTEX_POINT ( 'NONE', #10693 ) ;
#109480=FACE_OUTER_BOUND ( 'NONE', #17391, .T. ) ;
#109522=DIRECTION ( 'NONE',  ( -1.000000000000000000, -0.000000000000000000, -0.000000000000000000 ) ) ;
#109534=VERTEX_POINT ( 'NONE', #3396 ) ;
#109546=ORIENTED_EDGE ( 'NONE', *, *, #50281, .F. ) ;
#109558=CARTESIAN_POINT ( 'NONE',  ( 3.710381658649933634, 4.584330080086930965E-16, 0.000000000000000000 ) ) ;
#109603=CARTESIAN_POINT ( 'NONE',  ( 2.139447441471317379, 4.584330080086930965E-16, 0.000000000000000000 ) ) ;
#109612=CARTESIAN_POINT ( 'NONE',  ( 4.495848767239241539, -2.500000000000000444, 3.061616997868384127E-16 ) ) ;
#109621=CARTESIAN_POINT ( 'NONE',  ( 9.682526172861077640, 4.202752102959690472E-16, 0.000000000000000000 ) ) ;
#109639=CARTESIAN_POINT ( 'NONE',  ( 14.70692117890024697, 4.584330080086930965E-16, 0.000000000000000000 ) ) ;
#109699=CARTESIAN_POINT ( 'NONE',  ( 6.852250093007166143, -2.500000000000000000, 3.061616997868383634E-16 ) ) ;
#109718=CIRCLE ( 'NONE', #121303, 2.500000000000000444 ) ;
#109733=CARTESIAN_POINT ( 'NONE',  ( 0.7307956238753654521, -0.3999999999999997446, -2.467792535850613866 ) ) ;
#109746=EDGE_LOOP ( 'NONE', ( #109017, #114721, #29532, #21962, #55794, #32139 ) ) ;
#109788=DIRECTION ( 'NONE',  ( 0.000000000000000000, -1.000000000000000000, 0.000000000000000000 ) ) ;
#109801=DIRECTION ( 'NONE',  ( -1.000000000000000000, -1.224606353822377258E-16, -0.000000000000000000 ) ) ;
#109860=DIRECTION ( 'NONE',  ( 1.734723475976806848E-16, -1.000000000000000000, 0.000000000000000000 ) ) ;
#109909=FACE_OUTER_BOUND ( 'NONE', #7476, .T. ) ;
#109910=FACE_OUTER_BOUND ( 'NONE', #39373, .T. ) ;
#109926=EDGE_LOOP ( 'NONE', ( #11837, #57804, #19334, #56084, #85995 ) ) ;
#109980=VERTEX_POINT ( 'NONE', #16809 ) ;
#110035=ORIENTED_EDGE ( 'NONE', *, *, #128045, .T. ) ;
#110047=VECTOR ( 'NONE', #41068, 1000.000000000000000 ) ;
#110068=AXIS2_PLACEMENT_3D ( 'NONE', #52969, #110908, #113796 ) ;
#110101=EDGE_CURVE ( 'NONE', #137228, #140889, #96587, .T. ) ;
#110102=ORIENTED_EDGE ( 'NONE', *, *, #100629, .T. ) ;
#110118=ORIENTED_EDGE ( 'NONE', *, *, #2202, .T. ) ;
#110129=DIRECTION ( 'NONE',  ( -0.5735764363510499342, -0.8191520442889891340, 0.000000000000000000 ) ) ;
#110187=EDGE_LOOP ( 'NONE', ( #82227, #1282, #29672, #42163, #69361, #56599 ) ) ;
#110243=ORIENTED_EDGE ( 'NONE', *, *, #12697, .T. ) ;
#110298=CIRCLE ( 'NONE', #94173, 2.500000000000000444 ) ;
#110332=DIRECTION ( 'NONE',  ( 0.000000000000000000, -1.000000000000000000, 0.000000000000000000 ) ) ;
#110359=DIRECTION ( 'NONE',  ( 1.000000000000000000, 1.224606353822377258E-16, 0.000000000000000000 ) ) ;
#110367=VECTOR ( 'NONE', #4101, 999.9999999999998863 ) ;
#110370=PRODUCT_DEFINITION ( 'UNKNOWN', '', #118833, #42901 ) ;
#110422=CARTESIAN_POINT ( 'NONE',  ( 0.8348608954644654023, -0.3999999999999997446, -2.317232259782045833 ) ) ;
#110431=DIRECTION ( 'NONE',  ( 0.000000000000000000, -1.000000000000000000, 0.000000000000000000 ) ) ;
#110458=CARTESIAN_POINT ( 'NONE',  ( 16.27785539607886633, -2.500000000000000000, 3.061616997868383634E-16 ) ) ;
#110541=CARTESIAN_POINT ( 'NONE',  ( 7.637717201596474048, 0.000000000000000000, 2.500000000000000444 ) ) ;
#110548=CARTESIAN_POINT ( 'NONE',  ( 7.014532492589830248, 3.061616997868383634E-16, -2.500000000000000444 ) ) ;
#110571=CARTESIAN_POINT ( 'NONE',  ( 17.22560490425083657, 4.333342374871280669E-31, 2.500000000000000444 ) ) ;
#110581=DIRECTION ( 'NONE',  ( 0.000000000000000000, -1.000000000000000000, 0.000000000000000000 ) ) ;
#110594=EDGE_CURVE ( 'NONE', #93815, #764, #76755, .T. ) ;
#110596=EDGE_CURVE ( 'NONE', #46122, #73650, #66325, .T. ) ;
#110598=DIRECTION ( 'NONE',  ( 0.000000000000000000, 1.000000000000000000, 0.000000000000000000 ) ) ;
#110652=CARTESIAN_POINT ( 'NONE',  ( 1.353980332882009030, 2.500000000000000888, 0.000000000000000000 ) ) ;
#110654=DIRECTION ( 'NONE',  ( -1.000000000000000000, -1.224606353822377258E-16, -0.000000000000000000 ) ) ;
#110664=DIRECTION ( 'NONE',  ( 0.000000000000000000, -1.000000000000000000, 0.000000000000000000 ) ) ;
#110675=CARTESIAN_POINT ( 'NONE',  ( 7.014532492589830248, -2.499999999999999112, 0.000000000000000000 ) ) ;
#110678=FACE_OUTER_BOUND ( 'NONE', #85075, .T. ) ;
#110698=DIRECTION ( 'NONE',  ( -1.301042606982605074E-16, 1.000000000000000000, 0.000000000000000000 ) ) ;
#110745=ORIENTED_EDGE ( 'NONE', *, *, #29808, .F. ) ;
#110816=VERTEX_POINT ( 'NONE', #104897 ) ;
#110821=FACE_OUTER_BOUND ( 'NONE', #129581, .T. ) ;
#110863=LINE ( 'NONE', #100742, #79522 ) ;
#110892=ORIENTED_EDGE ( 'NONE', *, *, #62092, .F. ) ;
#110908=DIRECTION ( 'NONE',  ( -1.000000000000000000, -0.000000000000000000, -0.000000000000000000 ) ) ;
#110962=VERTEX_POINT ( 'NONE', #11262 ) ;
#110996=VECTOR ( 'NONE', #119670, 999.9999999999998863 ) ;
#111033=EDGE_CURVE ( 'NONE', #20222, #20849, #42532, .T. ) ;
#111050=EDGE_CURVE ( 'NONE', #111882, #5092, #70981, .T. ) ;
#111062=AXIS2_PLACEMENT_3D ( 'NONE', #88970, #12792, #135333 ) ;
#111067=CIRCLE ( 'NONE', #87916, 2.500000000000000444 ) ;
#111100=ORIENTED_EDGE ( 'NONE', *, *, #86072, .T. ) ;
#111111=CARTESIAN_POINT ( 'NONE',  ( 18.01107201284014536, 3.061616997868387579E-16, -2.500000000000000444 ) ) ;
#111114=AXIS2_PLACEMENT_3D ( 'NONE', #19657, #31267, #130585 ) ;
#111145=VECTOR ( 'NONE', #20685, 1000.000000000000000 ) ;
#111246=CARTESIAN_POINT ( 'NONE',  ( 15.49238828748955576, 4.584330080086930965E-16, 0.000000000000000000 ) ) ;
#111258=AXIS2_PLACEMENT_3D ( 'NONE', #138749, #69960, #17642 ) ;
#111286=AXIS2_PLACEMENT_3D ( 'NONE', #142602, #43290, #87500 ) ;
#111295=CIRCLE ( 'NONE', #58169, 2.500000000000000444 ) ;
#111444=FACE_OUTER_BOUND ( 'NONE', #115387, .T. ) ;
#111446=DIRECTION ( 'NONE',  ( 0.000000000000000000, -1.000000000000000000, 0.000000000000000000 ) ) ;
#111457=VERTEX_POINT ( 'NONE', #55363 ) ;
#111483=ORIENTED_EDGE ( 'NONE', *, *, #89600, .F. ) ;
#111499=ORIENTED_EDGE ( 'NONE', *, *, #3250, .T. ) ;
#111511=AXIS2_PLACEMENT_3D ( 'NONE', #68739, #78903, #13585 ) ;
#111525=ORIENTED_EDGE ( 'NONE', *, *, #130028, .T. ) ;
#111529=CIRCLE ( 'NONE', #67594, 2.500000000000000444 ) ;
#111530=CARTESIAN_POINT ( 'NONE',  ( -12.69999999999998153, 0.000000000000000000, 0.000000000000000000 ) ) ;
#111538=ORIENTED_EDGE ( 'NONE', *, *, #116674, .T. ) ;
#111561=CARTESIAN_POINT ( 'NONE',  ( 6.540657738503846907, -2.055000000000000160, 2.789133085058097101E-16 ) ) ;
#111567=ADVANCED_FACE ( 'NONE', ( #107909 ), #119666, .T. ) ;
#111569=ORIENTED_EDGE ( 'NONE', *, *, #14387, .T. ) ;
#111574=LINE ( 'NONE', #23865, #7004 ) ;
#111605=CARTESIAN_POINT ( 'NONE',  ( 16.75173015016484968, -2.055000000000000160, 2.789133085058097101E-16 ) ) ;
#111617=ADVANCED_FACE ( 'NONE', ( #115939 ), #106479, .T. ) ;
#111654=CARTESIAN_POINT ( 'NONE',  ( 2.139447441471317823, -2.500000000000000000, 3.061616997868383634E-16 ) ) ;
#111679=CARTESIAN_POINT ( 'NONE',  ( 5.443598275411213550, 3.821174125832445049E-16, 0.000000000000000000 ) ) ;
#111698=AXIS2_PLACEMENT_3D ( 'NONE', #44429, #122654, #131414 ) ;
#111756=DIRECTION ( 'NONE',  ( -1.000000000000000000, -1.224606353822377258E-16, -0.000000000000000000 ) ) ;
#111763=ORIENTED_EDGE ( 'NONE', *, *, #140662, .T. ) ;
#111838=CARTESIAN_POINT ( 'NONE',  ( 0.3605399447480615582, -0.3999999999999998002, -2.166563668000045517 ) ) ;
#111848=VERTEX_POINT ( 'NONE', #35425 ) ;
#111852=CARTESIAN_POINT ( 'NONE',  ( 6.066782984417857350, -9.629649721936179265E-32, 2.500000000000000444 ) ) ;
#111874=AXIS2_PLACEMENT_3D ( 'NONE', #3182, #68487, #33709 ) ;
#111882=VERTEX_POINT ( 'NONE', #91896 ) ;
#111944=CARTESIAN_POINT ( 'NONE',  ( 17.06332250466817158, 4.584330080086930965E-16, 0.000000000000000000 ) ) ;
#111973=ORIENTED_EDGE ( 'NONE', *, *, #63946, .T. ) ;
#111980=AXIS2_PLACEMENT_3D ( 'NONE', #105828, #94259, #107273 ) ;
#112021=DIRECTION ( 'NONE',  ( 0.5735764363510448272, -0.8191520442889927978, 1.003171929053526103E-16 ) ) ;
#112029=LINE ( 'NONE', #68536, #86025 ) ;
#112054=ORIENTED_EDGE ( 'NONE', *, *, #15291, .F. ) ;
#112103=LINE ( 'NONE', #56328, #49558 ) ;
#112104=CYLINDRICAL_SURFACE ( 'NONE', #108993, 2.500000000000000444 ) ;
#112136=B_SPLINE_CURVE_WITH_KNOTS ( 'NONE', 3,
 ( #6345, #86829, #117971, #107126 ),
 .UNSPECIFIED., .F., .F.,
 ( 4, 4 ),
 ( 0.008851590069444708123, 0.009100162336955337078 ),
 .UNSPECIFIED. ) ;
#112160=ADVANCED_FACE ( 'NONE', ( #34500 ), #78725, .T. ) ;
#112171=CIRCLE ( 'NONE', #49682, 2.500000000000000444 ) ;
#112192=CYLINDRICAL_SURFACE ( 'NONE', #139411, 2.500000000000000444 ) ;
#112194=ORIENTED_EDGE ( 'NONE', *, *, #132032, .T. ) ;
#112205=CARTESIAN_POINT ( 'NONE',  ( 16.27785539607886633, 4.584330080086930965E-16, 0.000000000000000000 ) ) ;
#112211=DIRECTION ( 'NONE',  ( -1.000000000000000000, -1.224606353822377258E-16, -0.000000000000000000 ) ) ;
#112215=CARTESIAN_POINT ( 'NONE',  ( 0.1161069444170879233, 0.4000000000000001332, -2.220360628129161462 ) ) ;
#112258=CIRCLE ( 'NONE', #54436, 2.500000000000000444 ) ;
#112268=DIRECTION ( 'NONE',  ( 1.055184596092948005E-16, -1.000000000000000000, 0.000000000000000000 ) ) ;
#112304=CARTESIAN_POINT ( 'NONE',  ( 4.495848767239241539, 4.584330080086930965E-16, 0.000000000000000000 ) ) ;
#112315=DIRECTION ( 'NONE',  ( -1.000000000000000000, -1.224606353822377258E-16, -0.000000000000000000 ) ) ;
#112363=VERTEX_POINT ( 'NONE', #137391 ) ;
#112377=DIRECTION ( 'NONE',  ( -0.5735764363510501562, 0.8191520442889890230, 1.003171929053521419E-16 ) ) ;
#112403=ORIENTED_EDGE ( 'NONE', *, *, #24236, .T. ) ;
#112447=ORIENTED_EDGE ( 'NONE', *, *, #4926, .T. ) ;
#112458=ORIENTED_EDGE ( 'NONE', *, *, #63553, .F. ) ;
#112469=CARTESIAN_POINT ( 'NONE',  ( 0.5685132242927012358, 0.4000000000000001887, -2.467792535850613866 ) ) ;
#112516=ORIENTED_EDGE ( 'NONE', *, *, #28608, .F. ) ;
#112518=EDGE_LOOP ( 'NONE', ( #110118, #64307, #47300, #123430, #101539, #73086 ) ) ;
#112524=DIRECTION ( 'NONE',  ( -1.000000000000000000, -1.224606353822377258E-16, -0.000000000000000000 ) ) ;
#112534=CARTESIAN_POINT ( 'NONE',  ( 3.087196949643289834, -4.814824860968089633E-32, 2.500000000000000444 ) ) ;
#112550=EDGE_CURVE ( 'NONE', #140889, #34230, #89773, .T. ) ;
#112671=CARTESIAN_POINT ( 'NONE',  ( 6.852250093007166143, 0.000000000000000000, 2.500000000000000444 ) ) ;
#112677=ORIENTED_EDGE ( 'NONE', *, *, #74290, .T. ) ;
#112747=DIRECTION ( 'NONE',  ( 0.5735764363510448272, -0.8191520442889927978, 1.003171929053526103E-16 ) ) ;
#112772=VERTEX_POINT ( 'NONE', #142562 ) ;
#112777=EDGE_LOOP ( 'NONE', ( #139951, #101421, #73647, #41602, #120809 ) ) ;
#112781=CARTESIAN_POINT ( 'NONE',  ( 10.94186803553636977, 2.500000000000003109, 3.061616997868386592E-16 ) ) ;
#112788=EDGE_LOOP ( 'NONE', ( #1644, #126895, #21813, #50414, #69764 ) ) ;
#112798=CARTESIAN_POINT ( 'NONE',  ( -12.69999999999998153, 0.000000000000000000, 0.000000000000000000 ) ) ;
#112829=FILL_AREA_STYLE ('',( #37430 ) ) ;
#112882=CIRCLE ( 'NONE', #87447, 2.500000000000000444 ) ;
#112895=DIRECTION ( 'NONE',  ( 0.5735764363510444941, 0.8191520442889929088, 0.000000000000000000 ) ) ;
#112968=CONICAL_SURFACE ( 'NONE', #22696, 2.055000000000000604, 0.9599310885968764806 ) ;
#113116=EDGE_CURVE ( 'NONE', #124115, #99111, #27175, .T. ) ;
#113155=FACE_OUTER_BOUND ( 'NONE', #85214, .T. ) ;
#113168=ORIENTED_EDGE ( 'NONE', *, *, #76954, .F. ) ;
#113177=DIRECTION ( 'NONE',  ( -1.000000000000000000, -0.000000000000000000, -0.000000000000000000 ) ) ;
#113236=CARTESIAN_POINT ( 'NONE',  ( 3.398789304146613954, 4.202752102959690472E-16, 0.000000000000000000 ) ) ;
#113295=DIRECTION ( 'NONE',  ( 1.000000000000000000, 1.224606353822377258E-16, 0.000000000000000000 ) ) ;
#113300=AXIS2_PLACEMENT_3D ( 'NONE', #138872, #93204, #16327 ) ;
#113318=ORIENTED_EDGE ( 'NONE', *, *, #67785, .F. ) ;
#113339=DIRECTION ( 'NONE',  ( 1.000000000000000000, 1.224606353822377258E-16, 0.000000000000000000 ) ) ;
#113377=AXIS2_PLACEMENT_3D ( 'NONE', #118287, #117558, #10242 ) ;
#113401=EDGE_CURVE ( 'NONE', #33386, #63294, #4331, .T. ) ;
#113404=CARTESIAN_POINT ( 'NONE',  ( 4.658131166821905644, 3.821174125832445049E-16, 0.000000000000000000 ) ) ;
#113448=ORIENTED_EDGE ( 'NONE', *, *, #26944, .F. ) ;
#113464=DIRECTION ( 'NONE',  ( -1.000000000000000000, -1.224606353822377258E-16, -0.000000000000000000 ) ) ;
#113499=ORIENTED_EDGE ( 'NONE', *, *, #64009, .T. ) ;
#113554=CARTESIAN_POINT ( 'NONE',  ( 16.75173015016484968, 4.202752102959690472E-16, 0.000000000000000000 ) ) ;
#113609=B_SPLINE_CURVE_WITH_KNOTS ( 'NONE', 3,
 ( #112469, #136351, #91439, #1524 ),
 .UNSPECIFIED., .F., .F.,
 ( 4, 4 ),
 ( 0.003615568590623256025, 0.004164643302645746128 ),
 .UNSPECIFIED. ) ;
#113612=CARTESIAN_POINT ( 'NONE',  ( -12.69999999999998153, 0.000000000000000000, 0.000000000000000000 ) ) ;
#113622=DIRECTION ( 'NONE',  ( 1.000000000000000000, 1.224606353822377258E-16, 0.000000000000000000 ) ) ;
#113641=CARTESIAN_POINT ( 'NONE',  ( 3.872664058232598183, 3.061616997868383634E-16, -2.500000000000000444 ) ) ;
#113654=ORIENTED_EDGE ( 'NONE', *, *, #15795, .F. ) ;
#113657=CIRCLE ( 'NONE', #51181, 2.500000000000000444 ) ;
#113682=DIRECTION ( 'NONE',  ( -1.000000000000000000, -1.224606353822377258E-16, -0.000000000000000000 ) ) ;
#113711=CIRCLE ( 'NONE', #106762, 2.500000000000000444 ) ;
#113764=DIRECTION ( 'NONE',  ( 0.000000000000000000, -1.000000000000000000, 0.000000000000000000 ) ) ;
#113792=EDGE_CURVE ( 'NONE', #24475, #109980, #122567, .T. ) ;
#113796=DIRECTION ( 'NONE',  ( 0.000000000000000000, 0.000000000000000000, 1.000000000000000000 ) ) ;
#113810=DIRECTION ( 'NONE',  ( 0.000000000000000000, -1.000000000000000000, 0.000000000000000000 ) ) ;
#113849=ORIENTED_EDGE ( 'NONE', *, *, #50672, .F. ) ;
#113891=DIRECTION ( 'NONE',  ( -1.000000000000000000, -1.224606353822377258E-16, -0.000000000000000000 ) ) ;
#113951=ORIENTED_EDGE ( 'NONE', *, *, #20200, .F. ) ;
#114011=EDGE_LOOP ( 'NONE', ( #103502, #74488, #90374, #143418, #129097 ) ) ;
#114022=CARTESIAN_POINT ( 'NONE',  ( -12.69999999999998153, 0.000000000000000000, 0.000000000000000000 ) ) ;
#114052=ORIENTED_EDGE ( 'NONE', *, *, #132032, .F. ) ;
#114057=AXIS2_PLACEMENT_3D ( 'NONE', #58763, #90637, #35569 ) ;
#114063=CARTESIAN_POINT ( 'NONE',  ( 22.25000000000000000, 2.143131898507868051E-16, -1.749999999999999778 ) ) ;
#114067=FACE_OUTER_BOUND ( 'NONE', #13500, .T. ) ;
#114069=AXIS2_PLACEMENT_3D ( 'NONE', #142971, #22588, #11718 ) ;
#114095=ORIENTED_EDGE ( 'NONE', *, *, #78222, .F. ) ;
#114114=CARTESIAN_POINT ( 'NONE',  ( 13.13598696172163116, 2.500000000000000444, 0.000000000000000000 ) ) ;
#114116=AXIS2_PLACEMENT_3D ( 'NONE', #89477, #11900, #133713 ) ;
#114131=DIRECTION ( 'NONE',  ( 0.000000000000000000, -1.000000000000000000, 0.000000000000000000 ) ) ;
#114175=CIRCLE ( 'NONE', #74884, 2.500000000000000444 ) ;
#114221=AXIS2_PLACEMENT_3D ( 'NONE', #69178, #47463, #45305 ) ;
#114265=CONICAL_SURFACE ( 'NONE', #17006, 2.500000000000000444, 0.9599310885968830309 ) ;
#114279=AXIS2_PLACEMENT_3D ( 'NONE', #65025, #29499, #86044 ) ;
#114311=DIRECTION ( 'NONE',  ( 1.000000000000000000, 1.224606353822377258E-16, 0.000000000000000000 ) ) ;
#114345=EDGE_CURVE ( 'NONE', #14650, #1294, #111067, .T. ) ;
#114354=EDGE_CURVE ( 'NONE', #142044, #46122, #64858, .T. ) ;
#114390=ORIENTED_EDGE ( 'NONE', *, *, #96960, .F. ) ;
#114393=ORIENTED_EDGE ( 'NONE', *, *, #5371, .T. ) ;
#114397=CARTESIAN_POINT ( 'NONE',  ( 2.924914550060625285, -9.629649721936179265E-32, 2.500000000000000444 ) ) ;
#114412=CARTESIAN_POINT ( 'NONE',  ( -12.69999999999998153, 0.000000000000000000, 0.000000000000000000 ) ) ;
#114450=ORIENTED_EDGE ( 'NONE', *, *, #22962, .T. ) ;
#114455=CARTESIAN_POINT ( 'NONE',  ( 10.15640092694706453, 0.000000000000000000, 2.500000000000000444 ) ) ;
#114585=CARTESIAN_POINT ( 'NONE',  ( -12.69999999999998153, 0.000000000000000000, 0.000000000000000000 ) ) ;
#114587=DIRECTION ( 'NONE',  ( -1.000000000000000000, -1.224606353822377258E-16, -0.000000000000000000 ) ) ;
#114594=VECTOR ( 'NONE', #112895, 1000.000000000000000 ) ;
#114602=CARTESIAN_POINT ( 'NONE',  ( -12.69999999999998153, 0.000000000000000000, 2.500000000000000444 ) ) ;
#114630=AXIS2_PLACEMENT_3D ( 'NONE', #125666, #67740, #70601 ) ;
#114653=VERTEX_POINT ( 'NONE', #124923 ) ;
#114667=ORIENTED_EDGE ( 'NONE', *, *, #64639, .F. ) ;
#114720=AXIS2_PLACEMENT_3D ( 'NONE', #64246, #29453, #85258 ) ;
#114721=ORIENTED_EDGE ( 'NONE', *, *, #78554, .T. ) ;
#114756=DIRECTION ( 'NONE',  ( -1.000000000000000000, -1.224606353822377258E-16, -0.000000000000000000 ) ) ;
#114772=LINE ( 'NONE', #35858, #92464 ) ;
#114821=DIRECTION ( 'NONE',  ( -1.734723475976806848E-16, 1.000000000000000000, 0.000000000000000000 ) ) ;
#114823=VECTOR ( 'NONE', #133425, 1000.000000000000000 ) ;
#114831=DIRECTION ( 'NONE',  ( -1.000000000000000000, -1.224606353822377258E-16, -0.000000000000000000 ) ) ;
#114832=CARTESIAN_POINT ( 'NONE',  ( 16.27785539607886633, -2.500000000000000444, 3.061616997868384127E-16 ) ) ;
#114866=FACE_OUTER_BOUND ( 'NONE', #52448, .T. ) ;
#114877=AXIS2_PLACEMENT_3D ( 'NONE', #64844, #75718, #65590 ) ;
#114879=ORIENTED_EDGE ( 'NONE', *, *, #18951, .F. ) ;
#114931=ADVANCED_FACE ( 'NONE', ( #27378 ), #6945, .T. ) ;
#114967=ORIENTED_EDGE ( 'NONE', *, *, #121273, .T. ) ;
#115000=DIRECTION ( 'NONE',  ( -1.000000000000000000, -1.224606353822377258E-16, -0.000000000000000000 ) ) ;
#115029=CARTESIAN_POINT ( 'NONE',  ( 1.827855086967997700, 4.202752102959690472E-16, 0.000000000000000000 ) ) ;
#115056=EDGE_LOOP ( 'NONE', ( #62744, #6215, #48498, #142566, #41493 ) ) ;
#115077=CARTESIAN_POINT ( 'NONE',  ( -12.69999999999998153, 0.000000000000000000, 0.000000000000000000 ) ) ;
#115093=VERTEX_POINT ( 'NONE', #73762 ) ;
#115131=DIRECTION ( 'NONE',  ( 0.000000000000000000, -1.000000000000000000, 0.000000000000000000 ) ) ;
#115138=DIRECTION ( 'NONE',  ( -1.000000000000000000, -1.224606353822377258E-16, -0.000000000000000000 ) ) ;
#115153=FACE_OUTER_BOUND ( 'NONE', #102396, .T. ) ;
#115236=ORIENTED_EDGE ( 'NONE', *, *, #90372, .T. ) ;
#115252=EDGE_CURVE ( 'NONE', #68516, #19275, #83594, .T. ) ;
#115258=EDGE_CURVE ( 'NONE', #43279, #112772, #21054, .T. ) ;
#115296=ORIENTED_EDGE ( 'NONE', *, *, #48536, .T. ) ;
#115317=CARTESIAN_POINT ( 'NONE',  ( 0.2569208697893814453, 4.202752102959690472E-16, 0.000000000000000000 ) ) ;
#115352=DIRECTION ( 'NONE',  ( -1.000000000000000000, -1.224606353822377258E-16, -0.000000000000000000 ) ) ;
#115375=DIRECTION ( 'NONE',  ( 0.000000000000000000, 0.000000000000000000, 1.000000000000000000 ) ) ;
#115381=DIRECTION ( 'NONE',  ( -1.000000000000000000, -1.224606353822377258E-16, -0.000000000000000000 ) ) ;
#115387=EDGE_LOOP ( 'NONE', ( #134878, #53315, #37664, #17738, #50157 ) ) ;
#115495=ADVANCED_FACE ( 'NONE', ( #43825 ), #118212, .T. ) ;
#115549=DIRECTION ( 'NONE',  ( 0.000000000000000000, -1.000000000000000000, 0.000000000000000000 ) ) ;
#115553=CIRCLE ( 'NONE', #113300, 2.055000000000000604 ) ;
#115564=ORIENTED_EDGE ( 'NONE', *, *, #63981, .T. ) ;
#115610=AXIS2_PLACEMENT_3D ( 'NONE', #44065, #14275, #67241 ) ;
#115673=CIRCLE ( 'NONE', #53203, 2.500000000000000444 ) ;
#115714=EDGE_CURVE ( 'NONE', #139082, #7243, #60526, .T. ) ;
#115716=CARTESIAN_POINT ( 'NONE',  ( 20.99065804761471199, 4.584330080086930965E-16, 0.000000000000000000 ) ) ;
#115718=DIRECTION ( 'NONE',  ( -1.000000000000000000, -1.224606353822377258E-16, -0.000000000000000000 ) ) ;
#115746=EDGE_CURVE ( 'NONE', #9950, #83013, #93751, .T. ) ;
#115797=DIRECTION ( 'NONE',  ( -1.000000000000000000, -0.000000000000000000, -0.000000000000000000 ) ) ;
#115830=ORIENTED_EDGE ( 'NONE', *, *, #121336, .F. ) ;
#115844=CIRCLE ( 'NONE', #2436, 2.055000000000000604 ) ;
#115847=ADVANCED_FACE ( 'NONE', ( #82889 ), #138699, .T. ) ;
#115888=AXIS2_PLACEMENT_3D ( 'NONE', #114585, #26873, #15254 ) ;
#115901=LINE ( 'NONE', #83320, #29354 ) ;
#115914=DIRECTION ( 'NONE',  ( -1.000000000000000000, -0.000000000000000000, -0.000000000000000000 ) ) ;
#115920=ORIENTED_EDGE ( 'NONE', *, *, #99685, .F. ) ;
#115939=FACE_OUTER_BOUND ( 'NONE', #58572, .T. ) ;
#115962=DIRECTION ( 'NONE',  ( 0.000000000000000000, -1.000000000000000000, 0.000000000000000000 ) ) ;
#115969=ORIENTED_EDGE ( 'NONE', *, *, #104200, .F. ) ;
#115977=CONICAL_SURFACE ( 'NONE', #53510, 2.500000000000000444, 0.9599310885968830309 ) ;
#115979=DIRECTION ( 'NONE',  ( -1.000000000000000000, -1.224606353822377258E-16, -0.000000000000000000 ) ) ;
#116020=EDGE_LOOP ( 'NONE', ( #91686, #121682, #62548, #125528, #1308 ) ) ;
#116062=DIRECTION ( 'NONE',  ( 1.000000000000000000, 1.224606353822377258E-16, 0.000000000000000000 ) ) ;
#116069=FACE_OUTER_BOUND ( 'NONE', #10931, .T. ) ;
#116094=DIRECTION ( 'NONE',  ( -1.000000000000000000, -0.000000000000000000, -0.000000000000000000 ) ) ;
#116116=AXIS2_PLACEMENT_3D ( 'NONE', #13647, #134775, #3481 ) ;
#116132=CARTESIAN_POINT ( 'NONE',  ( 11.56505274454301357, 2.500000000000000444, 0.000000000000000000 ) ) ;
#116134=AXIS2_PLACEMENT_3D ( 'NONE', #101846, #134494, #57662 ) ;
#116150=CIRCLE ( 'NONE', #86152, 2.500000000000000444 ) ;
#116157=AXIS2_PLACEMENT_3D ( 'NONE', #19277, #20690, #62088 ) ;
#116183=CIRCLE ( 'NONE', #134743, 2.500000000000000444 ) ;
#116216=DIRECTION ( 'NONE',  ( -1.000000000000000000, -1.224606353822377258E-16, -0.000000000000000000 ) ) ;
#116217=ORIENTED_EDGE ( 'NONE', *, *, #117092, .F. ) ;
#116234=DIRECTION ( 'NONE',  ( 0.000000000000000000, 1.000000000000000000, 0.000000000000000000 ) ) ;
#116300=EDGE_CURVE ( 'NONE', #8017, #79690, #48651, .T. ) ;
#116357=CARTESIAN_POINT ( 'NONE',  ( -12.69999999999998153, 3.061616997868383634E-16, -2.500000000000000444 ) ) ;
#116430=LINE ( 'NONE', #38169, #94962 ) ;
#116453=EDGE_LOOP ( 'NONE', ( #47556, #1352, #32489, #55597, #131731, #100339 ) ) ;
#116461=VECTOR ( 'NONE', #59557, 1000.000000000000000 ) ;
#116608=ORIENTED_EDGE ( 'NONE', *, *, #36836, .F. ) ;
#116615=AXIS2_PLACEMENT_3D ( 'NONE', #126704, #2049, #103520 ) ;
#116663=CARTESIAN_POINT ( 'NONE',  ( 18.32266436734346726, -2.055000000000000160, 2.789133085058097101E-16 ) ) ;
#116674=EDGE_CURVE ( 'NONE', #25493, #52416, #16361, .T. ) ;
#116687=EDGE_CURVE ( 'NONE', #104716, #44009, #64957, .T. ) ;
#116713=EDGE_LOOP ( 'NONE', ( #26234, #33996, #48425, #131048, #28011, #76338 ) ) ;
#116730=VERTEX_POINT ( 'NONE', #141304 ) ;
#116764=ORIENTED_EDGE ( 'NONE', *, *, #75688, .F. ) ;
#116807=CARTESIAN_POINT ( 'NONE',  ( 7.326124847093153925, 4.202752102959690472E-16, 0.000000000000000000 ) ) ;
#116818=AXIS2_PLACEMENT_3D ( 'NONE', #131714, #143292, #109235 ) ;
#116841=DIRECTION ( 'NONE',  ( 0.000000000000000000, -1.000000000000000000, 0.000000000000000000 ) ) ;
#116897=DIRECTION ( 'NONE',  ( 0.000000000000000000, 0.000000000000000000, 1.000000000000000000 ) ) ;
#116912=AXIS2_PLACEMENT_3D ( 'NONE', #11223, #90244, #134487 ) ;
#116937=DIRECTION ( 'NONE',  ( 1.000000000000000000, 1.224606353822377258E-16, 0.000000000000000000 ) ) ;
#116961=CARTESIAN_POINT ( 'NONE',  ( 10.46799328145038821, -2.055000000000000160, 2.789133085058097101E-16 ) ) ;
#116975=CARTESIAN_POINT ( 'NONE',  ( 9.994118527364397764, 2.500000000000000444, 0.000000000000000000 ) ) ;
#117017=VERTEX_POINT ( 'NONE', #52000 ) ;
#117065=VERTEX_POINT ( 'NONE', #129534 ) ;
#117067=ORIENTED_EDGE ( 'NONE', *, *, #62141, .F. ) ;
#117092=EDGE_CURVE ( 'NONE', #75992, #52339, #19141, .T. ) ;
#117101=AXIS2_PLACEMENT_3D ( 'NONE', #137361, #58415, #115549 ) ;
#117165=DIRECTION ( 'NONE',  ( 8.673617379884034239E-17, -1.000000000000000000, 0.000000000000000000 ) ) ;
#117176=ADVANCED_FACE ( 'NONE', ( #2585 ), #112104, .T. ) ;
#117222=DIRECTION ( 'NONE',  ( 0.000000000000000000, -1.000000000000000000, 0.000000000000000000 ) ) ;
#117231=DIRECTION ( 'NONE',  ( 0.000000000000000000, 1.000000000000000000, 0.000000000000000000 ) ) ;
#117239=VERTEX_POINT ( 'NONE', #33145 ) ;
#117244=VECTOR ( 'NONE', #90220, 999.9999999999998863 ) ;
#117257=EDGE_CURVE ( 'NONE', #117989, #12173, #122225, .T. ) ;
#117290=AXIS2_PLACEMENT_3D ( 'NONE', #59133, #12711, #25011 ) ;
#117320=EDGE_CURVE ( 'NONE', #79680, #109461, #139151, .T. ) ;
#117364=CARTESIAN_POINT ( 'NONE',  ( 15.49238828748955576, -2.500000000000000000, 3.061616997868383634E-16 ) ) ;
#117396=ORIENTED_EDGE ( 'NONE', *, *, #6318, .T. ) ;
#117403=DIRECTION ( 'NONE',  ( -1.301042606982605074E-16, 1.000000000000000000, 0.000000000000000000 ) ) ;
#117417=ORIENTED_EDGE ( 'NONE', *, *, #12057, .F. ) ;
#117441=EDGE_CURVE ( 'NONE', #128359, #9541, #113657, .T. ) ;
#117444=CIRCLE ( 'NONE', #78169, 2.055000000000000604 ) ;
#117454=CARTESIAN_POINT ( 'NONE',  ( 6.540657738503846907, -2.055000000000000160, 0.000000000000000000 ) ) ;
#117486=ORIENTED_EDGE ( 'NONE', *, *, #2891, .F. ) ;
#117522=LINE ( 'NONE', #62470, #55913 ) ;
#117551=ORIENTED_EDGE ( 'NONE', *, *, #11134, .F. ) ;
#117558=DIRECTION ( 'NONE',  ( -1.000000000000000000, -1.224606353822377258E-16, -0.000000000000000000 ) ) ;
#117589=CARTESIAN_POINT ( 'NONE',  ( 10.77958563595370833, 4.584330080086930965E-16, 0.000000000000000000 ) ) ;
#117592=AXIS2_PLACEMENT_3D ( 'NONE', #83582, #28484, #116897 ) ;
#117615=CARTESIAN_POINT ( 'NONE',  ( 7.326124847093153925, -2.055000000000000160, 0.000000000000000000 ) ) ;
#117617=CARTESIAN_POINT ( 'NONE',  ( 18.79653912142945060, 4.333342374871280669E-31, 2.500000000000000444 ) ) ;
#117627=VECTOR ( 'NONE', #90531, 999.9999999999998863 ) ;
#117637=DIRECTION ( 'NONE',  ( 0.000000000000000000, -1.000000000000000000, 0.000000000000000000 ) ) ;
#117649=EDGE_CURVE ( 'NONE', #102047, #77315, #132988, .T. ) ;
#117693=ORIENTED_EDGE ( 'NONE', *, *, #19486, .F. ) ;
#117704=CARTESIAN_POINT ( 'NONE',  ( 9.994118527364397764, -2.500000000000000444, 3.061616997868384127E-16 ) ) ;
#117757=ORIENTED_EDGE ( 'NONE', *, *, #18869, .T. ) ;
#117775=EDGE_CURVE ( 'NONE', #101752, #103464, #137961, .T. ) ;
#117784=VECTOR ( 'NONE', #141930, 1000.000000000000000 ) ;
#117796=AXIS2_PLACEMENT_3D ( 'NONE', #118181, #21761, #63854 ) ;
#117887=EDGE_CURVE ( 'NONE', #53690, #137228, #8799, .T. ) ;
#117898=CARTESIAN_POINT ( 'NONE',  ( 12.82439460721831104, 4.202752102959690472E-16, 0.000000000000000000 ) ) ;
#117900=ORIENTED_EDGE ( 'NONE', *, *, #6137, .F. ) ;
#117931=VERTEX_POINT ( 'NONE', #17574 ) ;
#117943=DIRECTION ( 'NONE',  ( 0.000000000000000000, -1.000000000000000000, 0.000000000000000000 ) ) ;
#117971=CARTESIAN_POINT ( 'NONE',  ( 0.1630955410174109166, -0.4000000000000003553, 2.152173700565806591 ) ) ;
#117989=VERTEX_POINT ( 'NONE', #54531 ) ;
#117992=DIRECTION ( 'NONE',  ( -1.000000000000000000, -1.224606353822377258E-16, -0.000000000000000000 ) ) ;
#117993=ORIENTED_EDGE ( 'NONE', *, *, #62141, .T. ) ;
#118014=VECTOR ( 'NONE', #50156, 1000.000000000000000 ) ;
#118027=CIRCLE ( 'NONE', #60245, 2.055000000000000604 ) ;
#118033=CIRCLE ( 'NONE', #71514, 2.500000000000000444 ) ;
#118040=ORIENTED_EDGE ( 'NONE', *, *, #11216, .T. ) ;
#118052=ORIENTED_EDGE ( 'NONE', *, *, #76972, .F. ) ;
#118060=ORIENTED_EDGE ( 'NONE', *, *, #2891, .T. ) ;
#118097=DIRECTION ( 'NONE',  ( 0.000000000000000000, -1.000000000000000000, 0.000000000000000000 ) ) ;
#118110=CARTESIAN_POINT ( 'NONE',  ( 3.710381658649933634, 4.584330080086930965E-16, 0.000000000000000000 ) ) ;
#118123=AXIS2_PLACEMENT_3D ( 'NONE', #71354, #118395, #52427 ) ;
#118128=VERTEX_POINT ( 'NONE', #139769 ) ;
#118149=VERTEX_POINT ( 'NONE', #60796 ) ;
#118155=DIRECTION ( 'NONE',  ( -1.000000000000000000, -1.224606353822377258E-16, -0.000000000000000000 ) ) ;
#118173=DIRECTION ( 'NONE',  ( 0.000000000000000000, 0.000000000000000000, 1.000000000000000000 ) ) ;
#118178=AXIS2_PLACEMENT_3D ( 'NONE', #29729, #118155, #96401 ) ;
#118181=CARTESIAN_POINT ( 'NONE',  ( -12.69999999999998153, 0.000000000000000000, 0.000000000000000000 ) ) ;
#118200=ADVANCED_FACE ( 'NONE', ( #65796 ), #72330, .T. ) ;
#118212=CONICAL_SURFACE ( 'NONE', #53453, 2.055000000000000604, 0.9599310885968764806 ) ;
#118232=DIRECTION ( 'NONE',  ( -1.000000000000000000, -1.224606353822377258E-16, -0.000000000000000000 ) ) ;
#118240=AXIS2_PLACEMENT_3D ( 'NONE', #20531, #40892, #77119 ) ;
#118272=ADVANCED_FACE ( 'NONE', ( #129561 ), #127761, .T. ) ;
#118283=ORIENTED_EDGE ( 'NONE', *, *, #97270, .T. ) ;
#118287=CARTESIAN_POINT ( 'NONE',  ( 4.969723521325230209, 4.202752102959690472E-16, 0.000000000000000000 ) ) ;
#118294=EDGE_CURVE ( 'NONE', #130884, #31083, #2726, .T. ) ;
#118307=CARTESIAN_POINT ( 'NONE',  ( 14.39532882439692862, 2.055000000000001048, 0.000000000000000000 ) ) ;
#118308=DIRECTION ( 'NONE',  ( -1.000000000000000000, -0.000000000000000000, -0.000000000000000000 ) ) ;
#118395=DIRECTION ( 'NONE',  ( -1.000000000000000000, -1.224606353822377258E-16, -0.000000000000000000 ) ) ;
#118408=CARTESIAN_POINT ( 'NONE',  ( 15.49238828748955576, 2.500000000000000888, 0.000000000000000000 ) ) ;
#118423=AXIS2_PLACEMENT_3D ( 'NONE', #89002, #1227, #77427 ) ;
#118430=FACE_OUTER_BOUND ( 'NONE', #63688, .T. ) ;
#118440=EDGE_CURVE ( 'NONE', #7626, #96600, #125473, .T. ) ;
#118503=CIRCLE ( 'NONE', #12012, 2.500000000000000444 ) ;
#118548=LINE ( 'NONE', #19249, #83588 ) ;
#118588=CARTESIAN_POINT ( 'NONE',  ( 8.423184310185783730, 4.584330080086930965E-16, 0.000000000000000000 ) ) ;
#118590=CIRCLE ( 'NONE', #16762, 2.500000000000000444 ) ;
#118597=DIRECTION ( 'NONE',  ( -1.000000000000000000, -1.224606353822377258E-16, -0.000000000000000000 ) ) ;
#118599=AXIS2_PLACEMENT_3D ( 'NONE', #123219, #23890, #101433 ) ;
#118613=ORIENTED_EDGE ( 'NONE', *, *, #127014, .F. ) ;
#118626=DIRECTION ( 'NONE',  ( 0.000000000000000000, -1.000000000000000000, 0.000000000000000000 ) ) ;
#118650=ORIENTED_EDGE ( 'NONE', *, *, #115746, .F. ) ;
#118663=CARTESIAN_POINT ( 'NONE',  ( 3.087196949643289834, 3.821174125832445049E-16, 0.000000000000000000 ) ) ;
#118669=CONICAL_SURFACE ( 'NONE', #42331, 2.055000000000000604, 0.9599310885968764806 ) ;
#118700=EDGE_LOOP ( 'NONE', ( #58116, #85432, #86095, #121009, #134934 ) ) ;
#118821=ORIENTED_EDGE ( 'NONE', *, *, #61221, .F. ) ;
#118833=PRODUCT_DEFINITION_FORMATION_WITH_SPECIFIED_SOURCE ( 'ANY', '', #120757, .NOT_KNOWN. ) ;
#118850=EDGE_CURVE ( 'NONE', #19554, #98048, #72421, .T. ) ;
#118864=DIRECTION ( 'NONE',  ( 0.000000000000000000, -1.000000000000000000, 0.000000000000000000 ) ) ;
#118865=ORIENTED_EDGE ( 'NONE', *, *, #39435, .F. ) ;
#118893=DIRECTION ( 'NONE',  ( 1.000000000000000000, 1.224606353822377258E-16, 0.000000000000000000 ) ) ;
#118898=CARTESIAN_POINT ( 'NONE',  ( 14.08373646989360317, 3.821174125832445049E-16, 0.000000000000000000 ) ) ;
#118920=DIRECTION ( 'NONE',  ( -8.673617379884034239E-17, 1.000000000000000000, 0.000000000000000000 ) ) ;
#118938=VERTEX_POINT ( 'NONE', #125685 ) ;
#118950=CARTESIAN_POINT ( 'NONE',  ( 25.00000000000000000, 2.143131898507868051E-16, -1.749999999999999778 ) ) ;
#118952=CIRCLE ( 'NONE', #137497, 2.500000000000000444 ) ;
#118965=CARTESIAN_POINT ( 'NONE',  ( 5.755190629914537226, 2.055000000000001048, 0.000000000000000000 ) ) ;
#119018=ORIENTED_EDGE ( 'NONE', *, *, #136043, .T. ) ;
#119081=PLANE ( 'NONE',  #129324 ) ;
#119091=EDGE_CURVE ( 'NONE', #138500, #95435, #18297, .T. ) ;
#119120=CARTESIAN_POINT ( 'NONE',  ( 20.99065804761471199, -2.500000000000000000, 3.061616997868383634E-16 ) ) ;
#119242=DIRECTION ( 'NONE',  ( -1.000000000000000000, -1.224606353822377258E-16, -0.000000000000000000 ) ) ;
#119273=DIRECTION ( 'NONE',  ( -1.000000000000000000, -1.224606353822377258E-16, -0.000000000000000000 ) ) ;
#119343=EDGE_LOOP ( 'NONE', ( #7874, #93082, #75201, #36620, #13637 ) ) ;
#119358=DIRECTION ( 'NONE',  ( -0.5735764363510501562, 0.8191520442889890230, 1.003171929053521419E-16 ) ) ;
#119377=DIRECTION ( 'NONE',  ( -0.5735764363510501562, 0.8191520442889890230, 1.003171929053521419E-16 ) ) ;
#119385=DIRECTION ( 'NONE',  ( -1.000000000000000000, -1.224606353822377258E-16, -0.000000000000000000 ) ) ;
#119393=VERTEX_POINT ( 'NONE', #16732 ) ;
#119441=DIRECTION ( 'NONE',  ( -1.000000000000000000, -1.224606353822377258E-16, -0.000000000000000000 ) ) ;
#119442=EDGE_CURVE ( 'NONE', #67004, #92014, #93591, .T. ) ;
#119481=ORIENTED_EDGE ( 'NONE', *, *, #15821, .F. ) ;
#119511=CARTESIAN_POINT ( 'NONE',  ( 1.516262732464674023, -2.500000000000000000, 0.000000000000000000 ) ) ;
#119585=AXIS2_PLACEMENT_3D ( 'NONE', #124479, #114311, #69402 ) ;
#119633=CARTESIAN_POINT ( 'NONE',  ( 8.897059064271770623, 4.202752102959690472E-16, 0.000000000000000000 ) ) ;
#119652=CARTESIAN_POINT ( 'NONE',  ( 17.06332250466817158, 4.584330080086930965E-16, 0.000000000000000000 ) ) ;
#119666=CONICAL_SURFACE ( 'NONE', #96483, 2.055000000000000604, 0.9599310885968764806 ) ;
#119670=DIRECTION ( 'NONE',  ( 0.5735764363510448272, -0.8191520442889927978, 1.003171929053526103E-16 ) ) ;
#119685=DIRECTION ( 'NONE',  ( -1.000000000000000000, -1.224606353822377258E-16, -0.000000000000000000 ) ) ;
#119695=DIRECTION ( 'NONE',  ( -1.000000000000000000, -1.224606353822377258E-16, -0.000000000000000000 ) ) ;
#119730=ORIENTED_EDGE ( 'NONE', *, *, #52021, .F. ) ;
#119775=AXIS2_PLACEMENT_3D ( 'NONE', #97045, #96341, #118097 ) ;
#119839=FACE_OUTER_BOUND ( 'NONE', #48423, .T. ) ;
#119894=CARTESIAN_POINT ( 'NONE',  ( 13.29826936130429260, 3.821174125832445049E-16, 0.000000000000000000 ) ) ;
#119926=ORIENTED_EDGE ( 'NONE', *, *, #140222, .T. ) ;
#119988=VERTEX_POINT ( 'NONE', #84677 ) ;
#120003=CARTESIAN_POINT ( 'NONE',  ( 0.07735809023238590654, -0.3999999999999998002, -2.152165253127959144 ) ) ;
#120027=CARTESIAN_POINT ( 'NONE',  ( 1.146007053337370074, -0.3999999999999998002, -2.166563668000046405 ) ) ;
#120081=AXIS2_PLACEMENT_3D ( 'NONE', #64373, #108543, #28893 ) ;
#120114=ORIENTED_EDGE ( 'NONE', *, *, #123288, .F. ) ;
#120152=EDGE_LOOP ( 'NONE', ( #34813, #81076, #50840, #68318, #77938, #41278 ) ) ;
#120207=AXIS2_PLACEMENT_3D ( 'NONE', #133032, #141754, #30853 ) ;
#120212=VERTEX_POINT ( 'NONE', #55502 ) ;
#120219=ADVANCED_FACE ( 'NONE', ( #33761 ), #101841, .T. ) ;
#120307=DIRECTION ( 'NONE',  ( -1.000000000000000000, -0.000000000000000000, -0.000000000000000000 ) ) ;
#120355=DIRECTION ( 'NONE',  ( 0.000000000000000000, -1.000000000000000000, 0.000000000000000000 ) ) ;
#120377=CIRCLE ( 'NONE', #88032, 2.500000000000000444 ) ;
#120386=ADVANCED_FACE ( 'NONE', ( #15504 ), #24975, .T. ) ;
#120402=CARTESIAN_POINT ( 'NONE',  ( 16.44013779566152778, 3.821174125832445049E-16, 0.000000000000000000 ) ) ;
#120417=EDGE_LOOP ( 'NONE', ( #23071, #134892, #40655, #117396, #85900 ) ) ;
#120468=CIRCLE ( 'NONE', #111511, 2.500000000000000444 ) ;
#120476=CONICAL_SURFACE ( 'NONE', #129718, 2.055000000000000604, 0.9599310885968764806 ) ;
#120496=AXIS2_PLACEMENT_3D ( 'NONE', #138580, #95772, #71194 ) ;
#120557=CIRCLE ( 'NONE', #4725, 2.500000000000000444 ) ;
#120561=CARTESIAN_POINT ( 'NONE',  ( -12.69999999999998153, 0.000000000000000000, 2.500000000000000444 ) ) ;
#120601=EDGE_CURVE ( 'NONE', #12106, #82511, #135570, .T. ) ;
#120649=ADVANCED_FACE ( 'NONE', ( #69610 ), #45719, .T. ) ;
#120661=FACE_OUTER_BOUND ( 'NONE', #123328, .T. ) ;
#120757=PRODUCT ( 'slotted set screw dog point_iso_ISO 7435 - M5 x 25-S', 'slotted set screw dog point_iso_ISO 7435 - M5 x 25-S', '', ( #104001 ) ) ;
#120772=VECTOR ( 'NONE', #86470, 1000.000000000000000 ) ;
#120777=CARTESIAN_POINT ( 'NONE',  ( 19.41972383043609440, 4.584330080086930965E-16, 0.000000000000000000 ) ) ;
#120781=DIRECTION ( 'NONE',  ( 0.000000000000000000, -1.000000000000000000, 0.000000000000000000 ) ) ;
#120809=ORIENTED_EDGE ( 'NONE', *, *, #7084, .F. ) ;
#120839=LINE ( 'NONE', #110652, #132012 ) ;
#120889=EDGE_CURVE ( 'NONE', #69156, #42684, #18004, .T. ) ;
#120897=DIRECTION ( 'NONE',  ( 0.000000000000000000, -1.000000000000000000, 0.000000000000000000 ) ) ;
#120915=DIRECTION ( 'NONE',  ( 0.5735764363510448272, -0.8191520442889927978, 1.003171929053526103E-16 ) ) ;
#120934=CARTESIAN_POINT ( 'NONE',  ( 1.042387978378689795, -2.055000000000000160, 0.000000000000000000 ) ) ;
#120957=B_SPLINE_CURVE_WITH_KNOTS ( 'NONE', 3,
 ( #79368, #46001, #24231, #67019 ),
 .UNSPECIFIED., .F., .F.,
 ( 4, 4 ),
 ( 0.003615568590623256459, 0.004164643302645746996 ),
 .UNSPECIFIED. ) ;
#121009=ORIENTED_EDGE ( 'NONE', *, *, #106256, .F. ) ;
#121034=CARTESIAN_POINT ( 'NONE',  ( 13.13598696172163116, 4.584330080086930965E-16, 0.000000000000000000 ) ) ;
#121067=AXIS2_PLACEMENT_3D ( 'NONE', #56614, #31426, #68889 ) ;
#121073=EDGE_CURVE ( 'NONE', #25809, #136698, #59317, .T. ) ;
#121115=VECTOR ( 'NONE', #79281, 999.9999999999998863 ) ;
#121119=VERTEX_POINT ( 'NONE', #70858 ) ;
#121123=LINE ( 'NONE', #99350, #46877 ) ;
#121182=ADVANCED_FACE ( 'NONE', ( #6236 ), #103246, .T. ) ;
#121215=FACE_OUTER_BOUND ( 'NONE', #108247, .T. ) ;
#121235=AXIS2_PLACEMENT_3D ( 'NONE', #40120, #116216, #51689 ) ;
#121262=DIRECTION ( 'NONE',  ( 0.5735764363510444941, 0.8191520442889929088, 0.000000000000000000 ) ) ;
#121273=EDGE_CURVE ( 'NONE', #7243, #141894, #77710, .T. ) ;
#121286=CIRCLE ( 'NONE', #26307, 2.500000000000000444 ) ;
#121301=EDGE_CURVE ( 'NONE', #44009, #104716, #5944, .T. ) ;
#121303=AXIS2_PLACEMENT_3D ( 'NONE', #111944, #99597, #45281 ) ;
#121336=EDGE_CURVE ( 'NONE', #102047, #33411, #80114, .T. ) ;
#121337=ORIENTED_EDGE ( 'NONE', *, *, #27374, .T. ) ;
#121345=DIRECTION ( 'NONE',  ( 0.000000000000000000, -1.000000000000000000, 0.000000000000000000 ) ) ;
#121377=ORIENTED_EDGE ( 'NONE', *, *, #17042, .F. ) ;
#121456=CARTESIAN_POINT ( 'NONE',  ( 20.20519093902540320, 3.061616997868383634E-16, -2.500000000000000444 ) ) ;
#121481=LINE ( 'NONE', #86008, #12089 ) ;
#121501=AXIS2_PLACEMENT_3D ( 'NONE', #47765, #68795, #80384 ) ;
#121505=DIRECTION ( 'NONE',  ( -1.000000000000000000, -1.224606353822377258E-16, -0.000000000000000000 ) ) ;
#121526=EDGE_CURVE ( 'NONE', #2478, #16173, #36119, .T. ) ;
#121545=AXIS2_PLACEMENT_3D ( 'NONE', #37884, #60351, #116841 ) ;
#121564=LINE ( 'NONE', #487, #18861 ) ;
#121565=VERTEX_POINT ( 'NONE', #16239 ) ;
#121568=ORIENTED_EDGE ( 'NONE', *, *, #89791, .T. ) ;
#121581=CARTESIAN_POINT ( 'NONE',  ( 5.755190629914537226, 2.055000000000001048, 2.516649172247811554E-16 ) ) ;
#121584=ADVANCED_FACE ( 'NONE', ( #3245 ), #71386, .T. ) ;
#121648=DIRECTION ( 'NONE',  ( 0.000000000000000000, -1.000000000000000000, 0.000000000000000000 ) ) ;
#121682=ORIENTED_EDGE ( 'NONE', *, *, #135795, .T. ) ;
#121746=CARTESIAN_POINT ( 'NONE',  ( 15.18079593298623564, 2.055000000000001048, 2.516649172247811554E-16 ) ) ;
#121766=FACE_OUTER_BOUND ( 'NONE', #40223, .T. ) ;
#121776=ORIENTED_EDGE ( 'NONE', *, *, #97143, .F. ) ;
#121782=DIRECTION ( 'NONE',  ( -1.000000000000000000, -1.224606353822377258E-16, -0.000000000000000000 ) ) ;
#121806=DIRECTION ( 'NONE',  ( 0.000000000000000000, -1.000000000000000000, 0.000000000000000000 ) ) ;
#121818=ORIENTED_EDGE ( 'NONE', *, *, #56937, .F. ) ;
#121849=VERTEX_POINT ( 'NONE', #76389 ) ;
#121866=CONICAL_SURFACE ( 'NONE', #119585, 2.500000000000000444, 0.9599310885968830309 ) ;
#121878=ORIENTED_EDGE ( 'NONE', *, *, #127434, .T. ) ;
#121930=DIRECTION ( 'NONE',  ( -1.000000000000000000, -0.000000000000000000, -0.000000000000000000 ) ) ;
#121934=DIRECTION ( 'NONE',  ( 0.5735764363510444941, 0.8191520442889929088, 0.000000000000000000 ) ) ;
#121969=VERTEX_POINT ( 'NONE', #116132 ) ;
#121981=EDGE_CURVE ( 'NONE', #22757, #137228, #12995, .T. ) ;
#121983=DIRECTION ( 'NONE',  ( 0.5735764363510448272, -0.8191520442889927978, 1.003171929053526103E-16 ) ) ;
#122023=CARTESIAN_POINT ( 'NONE',  ( 0.000000000000000000, -0.3999999999999998002, -2.015694669338588429 ) ) ;
#122054=DIRECTION ( 'NONE',  ( 0.5735764363510448272, -0.8191520442889927978, 1.003171929053526103E-16 ) ) ;
#122066=EDGE_CURVE ( 'NONE', #63283, #18713, #105703, .T. ) ;
#122106=CARTESIAN_POINT ( 'NONE',  ( 2.301729841053981040, 2.500000000000000444, 3.061616997868383634E-16 ) ) ;
#122143=CONICAL_SURFACE ( 'NONE', #8681, 2.500000000000000444, 0.9599310885968830309 ) ;
#122165=CARTESIAN_POINT ( 'NONE',  ( -12.69999999999998153, 0.000000000000000000, 0.000000000000000000 ) ) ;
#122178=DIRECTION ( 'NONE',  ( -1.000000000000000000, -1.224606353822377258E-16, -0.000000000000000000 ) ) ;
#122214=ORIENTED_EDGE ( 'NONE', *, *, #28782, .T. ) ;
#122221=DIRECTION ( 'NONE',  ( 0.000000000000000000, -1.000000000000000000, 0.000000000000000000 ) ) ;
#122222=VERTEX_POINT ( 'NONE', #70197 ) ;
#122225=LINE ( 'NONE', #66459, #35055 ) ;
#122233=VERTEX_POINT ( 'NONE', #3431 ) ;
#122249=VERTEX_POINT ( 'NONE', #31983 ) ;
#122282=ORIENTED_EDGE ( 'NONE', *, *, #4013, .T. ) ;
#122312=CARTESIAN_POINT ( 'NONE',  ( 12.51280225271498736, 3.821174125832445049E-16, 0.000000000000000000 ) ) ;
#122358=EDGE_CURVE ( 'NONE', #61548, #87797, #40394, .T. ) ;
#122362=ORIENTED_EDGE ( 'NONE', *, *, #65154, .T. ) ;
#122416=LINE ( 'NONE', #46343, #117627 ) ;
#122503=CIRCLE ( 'NONE', #94754, 2.500000000000000444 ) ;
#122504=EDGE_CURVE ( 'NONE', #88783, #69001, #68769, .T. ) ;
#122567=CIRCLE ( 'NONE', #20640, 2.500000000000000444 ) ;
#122572=CARTESIAN_POINT ( 'NONE',  ( -12.69999999999998153, -0.3999999999999997446, -2.467792535850613866 ) ) ;
#122577=ORIENTED_EDGE ( 'NONE', *, *, #125814, .F. ) ;
#122602=CIRCLE ( 'NONE', #34672, 2.500000000000000444 ) ;
#122654=DIRECTION ( 'NONE',  ( 1.000000000000000000, 1.224606353822377258E-16, 0.000000000000000000 ) ) ;
#122698=CARTESIAN_POINT ( 'NONE',  ( 20.20519093902540320, -2.500000000000000444, 3.061616997868384127E-16 ) ) ;
#122704=ADVANCED_FACE ( 'NONE', ( #114866 ), #52637, .T. ) ;
#122715=CARTESIAN_POINT ( 'NONE',  ( 2.301729841053981485, 3.821174125832445049E-16, 0.000000000000000000 ) ) ;
#122723=CARTESIAN_POINT ( 'NONE',  ( 2.139447441471316935, 2.500000000000000888, 0.000000000000000000 ) ) ;
#122742=CARTESIAN_POINT ( 'NONE',  ( 1.516262732464673579, -0.3999999999999997446, -2.467792535850613866 ) ) ;
#122748=EDGE_CURVE ( 'NONE', #15589, #52339, #133684, .T. ) ;
#122778=CARTESIAN_POINT ( 'NONE',  ( -12.69999999999998153, 0.000000000000000000, 0.000000000000000000 ) ) ;
#122791=VERTEX_POINT ( 'NONE', #70015 ) ;
#122805=VECTOR ( 'NONE', #131085, 999.9999999999998863 ) ;
#122858=CARTESIAN_POINT ( 'NONE',  ( 16.27785539607886633, 4.584330080086930965E-16, 0.000000000000000000 ) ) ;
#122877=CARTESIAN_POINT ( 'NONE',  ( 2.139447441471317379, 4.584330080086930965E-16, 0.000000000000000000 ) ) ;
#122881=ORIENTED_EDGE ( 'NONE', *, *, #5537, .F. ) ;
#122901=DIRECTION ( 'NONE',  ( 0.000000000000000000, -1.000000000000000000, 0.000000000000000000 ) ) ;
#122914=AXIS2_PLACEMENT_3D ( 'NONE', #104562, #81422, #71972 ) ;
#122940=DIRECTION ( 'NONE',  ( -1.000000000000000000, -0.000000000000000000, -0.000000000000000000 ) ) ;
#122953=CIRCLE ( 'NONE', #90572, 2.500000000000000444 ) ;
#122954=DIRECTION ( 'NONE',  ( 0.000000000000000000, -1.000000000000000000, 0.000000000000000000 ) ) ;
#122985=ORIENTED_EDGE ( 'NONE', *, *, #81151, .T. ) ;
#122987=DIRECTION ( 'NONE',  ( -1.000000000000000000, -0.000000000000000000, -0.000000000000000000 ) ) ;
#122991=ORIENTED_EDGE ( 'NONE', *, *, #65785, .F. ) ;
#123025=AXIS2_PLACEMENT_3D ( 'NONE', #50736, #28984, #8596 ) ;
#123031=EDGE_LOOP ( 'NONE', ( #130463, #99242, #126099, #23747, #10421 ) ) ;
#123047=DIRECTION ( 'NONE',  ( 0.000000000000000000, 1.000000000000000000, 0.000000000000000000 ) ) ;
#123064=DIRECTION ( 'NONE',  ( 1.055184596092948005E-16, -1.000000000000000000, 0.000000000000000000 ) ) ;
#123079=CARTESIAN_POINT ( 'NONE',  ( 20.20519093902540320, 2.500000000000000888, 0.000000000000000000 ) ) ;
#123112=VECTOR ( 'NONE', #106873, 1000.000000000000000 ) ;
#123116=CIRCLE ( 'NONE', #16591, 2.055000000000000604 ) ;
#123119=CYLINDRICAL_SURFACE ( 'NONE', #9935, 2.500000000000000444 ) ;
#123165=DIRECTION ( 'NONE',  ( -1.000000000000000000, -1.224606353822377258E-16, -0.000000000000000000 ) ) ;
#123170=FACE_OUTER_BOUND ( 'NONE', #15089, .T. ) ;
#123219=CARTESIAN_POINT ( 'NONE',  ( 20.99065804761471199, 4.584330080086930965E-16, 0.000000000000000000 ) ) ;
#123288=EDGE_CURVE ( 'NONE', #101443, #19509, #99800, .T. ) ;
#123295=CONICAL_SURFACE ( 'NONE', #32960, 2.055000000000000604, 0.9599310885968764806 ) ;
#123301=ORIENTED_EDGE ( 'NONE', *, *, #114354, .T. ) ;
#123317=CARTESIAN_POINT ( 'NONE',  ( 0.1161069444170879233, 0.4000000000000001332, -2.220360628129161462 ) ) ;
#123328=EDGE_LOOP ( 'NONE', ( #114879, #23775, #15288, #12090, #21320 ) ) ;
#123358=CONICAL_SURFACE ( 'NONE', #132689, 2.500000000000000444, 0.9599310885968830309 ) ;
#123404=CARTESIAN_POINT ( 'NONE',  ( 0.5685132242927009028, 2.500000000000000888, 0.000000000000000000 ) ) ;
#123430=ORIENTED_EDGE ( 'NONE', *, *, #379, .F. ) ;
#123453=DIRECTION ( 'NONE',  ( 2.110369192185896011E-16, -1.000000000000000000, 0.000000000000000000 ) ) ;
#123477=AXIS2_PLACEMENT_3D ( 'NONE', #133022, #33701, #90939 ) ;
#123480=EDGE_CURVE ( 'NONE', #98048, #77315, #6330, .T. ) ;
#123530=LINE ( 'NONE', #136501, #66730 ) ;
#123559=CARTESIAN_POINT ( 'NONE',  ( 14.39532882439692862, 4.202752102959690472E-16, 0.000000000000000000 ) ) ;
#123576=DIRECTION ( 'NONE',  ( 0.000000000000000000, 0.000000000000000000, 1.000000000000000000 ) ) ;
#123587=DIRECTION ( 'NONE',  ( 0.000000000000000000, -1.000000000000000000, 0.000000000000000000 ) ) ;
#123602=DIRECTION ( 'NONE',  ( 0.000000000000000000, -1.000000000000000000, 0.000000000000000000 ) ) ;
#123603=ORIENTED_EDGE ( 'NONE', *, *, #5206, .T. ) ;
#123604=DIRECTION ( 'NONE',  ( 0.000000000000000000, -1.000000000000000000, 0.000000000000000000 ) ) ;
#123608=DIRECTION ( 'NONE',  ( -1.000000000000000000, -1.224606353822377258E-16, -0.000000000000000000 ) ) ;
#123611=CARTESIAN_POINT ( 'NONE',  ( 1.353980332882009252, 0.4000000000000001887, -2.467792535850613866 ) ) ;
#123615=CIRCLE ( 'NONE', #19369, 2.500000000000000444 ) ;
#123638=VERTEX_POINT ( 'NONE', #68087 ) ;
#123643=EDGE_CURVE ( 'NONE', #88783, #93815, #43440, .T. ) ;
#123656=CARTESIAN_POINT ( 'NONE',  ( 19.89359858452208130, 4.202752102959690472E-16, 0.000000000000000000 ) ) ;
#123664=CIRCLE ( 'NONE', #121235, 2.500000000000000444 ) ;
#123694=DIRECTION ( 'NONE',  ( -1.000000000000000000, -0.000000000000000000, 0.000000000000000000 ) ) ;
#123696=DIRECTION ( 'NONE',  ( 1.000000000000000000, 1.224606353822377258E-16, 0.000000000000000000 ) ) ;
#123710=CYLINDRICAL_SURFACE ( 'NONE', #16513, 2.500000000000000444 ) ;
#123723=AXIS2_PLACEMENT_3D ( 'NONE', #127040, #127789, #19710 ) ;
#123779=DIRECTION ( 'NONE',  ( 0.000000000000000000, 0.000000000000000000, 1.000000000000000000 ) ) ;
#123847=( LENGTH_UNIT ( ) NAMED_UNIT ( * ) SI_UNIT ( .MILLI., .METRE. ) );
#123855=ADVANCED_FACE ( 'NONE', ( #52694 ), #112968, .T. ) ;
#123877=CONICAL_SURFACE ( 'NONE', #54456, 2.500000000000000444, 0.9599310885968830309 ) ;
#123895=VERTEX_POINT ( 'NONE', #84630 ) ;
#123960=VECTOR ( 'NONE', #47831, 1000.000000000000000 ) ;
#123977=VECTOR ( 'NONE', #26780, 1000.000000000000000 ) ;
#123998=EDGE_CURVE ( 'NONE', #84085, #82511, #123530, .T. ) ;
#124115=VERTEX_POINT ( 'NONE', #118307 ) ;
#124188=CARTESIAN_POINT ( 'NONE',  ( 13.13598696172163116, -2.500000000000000444, 3.061616997868384127E-16 ) ) ;
#124193=ADVANCED_FACE ( 'NONE', ( #84308 ), #29873, .T. ) ;
#124273=AXIS2_PLACEMENT_3D ( 'NONE', #133931, #34618, #123064 ) ;
#124291=VERTEX_POINT ( 'NONE', #11667 ) ;
#124372=ORIENTED_EDGE ( 'NONE', *, *, #41510, .F. ) ;
#124401=ORIENTED_EDGE ( 'NONE', *, *, #17851, .F. ) ;
#124479=CARTESIAN_POINT ( 'NONE',  ( 18.63425672184678916, 4.584330080086930965E-16, 0.000000000000000000 ) ) ;
#124588=ORIENTED_EDGE ( 'NONE', *, *, #43739, .F. ) ;
#124639=CARTESIAN_POINT ( 'NONE',  ( 20.20519093902540320, 4.584330080086930965E-16, 0.000000000000000000 ) ) ;
#124641=DIRECTION ( 'NONE',  ( -1.000000000000000000, -1.224606353822377258E-16, -0.000000000000000000 ) ) ;
#124671=DIRECTION ( 'NONE',  ( -1.000000000000000000, -0.000000000000000000, -0.000000000000000000 ) ) ;
#124683=DIRECTION ( 'NONE',  ( -1.000000000000000000, -0.000000000000000000, -0.000000000000000000 ) ) ;
#124696=CONICAL_SURFACE ( 'NONE', #13521, 2.500000000000000444, 0.9599310885968830309 ) ;
#124724=VERTEX_POINT ( 'NONE', #68802 ) ;
#124734=ORIENTED_EDGE ( 'NONE', *, *, #6001, .T. ) ;
#124755=CIRCLE ( 'NONE', #29845, 2.500000000000000444 ) ;
#124846=ORIENTED_EDGE ( 'NONE', *, *, #141959, .T. ) ;
#124856=ADVANCED_FACE ( 'NONE', ( #59358 ), #131709, .T. ) ;
#124864=AXIS2_PLACEMENT_3D ( 'NONE', #117589, #61846, #7415 ) ;
#124884=CARTESIAN_POINT ( 'NONE',  ( 2.139447441471316935, 2.500000000000000888, 0.000000000000000000 ) ) ;
#124892=AXIS2_PLACEMENT_3D ( 'NONE', #11048, #101659, #1602 ) ;
#124898=VECTOR ( 'NONE', #106586, 1000.000000000000000 ) ;
#124914=ORIENTED_EDGE ( 'NONE', *, *, #91991, .F. ) ;
#124923=CARTESIAN_POINT ( 'NONE',  ( 15.65467068707222076, 0.000000000000000000, 2.500000000000000444 ) ) ;
#124957=DIRECTION ( 'NONE',  ( 0.000000000000000000, 1.000000000000000000, 0.000000000000000000 ) ) ;
#124968=CARTESIAN_POINT ( 'NONE',  ( -12.69999999999998153, 3.061616997868383634E-16, -2.500000000000000444 ) ) ;
#124993=ORIENTED_EDGE ( 'NONE', *, *, #122504, .T. ) ;
#125006=DIRECTION ( 'NONE',  ( -1.000000000000000000, -1.224606353822377258E-16, -0.000000000000000000 ) ) ;
#125100=CIRCLE ( 'NONE', #25549, 2.055000000000000604 ) ;
#125164=CONICAL_SURFACE ( 'NONE', #48811, 2.500000000000000444, 0.9599310885968830309 ) ;
#125180=CIRCLE ( 'NONE', #134406, 2.500000000000000444 ) ;
#125189=DIRECTION ( 'NONE',  ( 0.000000000000000000, 0.000000000000000000, 1.000000000000000000 ) ) ;
#125313=DIRECTION ( 'NONE',  ( 0.000000000000000000, 1.000000000000000000, 0.000000000000000000 ) ) ;
#125328=CONICAL_SURFACE ( 'NONE', #74434, 2.055000000000000604, 0.9599310885968764806 ) ;
#125331=DIRECTION ( 'NONE',  ( -1.000000000000000000, -1.224606353822377258E-16, -0.000000000000000000 ) ) ;
#125333=CIRCLE ( 'NONE', #62851, 2.500000000000000444 ) ;
#125351=FACE_OUTER_BOUND ( 'NONE', #97262, .T. ) ;
#125390=VECTOR ( 'NONE', #139961, 999.9999999999998863 ) ;
#125402=ORIENTED_EDGE ( 'NONE', *, *, #48969, .T. ) ;
#125419=ORIENTED_EDGE ( 'NONE', *, *, #15457, .F. ) ;
#125461=ORIENTED_EDGE ( 'NONE', *, *, #117887, .F. ) ;
#125473=CIRCLE ( 'NONE', #62993, 2.500000000000000444 ) ;
#125475=CARTESIAN_POINT ( 'NONE',  ( 0.1161069444170877152, -0.3999999999999998002, -2.220360628129161906 ) ) ;
#125528=ORIENTED_EDGE ( 'NONE', *, *, #99659, .F. ) ;
#125568=ORIENTED_EDGE ( 'NONE', *, *, #103649, .T. ) ;
#125578=DIRECTION ( 'NONE',  ( 0.000000000000000000, -1.000000000000000000, 0.000000000000000000 ) ) ;
#125581=DIRECTION ( 'NONE',  ( -1.000000000000000000, -1.224606353822377258E-16, -0.000000000000000000 ) ) ;
#125633=DIRECTION ( 'NONE',  ( 0.000000000000000000, 0.000000000000000000, 1.000000000000000000 ) ) ;
#125648=CIRCLE ( 'NONE', #141803, 2.500000000000000444 ) ;
#125666=CARTESIAN_POINT ( 'NONE',  ( 19.58200623001875940, 3.821174125832445049E-16, 0.000000000000000000 ) ) ;
#125685=CARTESIAN_POINT ( 'NONE',  ( 17.84878961325748037, 3.061616997868383634E-16, -2.500000000000000444 ) ) ;
#125780=ORIENTED_EDGE ( 'NONE', *, *, #134919, .T. ) ;
#125787=EDGE_LOOP ( 'NONE', ( #75100, #34928, #73586, #54984, #34833 ) ) ;
#125808=SHAPE_DEFINITION_REPRESENTATION ( #132402, #64389 ) ;
#125814=EDGE_CURVE ( 'NONE', #61548, #95615, #142100, .T. ) ;
#125848=EDGE_CURVE ( 'NONE', #133129, #59855, #80698, .T. ) ;
#125863=ORIENTED_EDGE ( 'NONE', *, *, #99791, .F. ) ;
#125896=VERTEX_POINT ( 'NONE', #58697 ) ;
#125910=DIRECTION ( 'NONE',  ( 0.000000000000000000, -1.000000000000000000, 0.000000000000000000 ) ) ;
#125921=DIRECTION ( 'NONE',  ( 0.000000000000000000, 0.000000000000000000, 1.000000000000000000 ) ) ;
#125938=CARTESIAN_POINT ( 'NONE',  ( 11.72733514412567857, 0.000000000000000000, 2.500000000000000444 ) ) ;
#125949=ORIENTED_EDGE ( 'NONE', *, *, #137121, .F. ) ;
#125957=CARTESIAN_POINT ( 'NONE',  ( 0.5685132242927012358, -0.3999999999999997446, -2.467792535850613866 ) ) ;
#126014=FACE_OUTER_BOUND ( 'NONE', #96546, .T. ) ;
#126055=CARTESIAN_POINT ( 'NONE',  ( 10.77958563595370833, 4.584330080086930965E-16, 0.000000000000000000 ) ) ;
#126081=EDGE_CURVE ( 'NONE', #59855, #108385, #132497, .T. ) ;
#126099=ORIENTED_EDGE ( 'NONE', *, *, #119091, .T. ) ;
#126112=CARTESIAN_POINT ( 'NONE',  ( -12.69999999999998153, 0.4000000000000001887, -2.467792535850613866 ) ) ;
#126226=ORIENTED_EDGE ( 'NONE', *, *, #80186, .F. ) ;
#126296=CARTESIAN_POINT ( 'NONE',  ( 0.2569208697893814453, 4.202752102959690472E-16, 0.000000000000000000 ) ) ;
#126326=CARTESIAN_POINT ( 'NONE',  ( 19.41972383043609440, 4.584330080086930965E-16, 0.000000000000000000 ) ) ;
#126332=VERTEX_POINT ( 'NONE', #58522 ) ;
#126357=ORIENTED_EDGE ( 'NONE', *, *, #51031, .T. ) ;
#126390=DIRECTION ( 'NONE',  ( 0.000000000000000000, -1.000000000000000000, 0.000000000000000000 ) ) ;
#126407=EDGE_CURVE ( 'NONE', #31083, #23744, #124755, .T. ) ;
#126466=CIRCLE ( 'NONE', #3703, 2.500000000000000444 ) ;
#126491=VERTEX_POINT ( 'NONE', #139632 ) ;
#126498=EDGE_LOOP ( 'NONE', ( #94735, #25520, #6587, #126949, #72635 ) ) ;
#126510=CARTESIAN_POINT ( 'NONE',  ( 17.22560490425083657, 3.821174125832445049E-16, 0.000000000000000000 ) ) ;
#126511=DIRECTION ( 'NONE',  ( 0.000000000000000000, 0.000000000000000000, -1.000000000000000000 ) ) ;
#126629=CIRCLE ( 'NONE', #20142, 2.055000000000000160 ) ;
#126635=DIRECTION ( 'NONE',  ( -1.000000000000000000, -0.000000000000000000, -0.000000000000000000 ) ) ;
#126682=ORIENTED_EDGE ( 'NONE', *, *, #115714, .T. ) ;
#126704=CARTESIAN_POINT ( 'NONE',  ( -12.69999999999998153, 0.000000000000000000, 0.000000000000000000 ) ) ;
#126736=DIRECTION ( 'NONE',  ( -1.000000000000000000, -1.224606353822377258E-16, -0.000000000000000000 ) ) ;
#126748=CONICAL_SURFACE ( 'NONE', #24931, 2.055000000000000604, 0.9599310885968764806 ) ;
#126749=ORIENTED_EDGE ( 'NONE', *, *, #111050, .F. ) ;
#126761=EDGE_CURVE ( 'NONE', #82511, #12106, #78512, .T. ) ;
#126764=CARTESIAN_POINT ( 'NONE',  ( -12.69999999999998153, 0.000000000000000000, 0.000000000000000000 ) ) ;
#126808=CONICAL_SURFACE ( 'NONE', #75916, 2.055000000000000604, 0.9599310885968764806 ) ;
#126814=DIRECTION ( 'NONE',  ( 0.5735764363510448272, -0.8191520442889927978, 1.003171929053526103E-16 ) ) ;
#126823=DIRECTION ( 'NONE',  ( 0.5735764363510448272, -0.8191520442889927978, 1.003171929053526103E-16 ) ) ;
#126853=ORIENTED_EDGE ( 'NONE', *, *, #93938, .F. ) ;
#126895=ORIENTED_EDGE ( 'NONE', *, *, #2977, .T. ) ;
#126934=CARTESIAN_POINT ( 'NONE',  ( 21.66240673564756491, 2.337593264352435085, 0.000000000000000000 ) ) ;
#126949=ORIENTED_EDGE ( 'NONE', *, *, #54109, .F. ) ;
#127014=EDGE_CURVE ( 'NONE', #101752, #45062, #36301, .T. ) ;
#127040=CARTESIAN_POINT ( 'NONE',  ( 6.229065384000522343, 3.821174125832445049E-16, 0.000000000000000000 ) ) ;
#127065=VERTEX_POINT ( 'NONE', #47916 ) ;
#127067=EDGE_CURVE ( 'NONE', #102743, #122233, #2082, .T. ) ;
#127109=FACE_OUTER_BOUND ( 'NONE', #109926, .T. ) ;
#127161=AXIS2_PLACEMENT_3D ( 'NONE', #56269, #45379, #133784 ) ;
#127181=DIRECTION ( 'NONE',  ( -0.5735764363510501562, 0.8191520442889890230, 1.003171929053521419E-16 ) ) ;
#127201=CARTESIAN_POINT ( 'NONE',  ( 0.1161069444170876597, 0.000000000000000000, 0.000000000000000000 ) ) ;
#127221=CONICAL_SURFACE ( 'NONE', #64738, 2.500000000000000444, 0.9599310885968830309 ) ;
#127228=EDGE_LOOP ( 'NONE', ( #97910, #66162, #95390, #88360, #23171 ) ) ;
#127229=EDGE_CURVE ( 'NONE', #31359, #29345, #76336, .T. ) ;
#127289=EDGE_CURVE ( 'NONE', #139436, #36014, #25098, .T. ) ;
#127351=DIRECTION ( 'NONE',  ( 0.000000000000000000, -1.000000000000000000, 0.000000000000000000 ) ) ;
#127358=AXIS2_PLACEMENT_3D ( 'NONE', #20836, #87541, #42639 ) ;
#127363=CARTESIAN_POINT ( 'NONE',  ( 16.27785539607886633, 4.584330080086930965E-16, 0.000000000000000000 ) ) ;
#127373=EDGE_CURVE ( 'NONE', #140226, #112363, #62055, .T. ) ;
#127384=ORIENTED_EDGE ( 'NONE', *, *, #12697, .F. ) ;
#127385=ADVANCED_FACE ( 'NONE', ( #104815 ), #55543, .T. ) ;
#127428=ORIENTED_EDGE ( 'NONE', *, *, #116687, .F. ) ;
#127434=EDGE_CURVE ( 'NONE', #28611, #110962, #41651, .T. ) ;
#127442=CARTESIAN_POINT ( 'NONE',  ( 0.000000000000000000, 0.000000000000000000, 0.000000000000000000 ) ) ;
#127492=ADVANCED_FACE ( 'NONE', ( #100897 ), #127221, .T. ) ;
#127537=EDGE_CURVE ( 'NONE', #16019, #142252, #68322, .T. ) ;
#127546=DIRECTION ( 'NONE',  ( 0.000000000000000000, 1.000000000000000000, 0.000000000000000000 ) ) ;
#127549=CARTESIAN_POINT ( 'NONE',  ( 14.08373646989360317, 3.061616997868383634E-16, -2.500000000000000444 ) ) ;
#127561=AXIS2_PLACEMENT_3D ( 'NONE', #93991, #115000, #106270 ) ;
#127576=EDGE_LOOP ( 'NONE', ( #67081, #29635, #85618, #104517, #49692, #117993 ) ) ;
#127619=ORIENTED_EDGE ( 'NONE', *, *, #59101, .F. ) ;
#127642=ORIENTED_EDGE ( 'NONE', *, *, #77224, .F. ) ;
#127690=ORIENTED_EDGE ( 'NONE', *, *, #89791, .F. ) ;
#127738=ORIENTED_EDGE ( 'NONE', *, *, #34013, .F. ) ;
#127757=CARTESIAN_POINT ( 'NONE',  ( 14.08373646989360317, -2.500000000000001776, 0.000000000000000000 ) ) ;
#127761=CONICAL_SURFACE ( 'NONE', #65271, 2.055000000000000604, 0.9599310885968764806 ) ;
#127762=CIRCLE ( 'NONE', #60738, 2.500000000000000444 ) ;
#127767=VECTOR ( 'NONE', #49811, 1000.000000000000000 ) ;
#127789=DIRECTION ( 'NONE',  ( -1.000000000000000000, -1.224606353822377258E-16, -0.000000000000000000 ) ) ;
#127804=AXIS2_PLACEMENT_3D ( 'NONE', #91517, #125581, #137162 ) ;
#127805=DIRECTION ( 'NONE',  ( 0.5735764363510444941, 0.8191520442889929088, 0.000000000000000000 ) ) ;
#127850=ORIENTED_EDGE ( 'NONE', *, *, #27688, .F. ) ;
#127874=EDGE_CURVE ( 'NONE', #141465, #126332, #39968, .T. ) ;
#127880=AXIS2_PLACEMENT_3D ( 'NONE', #8925, #141658, #53195 ) ;
#127905=CARTESIAN_POINT ( 'NONE',  ( 12.03892749862900402, 2.055000000000001048, 2.516649172247811554E-16 ) ) ;
#127933=AXIS2_PLACEMENT_3D ( 'NONE', #59257, #135380, #57819 ) ;
#127969=VECTOR ( 'NONE', #1671, 999.9999999999998863 ) ;
#127981=COLOUR_RGB ( '', 0.40784314, 0.44705882, 0.49803922) ;
#128013=VERTEX_POINT ( 'NONE', #64536 ) ;
#128045=EDGE_CURVE ( 'NONE', #105369, #106357, #46358, .T. ) ;
#128052=DIRECTION ( 'NONE',  ( 0.000000000000000000, 1.000000000000000000, 0.000000000000000000 ) ) ;
#128069=DIRECTION ( 'NONE',  ( -1.000000000000000000, -1.224606353822377258E-16, -0.000000000000000000 ) ) ;
#128090=ORIENTED_EDGE ( 'NONE', *, *, #51778, .T. ) ;
#128124=( GEOMETRIC_REPRESENTATION_CONTEXT ( 3 ) GLOBAL_UNCERTAINTY_ASSIGNED_CONTEXT ( ( #81147 ) ) GLOBAL_UNIT_ASSIGNED_CONTEXT ( ( #13492, #2627, #21000 ) ) REPRESENTATION_CONTEXT ( 'NONE', 'WORKASPACE' ) );
#128146=ORIENTED_EDGE ( 'NONE', *, *, #122066, .T. ) ;
#128207=CARTESIAN_POINT ( 'NONE',  ( 19.41972383043609440, 4.584330080086930965E-16, 0.000000000000000000 ) ) ;
#128209=AXIS2_PLACEMENT_3D ( 'NONE', #16174, #39410, #106043 ) ;
#128244=ORIENTED_EDGE ( 'NONE', *, *, #141182, .T. ) ;
#128280=ORIENTED_EDGE ( 'NONE', *, *, #94990, .T. ) ;
#128285=DIRECTION ( 'NONE',  ( -1.000000000000000000, -0.000000000000000000, -0.000000000000000000 ) ) ;
#128300=CARTESIAN_POINT ( 'NONE',  ( 4.658131166821905644, 3.821174125832445049E-16, 0.000000000000000000 ) ) ;
#128322=ORIENTED_EDGE ( 'NONE', *, *, #139614, .F. ) ;
#128329=CARTESIAN_POINT ( 'NONE',  ( 0.5685132242927012358, 4.584330080086930965E-16, 0.000000000000000000 ) ) ;
#128359=VERTEX_POINT ( 'NONE', #47654 ) ;
#128367=FACE_OUTER_BOUND ( 'NONE', #57030, .T. ) ;
#128407=CIRCLE ( 'NONE', #130803, 2.055000000000000604 ) ;
#128495=ADVANCED_FACE ( 'NONE', ( #30130 ), #125164, .T. ) ;
#128523=EDGE_CURVE ( 'NONE', #59504, #57055, #4753, .T. ) ;
#128558=DIRECTION ( 'NONE',  ( -1.000000000000000000, -1.224606353822377258E-16, -0.000000000000000000 ) ) ;
#128578=FACE_OUTER_BOUND ( 'NONE', #49676, .T. ) ;
#128587=FACE_OUTER_BOUND ( 'NONE', #95925, .T. ) ;
#128621=AXIS2_PLACEMENT_3D ( 'NONE', #34829, #23948, #68894 ) ;
#128633=DIRECTION ( 'NONE',  ( 0.000000000000000000, 0.000000000000000000, 1.000000000000000000 ) ) ;
#128790=LINE ( 'NONE', #49840, #58427 ) ;
#128850=CARTESIAN_POINT ( 'NONE',  ( -12.69999999999998153, 3.061616997868383634E-16, -2.500000000000000444 ) ) ;
#128853=EDGE_LOOP ( 'NONE', ( #17702, #117486, #105067, #128244, #38391 ) ) ;
#128867=ORIENTED_EDGE ( 'NONE', *, *, #129668, .F. ) ;
#128886=DIRECTION ( 'NONE',  ( 0.000000000000000000, -1.000000000000000000, 0.000000000000000000 ) ) ;
#128907=CARTESIAN_POINT ( 'NONE',  ( 13.92145407031093818, 2.500000000000000444, 0.000000000000000000 ) ) ;
#128980=EDGE_LOOP ( 'NONE', ( #130188, #39204, #2535, #113448, #87356 ) ) ;
#129043=AXIS2_PLACEMENT_3D ( 'NONE', #139803, #51350, #130339 ) ;
#129097=ORIENTED_EDGE ( 'NONE', *, *, #73378, .T. ) ;
#129135=DIRECTION ( 'NONE',  ( -1.000000000000000000, -0.000000000000000000, -0.000000000000000000 ) ) ;
#129187=CARTESIAN_POINT ( 'NONE',  ( -12.69999999999998153, 0.000000000000000000, 2.500000000000000444 ) ) ;
#129260=DIRECTION ( 'NONE',  ( 0.000000000000000000, -1.000000000000000000, 0.000000000000000000 ) ) ;
#129324=AXIS2_PLACEMENT_3D ( 'NONE', #19771, #86482, #74171 ) ;
#129342=LINE ( 'NONE', #74274, #39701 ) ;
#129420=ORIENTED_EDGE ( 'NONE', *, *, #4841, .T. ) ;
#129467=ORIENTED_EDGE ( 'NONE', *, *, #11999, .T. ) ;
#129510=FACE_OUTER_BOUND ( 'NONE', #3401, .T. ) ;
#129512=VERTEX_POINT ( 'NONE', #99873 ) ;
#129521=CIRCLE ( 'NONE', #104053, 2.500000000000000444 ) ;
#129525=CARTESIAN_POINT ( 'NONE',  ( 10.77958563595370833, -2.500000000000000000, 3.061616997868383634E-16 ) ) ;
#129527=EDGE_CURVE ( 'NONE', #18713, #82210, #102214, .T. ) ;
#129534=CARTESIAN_POINT ( 'NONE',  ( 9.994118527364397764, 0.000000000000000000, 2.500000000000000444 ) ) ;
#129561=FACE_OUTER_BOUND ( 'NONE', #9429, .T. ) ;
#129581=EDGE_LOOP ( 'NONE', ( #54116, #28174, #19133, #118821, #84139, #126226 ) ) ;
#129606=EDGE_CURVE ( 'NONE', #90821, #32697, #15670, .T. ) ;
#129620=CARTESIAN_POINT ( 'NONE',  ( 10.77958563595370833, 2.500000000000000444, 0.000000000000000000 ) ) ;
#129643=DIRECTION ( 'NONE',  ( -1.000000000000000000, -0.000000000000000000, -0.000000000000000000 ) ) ;
#129668=EDGE_CURVE ( 'NONE', #90821, #41872, #38904, .T. ) ;
#129693=AXIS2_PLACEMENT_3D ( 'NONE', #127442, #28141, #139048 ) ;
#129697=CARTESIAN_POINT ( 'NONE',  ( 8.897059064271770623, 4.202752102959690472E-16, 0.000000000000000000 ) ) ;
#129703=AXIS2_PLACEMENT_3D ( 'NONE', #65999, #55100, #31911 ) ;
#129718=AXIS2_PLACEMENT_3D ( 'NONE', #119633, #76176, #21056 ) ;
#129719=ORIENTED_EDGE ( 'NONE', *, *, #85898, .T. ) ;
#129729=DIRECTION ( 'NONE',  ( -1.000000000000000000, -1.224606353822377258E-16, -0.000000000000000000 ) ) ;
#129743=ORIENTED_EDGE ( 'NONE', *, *, #132226, .T. ) ;
#129798=DIRECTION ( 'NONE',  ( 0.000000000000000000, -1.000000000000000000, 0.000000000000000000 ) ) ;
#129818=EDGE_CURVE ( 'NONE', #8776, #95615, #30597, .T. ) ;
#129822=AXIS2_PLACEMENT_3D ( 'NONE', #75589, #96571, #19760 ) ;
#129866=FACE_OUTER_BOUND ( 'NONE', #34373, .T. ) ;
#129926=AXIS2_PLACEMENT_3D ( 'NONE', #28359, #95005, #137115 ) ;
#129954=EDGE_LOOP ( 'NONE', ( #125402, #129467, #36146, #2317, #93336, #65523 ) ) ;
#129985=CONICAL_SURFACE ( 'NONE', #53623, 2.055000000000000604, 0.9599310885968764806 ) ;
#130007=CARTESIAN_POINT ( 'NONE',  ( 0.5685132242927012358, 0.3999999999999995226, 2.467792535850613866 ) ) ;
#130013=DIRECTION ( 'NONE',  ( -1.000000000000000000, -0.000000000000000000, -0.000000000000000000 ) ) ;
#130028=EDGE_CURVE ( 'NONE', #38008, #36502, #130146, .T. ) ;
#130031=ORIENTED_EDGE ( 'NONE', *, *, #127289, .F. ) ;
#130032=VECTOR ( 'NONE', #17801, 999.9999999999998863 ) ;
#130111=DIRECTION ( 'NONE',  ( 1.734723475976806848E-16, -1.000000000000000000, 0.000000000000000000 ) ) ;
#130119=ORIENTED_EDGE ( 'NONE', *, *, #52347, .T. ) ;
#130146=CIRCLE ( 'NONE', #109327, 2.500000000000000444 ) ;
#130184=CIRCLE ( 'NONE', #5114, 2.500000000000000444 ) ;
#130186=CARTESIAN_POINT ( 'NONE',  ( 6.229065384000522343, 3.821174125832445049E-16, 0.000000000000000000 ) ) ;
#130188=ORIENTED_EDGE ( 'NONE', *, *, #77234, .F. ) ;
#130209=AXIS2_PLACEMENT_3D ( 'NONE', #56586, #134841, #698 ) ;
#130214=LINE ( 'NONE', #85980, #103286 ) ;
#130309=CIRCLE ( 'NONE', #67836, 2.500000000000000444 ) ;
#130328=DIRECTION ( 'NONE',  ( 0.000000000000000000, 1.000000000000000000, 0.000000000000000000 ) ) ;
#130339=DIRECTION ( 'NONE',  ( 0.000000000000000000, 0.000000000000000000, 1.000000000000000000 ) ) ;
#130350=DIRECTION ( 'NONE',  ( -0.5735764363510501562, 0.8191520442889890230, 1.003171929053521419E-16 ) ) ;
#130403=ORIENTED_EDGE ( 'NONE', *, *, #81037, .T. ) ;
#130406=AXIS2_PLACEMENT_3D ( 'NONE', #69183, #90197, #123587 ) ;
#130422=CARTESIAN_POINT ( 'NONE',  ( 9.208651418775088970, -2.500000000000000444, 3.061616997868384127E-16 ) ) ;
#130434=VERTEX_POINT ( 'NONE', #111852 ) ;
#130445=ORIENTED_EDGE ( 'NONE', *, *, #129527, .F. ) ;
#130463=ORIENTED_EDGE ( 'NONE', *, *, #8888, .F. ) ;
#130467=VERTEX_POINT ( 'NONE', #135744 ) ;
#130470=DIRECTION ( 'NONE',  ( -1.000000000000000000, -1.224606353822377258E-16, -0.000000000000000000 ) ) ;
#130482=CARTESIAN_POINT ( 'NONE',  ( 14.86920357848291196, 3.821174125832445049E-16, 0.000000000000000000 ) ) ;
#130505=ORIENTED_EDGE ( 'NONE', *, *, #118440, .T. ) ;
#130512=DIRECTION ( 'NONE',  ( -1.000000000000000000, -1.224606353822377258E-16, -0.000000000000000000 ) ) ;
#130525=DIRECTION ( 'NONE',  ( -1.000000000000000000, -1.224606353822377258E-16, -0.000000000000000000 ) ) ;
#130527=ORIENTED_EDGE ( 'NONE', *, *, #52981, .T. ) ;
#130541=DIRECTION ( 'NONE',  ( 0.000000000000000000, 0.000000000000000000, 1.000000000000000000 ) ) ;
#130585=DIRECTION ( 'NONE',  ( 0.000000000000000000, -1.000000000000000000, 0.000000000000000000 ) ) ;
#130587=CARTESIAN_POINT ( 'NONE',  ( 7.014532492589830248, 3.821174125832445049E-16, 0.000000000000000000 ) ) ;
#130588=EDGE_CURVE ( 'NONE', #131428, #134578, #72341, .T. ) ;
#130598=AXIS2_PLACEMENT_3D ( 'NONE', #122715, #135751, #103117 ) ;
#130718=LINE ( 'NONE', #64720, #76144 ) ;
#130769=CYLINDRICAL_SURFACE ( 'NONE', #31662, 2.500000000000000444 ) ;
#130789=EDGE_CURVE ( 'NONE', #115093, #104746, #88647, .T. ) ;
#130803=AXIS2_PLACEMENT_3D ( 'NONE', #96079, #94648, #51175 ) ;
#130829=DIRECTION ( 'NONE',  ( -1.000000000000000000, -0.000000000000000000, -0.000000000000000000 ) ) ;
#130830=CARTESIAN_POINT ( 'NONE',  ( 8.111591955682463606, -2.055000000000000160, 2.789133085058097101E-16 ) ) ;
#130855=DIRECTION ( 'NONE',  ( -1.000000000000000000, -1.224606353822377258E-16, -0.000000000000000000 ) ) ;
#130869=EDGE_LOOP ( 'NONE', ( #30284, #122214, #56282, #51463, #85404 ) ) ;
#130883=AXIS2_PLACEMENT_3D ( 'NONE', #109337, #112211, #143388 ) ;
#130884=VERTEX_POINT ( 'NONE', #5646 ) ;
#130990=VERTEX_POINT ( 'NONE', #64868 ) ;
#131017=DIRECTION ( 'NONE',  ( -1.000000000000000000, -1.224606353822377258E-16, -0.000000000000000000 ) ) ;
#131036=CARTESIAN_POINT ( 'NONE',  ( 6.852250093007166143, -2.500000000000000444, 3.061616997868384127E-16 ) ) ;
#131048=ORIENTED_EDGE ( 'NONE', *, *, #24289, .T. ) ;
#131056=ORIENTED_EDGE ( 'NONE', *, *, #66104, .F. ) ;
#131085=DIRECTION ( 'NONE',  ( -0.5735764363510501562, 0.8191520442889890230, 1.003171929053521419E-16 ) ) ;
#131145=CARTESIAN_POINT ( 'NONE',  ( 13.13598696172163116, 4.584330080086930965E-16, 0.000000000000000000 ) ) ;
#131200=DIRECTION ( 'NONE',  ( 0.5735764363510444941, 0.8191520442889929088, 0.000000000000000000 ) ) ;
#131201=EDGE_CURVE ( 'NONE', #101752, #41149, #14320, .T. ) ;
#131247=ORIENTED_EDGE ( 'NONE', *, *, #4013, .F. ) ;
#131248=EDGE_CURVE ( 'NONE', #57055, #136234, #67658, .T. ) ;
#131251=ORIENTED_EDGE ( 'NONE', *, *, #13851, .F. ) ;
#131254=AXIS2_PLACEMENT_3D ( 'NONE', #86505, #9611, #129260 ) ;
#131263=CARTESIAN_POINT ( 'NONE',  ( 4.658131166821905644, 3.061616997868383634E-16, -2.500000000000000444 ) ) ;
#131277=ORIENTED_EDGE ( 'NONE', *, *, #127537, .F. ) ;
#131281=DIRECTION ( 'NONE',  ( -1.000000000000000000, -1.224606353822377258E-16, -0.000000000000000000 ) ) ;
#131348=DIRECTION ( 'NONE',  ( 0.000000000000000000, -1.000000000000000000, 0.000000000000000000 ) ) ;
#131353=ORIENTED_EDGE ( 'NONE', *, *, #54129, .F. ) ;
#131366=ORIENTED_EDGE ( 'NONE', *, *, #10751, .F. ) ;
#131368=DIRECTION ( 'NONE',  ( 1.734723475976806848E-16, -1.000000000000000000, 0.000000000000000000 ) ) ;
#131390=EDGE_CURVE ( 'NONE', #42684, #10551, #113609, .T. ) ;
#131403=EDGE_LOOP ( 'NONE', ( #91878, #58431, #61618, #50721, #33766, #104842 ) ) ;
#131414=DIRECTION ( 'NONE',  ( -8.673617379884034239E-17, 1.000000000000000000, 0.000000000000000000 ) ) ;
#131428=VERTEX_POINT ( 'NONE', #57394 ) ;
#131431=ORIENTED_EDGE ( 'NONE', *, *, #17851, .T. ) ;
#131432=EDGE_CURVE ( 'NONE', #140149, #124115, #12025, .T. ) ;
#131472=ADVANCED_FACE ( 'NONE', ( #25438 ), #42079, .T. ) ;
#131513=VERTEX_POINT ( 'NONE', #40630 ) ;
#131547=CARTESIAN_POINT ( 'NONE',  ( 19.89359858452208130, 4.202752102959690472E-16, 0.000000000000000000 ) ) ;
#131623=DIRECTION ( 'NONE',  ( 0.000000000000000000, -1.000000000000000000, 0.000000000000000000 ) ) ;
#131645=CARTESIAN_POINT ( 'NONE',  ( 0.1161069444170877152, -0.3999999999999998002, -2.220360628129161906 ) ) ;
#131651=DIRECTION ( 'NONE',  ( 0.000000000000000000, -1.000000000000000000, 0.000000000000000000 ) ) ;
#131709=CONICAL_SURFACE ( 'NONE', #43428, 2.055000000000000604, 0.9599310885968764806 ) ;
#131714=CARTESIAN_POINT ( 'NONE',  ( 17.53719725875415847, 4.202752102959690472E-16, 0.000000000000000000 ) ) ;
#131728=ORIENTED_EDGE ( 'NONE', *, *, #100503, .F. ) ;
#131731=ORIENTED_EDGE ( 'NONE', *, *, #24083, .F. ) ;
#131786=CARTESIAN_POINT ( 'NONE',  ( 2.613322195557305605, 4.202752102959690472E-16, 0.000000000000000000 ) ) ;
#131789=DIRECTION ( 'NONE',  ( 0.000000000000000000, -1.000000000000000000, 0.000000000000000000 ) ) ;
#131793=CARTESIAN_POINT ( 'NONE',  ( 7.637717201596474048, 4.584330080086930965E-16, 0.000000000000000000 ) ) ;
#131800=CARTESIAN_POINT ( 'NONE',  ( 5.443598275411213550, 2.500000000000000444, 3.061616997868383634E-16 ) ) ;
#131851=AXIS2_PLACEMENT_3D ( 'NONE', #58566, #135382, #111446 ) ;
#131872=CARTESIAN_POINT ( 'NONE',  ( 18.01107201284014536, 3.821174125832445049E-16, 0.000000000000000000 ) ) ;
#131947=DIRECTION ( 'NONE',  ( -0.5735764363510501562, 0.8191520442889890230, 1.003171929053521419E-16 ) ) ;
#132010=DIRECTION ( 'NONE',  ( -1.000000000000000000, -1.224606353822377258E-16, -0.000000000000000000 ) ) ;
#132012=VECTOR ( 'NONE', #141923, 1000.000000000000000 ) ;
#132032=EDGE_CURVE ( 'NONE', #132148, #111457, #60732, .T. ) ;
#132061=EDGE_LOOP ( 'NONE', ( #106194, #88270, #58505, #67534, #121337 ) ) ;
#132071=EDGE_CURVE ( 'NONE', #47310, #52143, #100115, .T. ) ;
#132081=LINE ( 'NONE', #129187, #28519 ) ;
#132147=AXIS2_PLACEMENT_3D ( 'NONE', #105942, #139352, #115375 ) ;
#132148=VERTEX_POINT ( 'NONE', #54037 ) ;
#132194=DIRECTION ( 'NONE',  ( 0.000000000000000000, -1.000000000000000000, 0.000000000000000000 ) ) ;
#132200=EDGE_CURVE ( 'NONE', #44009, #71093, #137287, .T. ) ;
#132226=EDGE_CURVE ( 'NONE', #106919, #61275, #78982, .T. ) ;
#132264=AXIS2_PLACEMENT_3D ( 'NONE', #8905, #98818, #53174 ) ;
#132283=EDGE_CURVE ( 'NONE', #91199, #7626, #72417, .T. ) ;
#132332=EDGE_CURVE ( 'NONE', #41149, #101752, #51595, .T. ) ;
#132364=DIRECTION ( 'NONE',  ( 0.000000000000000000, -1.000000000000000000, 0.000000000000000000 ) ) ;
#132381=AXIS2_PLACEMENT_3D ( 'NONE', #24616, #81902, #25322 ) ;
#132402=PRODUCT_DEFINITION_SHAPE ( 'NONE', 'NONE',  #110370 ) ;
#132414=DIRECTION ( 'NONE',  ( -1.000000000000000000, -1.224606353822377258E-16, -0.000000000000000000 ) ) ;
#132418=CONICAL_SURFACE ( 'NONE', #79116, 2.500000000000000444, 0.9599310885968830309 ) ;
#132454=AXIS2_PLACEMENT_3D ( 'NONE', #107577, #140914, #142377 ) ;
#132478=CONICAL_SURFACE ( 'NONE', #83836, 2.500000000000000444, 0.9599310885968830309 ) ;
#132497=LINE ( 'NONE', #20099, #117784 ) ;
#132498=CARTESIAN_POINT ( 'NONE',  ( 9.370933818357753964, 3.821174125832445049E-16, 0.000000000000000000 ) ) ;
#132555=VERTEX_POINT ( 'NONE', #76308 ) ;
#132575=DIRECTION ( 'NONE',  ( 0.000000000000000000, -1.000000000000000000, 0.000000000000000000 ) ) ;
#132588=EDGE_CURVE ( 'NONE', #95615, #136985, #44695, .T. ) ;
#132627=AXIS2_PLACEMENT_3D ( 'NONE', #113236, #2312, #123453 ) ;
#132689=AXIS2_PLACEMENT_3D ( 'NONE', #35392, #1956, #15010 ) ;
#132727=CARTESIAN_POINT ( 'NONE',  ( 10.15640092694706453, 3.821174125832445049E-16, 0.000000000000000000 ) ) ;
#132735=FACE_OUTER_BOUND ( 'NONE', #71193, .T. ) ;
#132749=CARTESIAN_POINT ( 'NONE',  ( 20.67906569311139009, 4.202752102959690472E-16, 0.000000000000000000 ) ) ;
#132775=AXIS2_PLACEMENT_3D ( 'NONE', #34378, #90918, #69160 ) ;
#132798=EDGE_CURVE ( 'NONE', #5701, #93024, #114175, .T. ) ;
#132882=EDGE_CURVE ( 'NONE', #22872, #128013, #18131, .T. ) ;
#132891=ORIENTED_EDGE ( 'NONE', *, *, #123643, .T. ) ;
#132974=AXIS2_PLACEMENT_3D ( 'NONE', #57098, #101282, #110698 ) ;
#132988=LINE ( 'NONE', #110458, #28088 ) ;
#133022=CARTESIAN_POINT ( 'NONE',  ( 15.65467068707222076, 3.821174125832445049E-16, 0.000000000000000000 ) ) ;
#133032=CARTESIAN_POINT ( 'NONE',  ( 18.01107201284014536, 3.821174125832445049E-16, 0.000000000000000000 ) ) ;
#133036=ORIENTED_EDGE ( 'NONE', *, *, #27711, .T. ) ;
#133038=DIRECTION ( 'NONE',  ( -1.000000000000000000, -1.224606353822377258E-16, -0.000000000000000000 ) ) ;
#133060=ORIENTED_EDGE ( 'NONE', *, *, #39427, .F. ) ;
#133129=VERTEX_POINT ( 'NONE', #100735 ) ;
#133133=VERTEX_POINT ( 'NONE', #90583 ) ;
#133180=CARTESIAN_POINT ( 'NONE',  ( 2.613322195557305161, 2.055000000000001048, 0.000000000000000000 ) ) ;
#133199=EDGE_CURVE ( 'NONE', #103464, #16482, #47085, .T. ) ;
#133208=CARTESIAN_POINT ( 'NONE',  ( 0.000000000000000000, 0.000000000000000000, 0.000000000000000000 ) ) ;
#133210=DIRECTION ( 'NONE',  ( 0.5735764363510444941, 0.8191520442889929088, 0.000000000000000000 ) ) ;
#133225=FACE_OUTER_BOUND ( 'NONE', #44568, .T. ) ;
#133235=DIRECTION ( 'NONE',  ( -1.000000000000000000, -1.224606353822377258E-16, -0.000000000000000000 ) ) ;
#133242=DIRECTION ( 'NONE',  ( -1.000000000000000000, -1.224606353822377258E-16, -0.000000000000000000 ) ) ;
#133271=LINE ( 'NONE', #78892, #50921 ) ;
#133284=ORIENTED_EDGE ( 'NONE', *, *, #132882, .T. ) ;
#133308=CARTESIAN_POINT ( 'NONE',  ( 20.20519093902540320, 4.584330080086930965E-16, 0.000000000000000000 ) ) ;
#133355=EDGE_CURVE ( 'NONE', #13056, #12477, #97699, .T. ) ;
#133357=VECTOR ( 'NONE', #126823, 999.9999999999998863 ) ;
#133425=DIRECTION ( 'NONE',  ( -1.000000000000000000, -0.000000000000000000, -0.000000000000000000 ) ) ;
#133428=DIRECTION ( 'NONE',  ( 1.000000000000000000, 0.000000000000000000, 0.000000000000000000 ) ) ;
#133430=EDGE_LOOP ( 'NONE', ( #60186, #1959, #13931, #81043, #54123 ) ) ;
#133452=DIRECTION ( 'NONE',  ( -0.7071067811865477948, 0.000000000000000000, 0.7071067811865473507 ) ) ;
#133462=CARTESIAN_POINT ( 'NONE',  ( 0.2100385299584282828, 0.4000000000000001332, -2.083955186700111817 ) ) ;
#133545=DIRECTION ( 'NONE',  ( 1.000000000000000000, 1.224606353822377258E-16, 0.000000000000000000 ) ) ;
#133556=DIRECTION ( 'NONE',  ( 0.000000000000000000, -1.000000000000000000, 0.000000000000000000 ) ) ;
#133566=DIRECTION ( 'NONE',  ( 0.000000000000000000, -1.000000000000000000, 0.000000000000000000 ) ) ;
#133592=DIRECTION ( 'NONE',  ( -1.000000000000000000, -1.224606353822377258E-16, -0.000000000000000000 ) ) ;
#133623=CARTESIAN_POINT ( 'NONE',  ( 1.629999999999999893, 0.4000000000000001887, -2.303088455023527104 ) ) ;
#133666=CYLINDRICAL_SURFACE ( 'NONE', #80796, 2.500000000000000444 ) ;
#133668=CARTESIAN_POINT ( 'NONE',  ( 1.516262732464673579, 0.3999999999999995226, 2.467792535850613866 ) ) ;
#133684=CIRCLE ( 'NONE', #103531, 2.055000000000000160 ) ;
#133713=DIRECTION ( 'NONE',  ( 1.734723475976806848E-16, -1.000000000000000000, 0.000000000000000000 ) ) ;
#133774=DIRECTION ( 'NONE',  ( 0.000000000000000000, -1.000000000000000000, 0.000000000000000000 ) ) ;
#133784=DIRECTION ( 'NONE',  ( 0.000000000000000000, -1.000000000000000000, 0.000000000000000000 ) ) ;
#133859=EDGE_LOOP ( 'NONE', ( #104846, #44259, #114390, #38801, #99779, #99014, #32818, #62570 ) ) ;
#133869=ORIENTED_EDGE ( 'NONE', *, *, #126081, .F. ) ;
#133874=DIRECTION ( 'NONE',  ( 0.000000000000000000, -1.000000000000000000, 0.000000000000000000 ) ) ;
#133881=SURFACE_STYLE_FILL_AREA ( #112829 ) ;
#133931=CARTESIAN_POINT ( 'NONE',  ( 1.827855086967997700, 4.202752102959690472E-16, 0.000000000000000000 ) ) ;
#133977=ORIENTED_EDGE ( 'NONE', *, *, #127014, .T. ) ;
#134126=VECTOR ( 'NONE', #36593, 999.9999999999998863 ) ;
#134182=AXIS2_PLACEMENT_3D ( 'NONE', #59904, #94638, #26549 ) ;
#134208=AXIS2_PLACEMENT_3D ( 'NONE', #96246, #117992, #140488 ) ;
#134214=DIRECTION ( 'NONE',  ( -1.000000000000000000, -1.224606353822377258E-16, -0.000000000000000000 ) ) ;
#134216=ADVANCED_FACE ( 'NONE', ( #16579 ), #107164, .T. ) ;
#134225=CIRCLE ( 'NONE', #81045, 2.055000000000000604 ) ;
#134248=FACE_OUTER_BOUND ( 'NONE', #129954, .T. ) ;
#134322=CIRCLE ( 'NONE', #136666, 2.055000000000000604 ) ;
#134342=CARTESIAN_POINT ( 'NONE',  ( 12.51280225271498736, 2.500000000000000444, 3.061616997868383634E-16 ) ) ;
#134360=EDGE_LOOP ( 'NONE', ( #14100, #87438, #31973, #40935, #110892, #121377 ) ) ;
#134364=CARTESIAN_POINT ( 'NONE',  ( 0.8348608954644654023, 0.3999999999999995226, 2.317232259782045833 ) ) ;
#134367=ADVANCED_FACE ( 'NONE', ( #31765 ), #15374, .T. ) ;
#134397=ORIENTED_EDGE ( 'NONE', *, *, #127373, .F. ) ;
#134400=ORIENTED_EDGE ( 'NONE', *, *, #76954, .T. ) ;
#134406=AXIS2_PLACEMENT_3D ( 'NONE', #83311, #94864, #37680 ) ;
#134427=EDGE_CURVE ( 'NONE', #109534, #66627, #98700, .T. ) ;
#134431=CYLINDRICAL_SURFACE ( 'NONE', #94834, 1.749999999999999778 ) ;
#134487=DIRECTION ( 'NONE',  ( 0.000000000000000000, 0.000000000000000000, 1.000000000000000000 ) ) ;
#134491=CARTESIAN_POINT ( 'NONE',  ( 7.014532492589830248, 3.821174125832445049E-16, 0.000000000000000000 ) ) ;
#134494=DIRECTION ( 'NONE',  ( 1.000000000000000000, 1.224606353822377258E-16, 0.000000000000000000 ) ) ;
#134502=DIRECTION ( 'NONE',  ( 0.000000000000000000, -1.000000000000000000, 0.000000000000000000 ) ) ;
#134531=ADVANCED_FACE ( 'NONE', ( #102015 ), #121866, .T. ) ;
#134562=DIRECTION ( 'NONE',  ( -1.000000000000000000, -1.224606353822377258E-16, -0.000000000000000000 ) ) ;
#134567=DIRECTION ( 'NONE',  ( 0.000000000000000000, 1.000000000000000000, 0.000000000000000000 ) ) ;
#134571=ADVANCED_FACE ( 'NONE', ( #3386 ), #47845, .T. ) ;
#134578=VERTEX_POINT ( 'NONE', #23741 ) ;
#134642=FACE_OUTER_BOUND ( 'NONE', #59156, .T. ) ;
#134649=ADVANCED_FACE ( 'NONE', ( #95959 ), #130769, .T. ) ;
#134668=VECTOR ( 'NONE', #52932, 1000.000000000000000 ) ;
#134671=EDGE_CURVE ( 'NONE', #114653, #122222, #96501, .T. ) ;
#134678=CARTESIAN_POINT ( 'NONE',  ( 1.629999999999999893, -0.4000000000000004108, 2.303088455023526215 ) ) ;
#134686=ORIENTED_EDGE ( 'NONE', *, *, #69438, .T. ) ;
#134708=CIRCLE ( 'NONE', #72216, 2.500000000000000444 ) ;
#134715=CARTESIAN_POINT ( 'NONE',  ( -12.69999999999998153, 0.000000000000000000, 0.000000000000000000 ) ) ;
#134722=CARTESIAN_POINT ( 'NONE',  ( -12.69999999999998153, 0.000000000000000000, 0.000000000000000000 ) ) ;
#134737=EDGE_LOOP ( 'NONE', ( #71904, #82131, #104178, #65283 ) ) ;
#134743=AXIS2_PLACEMENT_3D ( 'NONE', #48249, #59171, #122221 ) ;
#134775=DIRECTION ( 'NONE',  ( -1.000000000000000000, -1.224606353822377258E-16, -0.000000000000000000 ) ) ;
#134788=CARTESIAN_POINT ( 'NONE',  ( -12.69999999999998153, 0.000000000000000000, 0.000000000000000000 ) ) ;
#134833=EDGE_CURVE ( 'NONE', #17542, #74043, #23392, .T. ) ;
#134841=DIRECTION ( 'NONE',  ( 1.000000000000000000, 1.224606353822377258E-16, 0.000000000000000000 ) ) ;
#134856=CIRCLE ( 'NONE', #95476, 2.500000000000000444 ) ;
#134878=ORIENTED_EDGE ( 'NONE', *, *, #5281, .F. ) ;
#134887=DIRECTION ( 'NONE',  ( 8.673617379884034239E-17, -1.000000000000000000, 0.000000000000000000 ) ) ;
#134892=ORIENTED_EDGE ( 'NONE', *, *, #863, .T. ) ;
#134919=EDGE_CURVE ( 'NONE', #97217, #104460, #15953, .T. ) ;
#134923=CONICAL_SURFACE ( 'NONE', #107139, 2.055000000000000604, 0.9599310885968764806 ) ;
#134934=ORIENTED_EDGE ( 'NONE', *, *, #40098, .F. ) ;
#134957=CARTESIAN_POINT ( 'NONE',  ( 8.111591955682463606, -2.055000000000000160, 0.000000000000000000 ) ) ;
#134959=ORIENTED_EDGE ( 'NONE', *, *, #67462, .F. ) ;
#134963=ORIENTED_EDGE ( 'NONE', *, *, #132200, .T. ) ;
#134965=DIRECTION ( 'NONE',  ( 0.000000000000000000, -1.000000000000000000, 0.000000000000000000 ) ) ;
#134984=CYLINDRICAL_SURFACE ( 'NONE', #135158, 2.500000000000000444 ) ;
#135016=VECTOR ( 'NONE', #19046, 1000.000000000000000 ) ;
#135057=ORIENTED_EDGE ( 'NONE', *, *, #117257, .T. ) ;
#135095=CARTESIAN_POINT ( 'NONE',  ( 0.2569208697893813897, 0.3999999999999995781, 2.015694669338588429 ) ) ;
#135096=ORIENTED_EDGE ( 'NONE', *, *, #77304, .T. ) ;
#135105=DIRECTION ( 'NONE',  ( -1.000000000000000000, -1.224606353822377258E-16, -0.000000000000000000 ) ) ;
#135131=CARTESIAN_POINT ( 'NONE',  ( 19.41972383043609440, 2.500000000000000888, 0.000000000000000000 ) ) ;
#135144=ORIENTED_EDGE ( 'NONE', *, *, #129818, .T. ) ;
#135158=AXIS2_PLACEMENT_3D ( 'NONE', #24756, #113177, #13853 ) ;
#135177=DIRECTION ( 'NONE',  ( -1.000000000000000000, -0.000000000000000000, -0.000000000000000000 ) ) ;
#135184=DIRECTION ( 'NONE',  ( 0.000000000000000000, -1.000000000000000000, 0.000000000000000000 ) ) ;
#135225=EDGE_CURVE ( 'NONE', #25103, #1859, #112882, .T. ) ;
#135288=CARTESIAN_POINT ( 'NONE',  ( 21.77612515620402078, 4.584330080086930965E-16, 0.000000000000000000 ) ) ;
#135292=CARTESIAN_POINT ( 'NONE',  ( -12.69999999999998153, 3.061616997868383634E-16, -2.500000000000000444 ) ) ;
#135294=CARTESIAN_POINT ( 'NONE',  ( 17.06332250466817158, 4.584330080086930965E-16, 0.000000000000000000 ) ) ;
#135298=ORIENTED_EDGE ( 'NONE', *, *, #110101, .T. ) ;
#135299=EDGE_CURVE ( 'NONE', #137211, #78146, #31860, .T. ) ;
#135333=DIRECTION ( 'NONE',  ( 0.000000000000000000, -1.000000000000000000, 0.000000000000000000 ) ) ;
#135380=DIRECTION ( 'NONE',  ( -1.000000000000000000, -1.224606353822377258E-16, -0.000000000000000000 ) ) ;
#135382=DIRECTION ( 'NONE',  ( -1.000000000000000000, -1.224606353822377258E-16, -0.000000000000000000 ) ) ;
#135425=FACE_OUTER_BOUND ( 'NONE', #11049, .T. ) ;
#135429=DIRECTION ( 'NONE',  ( 0.000000000000000000, 0.000000000000000000, 1.000000000000000000 ) ) ;
#135441=EDGE_LOOP ( 'NONE', ( #75559, #122362, #54726, #57912, #40620 ) ) ;
#135447=ORIENTED_EDGE ( 'NONE', *, *, #77954, .F. ) ;
#135521=ADVANCED_FACE ( 'NONE', ( #75855 ), #141832, .T. ) ;
#135554=DIRECTION ( 'NONE',  ( 0.000000000000000000, -1.000000000000000000, 0.000000000000000000 ) ) ;
#135562=LINE ( 'NONE', #100777, #74299 ) ;
#135570=CIRCLE ( 'NONE', #110068, 1.749999999999999778 ) ;
#135579=CIRCLE ( 'NONE', #8229, 2.500000000000000444 ) ;
#135597=ORIENTED_EDGE ( 'NONE', *, *, #22242, .F. ) ;
#135628=AXIS2_PLACEMENT_3D ( 'NONE', #9678, #140219, #86560 ) ;
#135669=DIRECTION ( 'NONE',  ( -1.000000000000000000, -1.224606353822377258E-16, -0.000000000000000000 ) ) ;
#135728=LINE ( 'NONE', #14657, #82861 ) ;
#135739=ORIENTED_EDGE ( 'NONE', *, *, #26944, .T. ) ;
#135742=VERTEX_POINT ( 'NONE', #65730 ) ;
#135744=CARTESIAN_POINT ( 'NONE',  ( 1.042387978378689350, 0.4000000000000001332, -2.015694669338588429 ) ) ;
#135751=DIRECTION ( 'NONE',  ( -1.000000000000000000, -1.224606353822377258E-16, -0.000000000000000000 ) ) ;
#135791=ADVANCED_FACE ( 'NONE', ( #48939 ), #138805, .T. ) ;
#135795=EDGE_CURVE ( 'NONE', #59855, #19525, #70006, .T. ) ;
#135907=CONICAL_SURFACE ( 'NONE', #103386, 2.055000000000000604, 0.9599310885968764806 ) ;
#135914=DIRECTION ( 'NONE',  ( -1.000000000000000000, -1.224606353822377258E-16, -0.000000000000000000 ) ) ;
#135963=DIRECTION ( 'NONE',  ( 0.000000000000000000, -1.000000000000000000, 0.000000000000000000 ) ) ;
#135974=DIRECTION ( 'NONE',  ( -1.000000000000000000, -1.224606353822377258E-16, -0.000000000000000000 ) ) ;
#135989=DIRECTION ( 'NONE',  ( 0.000000000000000000, -1.000000000000000000, 0.000000000000000000 ) ) ;
#136043=EDGE_CURVE ( 'NONE', #59073, #112772, #43064, .T. ) ;
#136128=AXIS2_PLACEMENT_3D ( 'NONE', #45183, #133592, #32123 ) ;
#136150=CARTESIAN_POINT ( 'NONE',  ( 15.49238828748955576, -2.500000000000000444, 3.061616997868384127E-16 ) ) ;
#136165=CYLINDRICAL_SURFACE ( 'NONE', #10417, 2.500000000000000444 ) ;
#136174=AXIS2_PLACEMENT_3D ( 'NONE', #77050, #43679, #110332 ) ;
#136187=CARTESIAN_POINT ( 'NONE',  ( 8.897059064271770623, 4.202752102959690472E-16, 0.000000000000000000 ) ) ;
#136234=VERTEX_POINT ( 'NONE', #124884 ) ;
#136242=CIRCLE ( 'NONE', #62275, 2.500000000000000444 ) ;
#136273=ORIENTED_EDGE ( 'NONE', *, *, #116300, .T. ) ;
#136280=ORIENTED_EDGE ( 'NONE', *, *, #74455, .F. ) ;
#136283=CONICAL_SURFACE ( 'NONE', #73787, 2.055000000000000604, 0.9599310885968764806 ) ;
#136310=CARTESIAN_POINT ( 'NONE',  ( 21.66240673564756491, 0.000000000000000000, 0.000000000000000000 ) ) ;
#136313=ORIENTED_EDGE ( 'NONE', *, *, #94026, .T. ) ;
#136322=FACE_OUTER_BOUND ( 'NONE', #26651, .T. ) ;
#136345=CARTESIAN_POINT ( 'NONE',  ( 9.208651418775088970, 4.584330080086930965E-16, 0.000000000000000000 ) ) ;
#136351=CARTESIAN_POINT ( 'NONE',  ( 0.4644479527036028399, 0.4000000000000001887, -2.317232259782045833 ) ) ;
#136443=AXIS2_PLACEMENT_3D ( 'NONE', #128329, #139213, #117403 ) ;
#136482=DIRECTION ( 'NONE',  ( 1.318980745116185161E-16, -1.000000000000000000, 0.000000000000000000 ) ) ;
#136501=CARTESIAN_POINT ( 'NONE',  ( -12.69999999999998153, 2.143131898507868051E-16, -1.749999999999999778 ) ) ;
#136504=ORIENTED_EDGE ( 'NONE', *, *, #97915, .F. ) ;
#136505=ORIENTED_EDGE ( 'NONE', *, *, #50286, .F. ) ;
#136529=ORIENTED_EDGE ( 'NONE', *, *, #82115, .T. ) ;
#136584=DIRECTION ( 'NONE',  ( -1.000000000000000000, -1.224606353822377258E-16, -0.000000000000000000 ) ) ;
#136594=ORIENTED_EDGE ( 'NONE', *, *, #20794, .F. ) ;
#136599=DIRECTION ( 'NONE',  ( 0.000000000000000000, 0.000000000000000000, 1.000000000000000000 ) ) ;
#136608=ORIENTED_EDGE ( 'NONE', *, *, #53589, .F. ) ;
#136638=ORIENTED_EDGE ( 'NONE', *, *, #140873, .T. ) ;
#136642=DIRECTION ( 'NONE',  ( 1.000000000000000000, 1.224606353822377258E-16, 0.000000000000000000 ) ) ;
#136666=AXIS2_PLACEMENT_3D ( 'NONE', #60529, #62648, #51056 ) ;
#136698=VERTEX_POINT ( 'NONE', #101518 ) ;
#136708=EDGE_LOOP ( 'NONE', ( #90491, #93989, #4196, #99776, #22652, #104803 ) ) ;
#136722=DIRECTION ( 'NONE',  ( -1.000000000000000000, -1.224606353822377258E-16, -0.000000000000000000 ) ) ;
#136774=AXIS2_PLACEMENT_3D ( 'NONE', #80100, #46034, #123604 ) ;
#136790=AXIS2_PLACEMENT_3D ( 'NONE', #139294, #19619, #84881 ) ;
#136791=CARTESIAN_POINT ( 'NONE',  ( 0.4644479527036028954, -0.4000000000000004108, 2.317232259782045389 ) ) ;
#136804=ORIENTED_EDGE ( 'NONE', *, *, #51537, .F. ) ;
#136896=FACE_OUTER_BOUND ( 'NONE', #82243, .T. ) ;
#136911=DIRECTION ( 'NONE',  ( 0.000000000000000000, -1.000000000000000000, 0.000000000000000000 ) ) ;
#136934=AXIS2_PLACEMENT_3D ( 'NONE', #115317, #16013, #104477 ) ;
#136951=VECTOR ( 'NONE', #3342, 1000.000000000000000 ) ;
#136985=VERTEX_POINT ( 'NONE', #23052 ) ;
#136995=AXIS2_PLACEMENT_3D ( 'NONE', #111530, #76802, #11472 ) ;
#137061=ORIENTED_EDGE ( 'NONE', *, *, #132200, .F. ) ;
#137072=LINE ( 'NONE', #18838, #31784 ) ;
#137077=FACE_OUTER_BOUND ( 'NONE', #38230, .T. ) ;
#137115=DIRECTION ( 'NONE',  ( 0.000000000000000000, -1.000000000000000000, 0.000000000000000000 ) ) ;
#137121=EDGE_CURVE ( 'NONE', #102047, #118149, #61983, .T. ) ;
#137155=AXIS2_PLACEMENT_3D ( 'NONE', #42854, #34113, #23187 ) ;
#137162=DIRECTION ( 'NONE',  ( 0.000000000000000000, -1.000000000000000000, 0.000000000000000000 ) ) ;
#137192=CARTESIAN_POINT ( 'NONE',  ( 6.066782984417857350, -2.500000000000000444, 3.061616997868384127E-16 ) ) ;
#137211=VERTEX_POINT ( 'NONE', #20575 ) ;
#137219=DIRECTION ( 'NONE',  ( -1.000000000000000000, -1.224606353822377258E-16, -0.000000000000000000 ) ) ;
#137228=VERTEX_POINT ( 'NONE', #53208 ) ;
#137232=ORIENTED_EDGE ( 'NONE', *, *, #122504, .F. ) ;
#137242=CONICAL_SURFACE ( 'NONE', #141918, 2.055000000000000604, 0.9599310885968764806 ) ;
#137252=EDGE_CURVE ( 'NONE', #132148, #115093, #64103, .T. ) ;
#137282=VERTEX_POINT ( 'NONE', #74276 ) ;
#137287=LINE ( 'NONE', #71317, #74672 ) ;
#137307=VECTOR ( 'NONE', #115797, 1000.000000000000000 ) ;
#137327=CARTESIAN_POINT ( 'NONE',  ( 16.44013779566152778, 3.821174125832445049E-16, 0.000000000000000000 ) ) ;
#137347=CARTESIAN_POINT ( 'NONE',  ( 16.27785539607886633, 2.500000000000000888, 0.000000000000000000 ) ) ;
#137349=CARTESIAN_POINT ( 'NONE',  ( 20.67906569311139009, -2.055000000000000160, 2.789133085058097101E-16 ) ) ;
#137351=ORIENTED_EDGE ( 'NONE', *, *, #90688, .T. ) ;
#137361=CARTESIAN_POINT ( 'NONE',  ( 18.79653912142945060, 3.821174125832445049E-16, 0.000000000000000000 ) ) ;
#137372=CARTESIAN_POINT ( 'NONE',  ( -12.69999999999998153, 0.000000000000000000, 0.000000000000000000 ) ) ;
#137391=CARTESIAN_POINT ( 'NONE',  ( 5.443598275411213550, -2.499999999999999112, 0.000000000000000000 ) ) ;
#137399=ORIENTED_EDGE ( 'NONE', *, *, #118440, .F. ) ;
#137410=DIRECTION ( 'NONE',  ( -1.000000000000000000, -1.224606353822377258E-16, -0.000000000000000000 ) ) ;
#137426=CONICAL_SURFACE ( 'NONE', #49504, 2.500000000000000444, 0.9599310885968830309 ) ;
#137456=ORIENTED_EDGE ( 'NONE', *, *, #80975, .T. ) ;
#137486=EDGE_CURVE ( 'NONE', #99466, #138500, #13400, .T. ) ;
#137497=AXIS2_PLACEMENT_3D ( 'NONE', #126510, #135974, #71445 ) ;
#137523=ADVANCED_FACE ( 'NONE', ( #80708 ), #66631, .T. ) ;
#137576=CARTESIAN_POINT ( 'NONE',  ( 4.495848767239241539, 3.061616997868383634E-16, -2.500000000000000444 ) ) ;
#137578=CARTESIAN_POINT ( 'NONE',  ( 21.15294044719737698, 3.821174125832445049E-16, 0.000000000000000000 ) ) ;
#137601=EDGE_CURVE ( 'NONE', #29556, #68546, #40764, .T. ) ;
#137627=AXIS2_PLACEMENT_3D ( 'NONE', #91113, #103361, #92492 ) ;
#137645=DIRECTION ( 'NONE',  ( -1.000000000000000000, -1.224606353822377258E-16, -0.000000000000000000 ) ) ;
#137665=ORIENTED_EDGE ( 'NONE', *, *, #83477, .T. ) ;
#137675=CARTESIAN_POINT ( 'NONE',  ( 0.3605399447480615582, 0.3999999999999995781, 2.166563668000046405 ) ) ;
#137677=CARTESIAN_POINT ( 'NONE',  ( 25.00000000000000000, 0.000000000000000000, 1.749999999999999778 ) ) ;
#137781=DIRECTION ( 'NONE',  ( -1.000000000000000000, -1.224606353822377258E-16, -0.000000000000000000 ) ) ;
#137807=LINE ( 'NONE', #28328, #91287 ) ;
#137823=ORIENTED_EDGE ( 'NONE', *, *, #94990, .F. ) ;
#137839=CARTESIAN_POINT ( 'NONE',  ( 11.56505274454301357, 3.061616997868383634E-16, -2.500000000000000444 ) ) ;
#137851=FACE_OUTER_BOUND ( 'NONE', #33434, .T. ) ;
#137858=ORIENTED_EDGE ( 'NONE', *, *, #15934, .F. ) ;
#137871=DIRECTION ( 'NONE',  ( 0.000000000000000000, -1.000000000000000000, 0.000000000000000000 ) ) ;
#137949=EDGE_CURVE ( 'NONE', #79680, #136698, #98082, .T. ) ;
#137961=LINE ( 'NONE', #135131, #37407 ) ;
#137995=CARTESIAN_POINT ( 'NONE',  ( 11.56505274454301357, 4.584330080086930965E-16, 0.000000000000000000 ) ) ;
#138173=DIRECTION ( 'NONE',  ( -1.000000000000000000, -1.224606353822377258E-16, -0.000000000000000000 ) ) ;
#138294=CARTESIAN_POINT ( 'NONE',  ( 13.13598696172163116, 3.061616997868383634E-16, -2.500000000000000444 ) ) ;
#138316=DIRECTION ( 'NONE',  ( 0.000000000000000000, 0.000000000000000000, 1.000000000000000000 ) ) ;
#138400=ADVANCED_FACE ( 'NONE', ( #139017 ), #83073, .T. ) ;
#138406=DIRECTION ( 'NONE',  ( 0.000000000000000000, -1.000000000000000000, 0.000000000000000000 ) ) ;
#138416=ORIENTED_EDGE ( 'NONE', *, *, #9105, .T. ) ;
#138423=CYLINDRICAL_SURFACE ( 'NONE', #90621, 2.500000000000000444 ) ;
#138473=CARTESIAN_POINT ( 'NONE',  ( 1.592112669765240796, 0.4000000000000001887, -2.358007193124714629 ) ) ;
#138486=DIRECTION ( 'NONE',  ( 1.301042606982605074E-16, -1.000000000000000000, 0.000000000000000000 ) ) ;
#138487=AXIS2_PLACEMENT_3D ( 'NONE', #60050, #26689, #2783 ) ;
#138500=VERTEX_POINT ( 'NONE', #137349 ) ;
#138553=DIRECTION ( 'NONE',  ( 8.673617379884034239E-17, -1.000000000000000000, 0.000000000000000000 ) ) ;
#138580=CARTESIAN_POINT ( 'NONE',  ( 6.852250093007166143, 4.584330080086930965E-16, 0.000000000000000000 ) ) ;
#138581=LINE ( 'NONE', #102748, #102522 ) ;
#138583=CARTESIAN_POINT ( 'NONE',  ( 17.22560490425083657, 3.061616997868387579E-16, -2.500000000000000444 ) ) ;
#138587=DIRECTION ( 'NONE',  ( 0.000000000000000000, -1.000000000000000000, 0.000000000000000000 ) ) ;
#138614=CARTESIAN_POINT ( 'NONE',  ( 7.799999601179139042, 0.000000000000000000, 2.500000000000000444 ) ) ;
#138646=DIRECTION ( 'NONE',  ( -1.000000000000000000, -0.000000000000000000, -0.000000000000000000 ) ) ;
#138683=ORIENTED_EDGE ( 'NONE', *, *, #48536, .F. ) ;
#138699=CYLINDRICAL_SURFACE ( 'NONE', #51194, 2.500000000000000444 ) ;
#138731=DIRECTION ( 'NONE',  ( -1.000000000000000000, -1.224606353822377258E-16, -0.000000000000000000 ) ) ;
#138749=CARTESIAN_POINT ( 'NONE',  ( 22.25000000000000000, 0.000000000000000000, 0.000000000000000000 ) ) ;
#138763=ORIENTED_EDGE ( 'NONE', *, *, #86269, .T. ) ;
#138796=CIRCLE ( 'NONE', #131851, 2.500000000000000444 ) ;
#138805=CYLINDRICAL_SURFACE ( 'NONE', #57146, 2.500000000000000444 ) ;
#138866=CONICAL_SURFACE ( 'NONE', #83288, 2.500000000000000444, 0.9599310885968830309 ) ;
#138872=CARTESIAN_POINT ( 'NONE',  ( 1.827855086967997700, 4.202752102959690472E-16, 0.000000000000000000 ) ) ;
#138879=ORIENTED_EDGE ( 'NONE', *, *, #99089, .F. ) ;
#138890=VECTOR ( 'NONE', #47940, 999.9999999999998863 ) ;
#138891=EDGE_CURVE ( 'NONE', #38043, #124291, #130718, .T. ) ;
#138967=EDGE_LOOP ( 'NONE', ( #3486, #7343, #94101, #103783, #107429 ) ) ;
#139005=CARTESIAN_POINT ( 'NONE',  ( 6.229065384000522343, 0.000000000000000000, 2.500000000000000444 ) ) ;
#139017=FACE_OUTER_BOUND ( 'NONE', #30263, .T. ) ;
#139038=EDGE_LOOP ( 'NONE', ( #79228, #133977, #30085, #63113, #75772 ) ) ;
#139048=DIRECTION ( 'NONE',  ( -0.000000000000000000, 0.000000000000000000, 1.000000000000000000 ) ) ;
#139071=VECTOR ( 'NONE', #141461, 1000.000000000000000 ) ;
#139082=VERTEX_POINT ( 'NONE', #69751 ) ;
#139094=ORIENTED_EDGE ( 'NONE', *, *, #132283, .T. ) ;
#139109=DIRECTION ( 'NONE',  ( 0.000000000000000000, 0.000000000000000000, 1.000000000000000000 ) ) ;
#139151=CIRCLE ( 'NONE', #99793, 2.337566348077130929 ) ;
#139213=DIRECTION ( 'NONE',  ( 1.000000000000000000, 1.224606353822377258E-16, 0.000000000000000000 ) ) ;
#139252=ORIENTED_EDGE ( 'NONE', *, *, #113792, .F. ) ;
#139262=ADVANCED_FACE ( 'NONE', ( #109480 ), #43509, .T. ) ;
#139289=CARTESIAN_POINT ( 'NONE',  ( 1.516262732464673579, 3.821174125832445049E-16, 0.000000000000000000 ) ) ;
#139294=CARTESIAN_POINT ( 'NONE',  ( 0.5685132242927012358, 4.584330080086930965E-16, 0.000000000000000000 ) ) ;
#139297=AXIS2_PLACEMENT_3D ( 'NONE', #73912, #6454, #115962 ) ;
#139352=DIRECTION ( 'NONE',  ( -1.000000000000000000, -0.000000000000000000, -0.000000000000000000 ) ) ;
#139358=DIRECTION ( 'NONE',  ( 0.000000000000000000, -1.000000000000000000, 0.000000000000000000 ) ) ;
#139411=AXIS2_PLACEMENT_3D ( 'NONE', #90420, #3385, #125921 ) ;
#139436=VERTEX_POINT ( 'NONE', #90595 ) ;
#139495=CARTESIAN_POINT ( 'NONE',  ( 1.629999999999999893, -0.3999999999999997446, -2.500000000000000000 ) ) ;
#139503=VERTEX_POINT ( 'NONE', #137677 ) ;
#139519=DIRECTION ( 'NONE',  ( -0.5735764363510501562, 0.8191520442889890230, 1.003171929053521419E-16 ) ) ;
#139604=ORIENTED_EDGE ( 'NONE', *, *, #27374, .F. ) ;
#139614=EDGE_CURVE ( 'NONE', #93248, #87033, #80905, .T. ) ;
#139622=EDGE_CURVE ( 'NONE', #17540, #20222, #9120, .T. ) ;
#139632=CARTESIAN_POINT ( 'NONE',  ( 4.658131166821905644, 0.000000000000000000, 2.500000000000000444 ) ) ;
#139689=AXIS2_PLACEMENT_3D ( 'NONE', #27750, #60419, #36495 ) ;
#139715=CARTESIAN_POINT ( 'NONE',  ( -12.69999999999998153, 0.000000000000000000, 2.500000000000000444 ) ) ;
#139717=CIRCLE ( 'NONE', #114221, 2.500000000000000444 ) ;
#139729=EDGE_LOOP ( 'NONE', ( #107103, #126682, #114967, #21468, #118052, #109546 ) ) ;
#139737=ADVANCED_FACE ( 'NONE', ( #33907 ), #69393, .T. ) ;
#139759=CARTESIAN_POINT ( 'NONE',  ( -12.69999999999998153, 3.061616997868383634E-16, -2.500000000000000444 ) ) ;
#139769=CARTESIAN_POINT ( 'NONE',  ( 14.70692117890024697, 2.500000000000000444, 0.000000000000000000 ) ) ;
#139788=ADVANCED_FACE ( 'NONE', ( #1923 ), #46229, .T. ) ;
#139803=CARTESIAN_POINT ( 'NONE',  ( -12.69999999999998153, 0.000000000000000000, 0.000000000000000000 ) ) ;
#139849=VECTOR ( 'NONE', #102519, 1000.000000000000000 ) ;
#139868=CARTESIAN_POINT ( 'NONE',  ( 21.77612515620402078, 2.500000000000000888, 0.000000000000000000 ) ) ;
#139913=CARTESIAN_POINT ( 'NONE',  ( 2.613322195557306049, -2.055000000000000160, 0.000000000000000000 ) ) ;
#139928=DIRECTION ( 'NONE',  ( -1.734723475976806848E-16, 1.000000000000000000, 0.000000000000000000 ) ) ;
#139951=ORIENTED_EDGE ( 'NONE', *, *, #2977, .F. ) ;
#139961=DIRECTION ( 'NONE',  ( 0.5735764363510448272, -0.8191520442889927978, 1.003171929053526103E-16 ) ) ;
#139969=EDGE_CURVE ( 'NONE', #140092, #128013, #120377, .T. ) ;
#139974=CARTESIAN_POINT ( 'NONE',  ( 18.63425672184678916, 2.500000000000000444, 0.000000000000000000 ) ) ;
#139978=CARTESIAN_POINT ( 'NONE',  ( -12.69999999999998153, 0.000000000000000000, 2.500000000000000444 ) ) ;
#139991=CARTESIAN_POINT ( 'NONE',  ( 5.281315875828549444, -9.629649721936179265E-32, 2.500000000000000444 ) ) ;
#140026=DIRECTION ( 'NONE',  ( -1.000000000000000000, -1.224606353822377258E-16, -0.000000000000000000 ) ) ;
#140035=AXIS2_PLACEMENT_3D ( 'NONE', #54904, #110654, #99814 ) ;
#140048=CARTESIAN_POINT ( 'NONE',  ( 17.53719725875415847, 4.202752102959690472E-16, 0.000000000000000000 ) ) ;
#140066=ORIENTED_EDGE ( 'NONE', *, *, #133199, .T. ) ;
#140092=VERTEX_POINT ( 'NONE', #110541 ) ;
#140094=AXIS2_PLACEMENT_3D ( 'NONE', #64398, #116094, #61751 ) ;
#140097=ORIENTED_EDGE ( 'NONE', *, *, #79583, .T. ) ;
#140143=DIRECTION ( 'NONE',  ( 0.000000000000000000, -1.000000000000000000, 0.000000000000000000 ) ) ;
#140149=VERTEX_POINT ( 'NONE', #79426 ) ;
#140176=CARTESIAN_POINT ( 'NONE',  ( 21.15294044719737698, 3.821174125832445049E-16, 0.000000000000000000 ) ) ;
#140197=DIRECTION ( 'NONE',  ( -1.000000000000000000, -1.224606353822377258E-16, -0.000000000000000000 ) ) ;
#140219=DIRECTION ( 'NONE',  ( -1.000000000000000000, -1.224606353822377258E-16, -0.000000000000000000 ) ) ;
#140222=EDGE_CURVE ( 'NONE', #82210, #43404, #108798, .T. ) ;
#140226=VERTEX_POINT ( 'NONE', #95768 ) ;
#140264=ORIENTED_EDGE ( 'NONE', *, *, #130789, .T. ) ;
#140335=EDGE_CURVE ( 'NONE', #11920, #22872, #81224, .T. ) ;
#140377=CARTESIAN_POINT ( 'NONE',  ( -12.69999999999998153, 0.000000000000000000, 2.500000000000000444 ) ) ;
#140402=ADVANCED_FACE ( 'NONE', ( #52961 ), #120476, .T. ) ;
#140441=DIRECTION ( 'NONE',  ( 0.000000000000000000, -1.000000000000000000, 0.000000000000000000 ) ) ;
#140442=VECTOR ( 'NONE', #124683, 1000.000000000000000 ) ;
#140485=ORIENTED_EDGE ( 'NONE', *, *, #113401, .T. ) ;
#140488=DIRECTION ( 'NONE',  ( 1.734723475976806848E-16, -1.000000000000000000, 0.000000000000000000 ) ) ;
#140506=VECTOR ( 'NONE', #121983, 999.9999999999998863 ) ;
#140563=DIRECTION ( 'NONE',  ( -1.000000000000000000, -1.224606353822377258E-16, -0.000000000000000000 ) ) ;
#140572=CARTESIAN_POINT ( 'NONE',  ( 1.516262732464673579, -0.4000000000000004108, 2.467792535850613866 ) ) ;
#140586=CARTESIAN_POINT ( 'NONE',  ( 18.79653912142945060, -2.499999999999996447, 0.000000000000000000 ) ) ;
#140599=CARTESIAN_POINT ( 'NONE',  ( 12.51280225271498736, 3.061616997868383634E-16, -2.500000000000000444 ) ) ;
#140611=ORIENTED_EDGE ( 'NONE', *, *, #51443, .F. ) ;
#140635=ORIENTED_EDGE ( 'NONE', *, *, #18951, .T. ) ;
#140655=EDGE_LOOP ( 'NONE', ( #140611, #9048, #112677, #57406, #43682, #64207 ) ) ;
#140662=EDGE_CURVE ( 'NONE', #47408, #87797, #125180, .T. ) ;
#140666=FACE_OUTER_BOUND ( 'NONE', #143002, .T. ) ;
#140681=AXIS2_PLACEMENT_3D ( 'NONE', #39454, #72829, #73501 ) ;
#140685=DIRECTION ( 'NONE',  ( -1.000000000000000000, -1.224606353822377258E-16, -0.000000000000000000 ) ) ;
#140686=DIRECTION ( 'NONE',  ( 0.000000000000000000, 1.000000000000000000, 0.000000000000000000 ) ) ;
#140689=DIRECTION ( 'NONE',  ( 1.734723475976806848E-16, -1.000000000000000000, 0.000000000000000000 ) ) ;
#140740=ORIENTED_EDGE ( 'NONE', *, *, #97366, .F. ) ;
#140757=ORIENTED_EDGE ( 'NONE', *, *, #52666, .F. ) ;
#140763=EDGE_LOOP ( 'NONE', ( #79316, #24751, #76748, #30368, #53718 ) ) ;
#140766=DIRECTION ( 'NONE',  ( 0.5735764363510444941, 0.8191520442889929088, 0.000000000000000000 ) ) ;
#140835=DIRECTION ( 'NONE',  ( -1.000000000000000000, -1.224606353822377258E-16, -0.000000000000000000 ) ) ;
#140853=ORIENTED_EDGE ( 'NONE', *, *, #87896, .T. ) ;
#140859=DIRECTION ( 'NONE',  ( 1.301042606982605074E-16, -1.000000000000000000, 0.000000000000000000 ) ) ;
#140868=LINE ( 'NONE', #118408, #106344 ) ;
#140873=EDGE_CURVE ( 'NONE', #90362, #5701, #85417, .T. ) ;
#140889=VERTEX_POINT ( 'NONE', #86879 ) ;
#140903=VERTEX_POINT ( 'NONE', #98454 ) ;
#140914=DIRECTION ( 'NONE',  ( -1.000000000000000000, -1.224606353822377258E-16, -0.000000000000000000 ) ) ;
#141001=EDGE_CURVE ( 'NONE', #77315, #86117, #111295, .T. ) ;
#141041=CIRCLE ( 'NONE', #64685, 2.500000000000000444 ) ;
#141059=EDGE_CURVE ( 'NONE', #11920, #56350, #102754, .T. ) ;
#141067=DIRECTION ( 'NONE',  ( -1.000000000000000000, -1.224606353822377258E-16, -0.000000000000000000 ) ) ;
#141102=ORIENTED_EDGE ( 'NONE', *, *, #133199, .F. ) ;
#141108=CONICAL_SURFACE ( 'NONE', #6756, 2.055000000000000604, 0.9599310885968764806 ) ;
#141131=ADVANCED_FACE ( 'NONE', ( #93293 ), #23326, .T. ) ;
#141154=ORIENTED_EDGE ( 'NONE', *, *, #66104, .T. ) ;
#141182=EDGE_CURVE ( 'NONE', #93303, #132555, #141429, .T. ) ;
#141189=AXIS2_PLACEMENT_3D ( 'NONE', #136345, #25433, #37036 ) ;
#141248=ORIENTED_EDGE ( 'NONE', *, *, #131201, .T. ) ;
#141287=AXIS2_PLACEMENT_3D ( 'NONE', #58254, #938, #143064 ) ;
#141304=CARTESIAN_POINT ( 'NONE',  ( 12.35051985313232237, 0.000000000000000000, 2.500000000000000444 ) ) ;
#141333=ORIENTED_EDGE ( 'NONE', *, *, #121336, .T. ) ;
#141336=FACE_OUTER_BOUND ( 'NONE', #50864, .T. ) ;
#141344=VERTEX_POINT ( 'NONE', #8379 ) ;
#141409=EDGE_LOOP ( 'NONE', ( #55017, #128146, #36477, #69810, #20038, #80101 ) ) ;
#141418=AXIS2_PLACEMENT_3D ( 'NONE', #132749, #33439, #99341 ) ;
#141429=CIRCLE ( 'NONE', #95154, 2.500000000000000444 ) ;
#141455=DIRECTION ( 'NONE',  ( -1.000000000000000000, -1.224606353822377258E-16, -0.000000000000000000 ) ) ;
#141461=DIRECTION ( 'NONE',  ( -0.5735764363510499342, -0.8191520442889891340, 0.000000000000000000 ) ) ;
#141465=VERTEX_POINT ( 'NONE', #89547 ) ;
#141495=EDGE_CURVE ( 'NONE', #135742, #128359, #69990, .T. ) ;
#141573=FACE_OUTER_BOUND ( 'NONE', #72501, .T. ) ;
#141578=CARTESIAN_POINT ( 'NONE',  ( 19.10813147593277250, 4.202752102959690472E-16, 0.000000000000000000 ) ) ;
#141606=VECTOR ( 'NONE', #27133, 999.9999999999998863 ) ;
#141640=FACE_OUTER_BOUND ( 'NONE', #55193, .T. ) ;
#141645=LINE ( 'NONE', #85812, #42261 ) ;
#141658=DIRECTION ( 'NONE',  ( 0.000000000000000000, 0.000000000000000000, 1.000000000000000000 ) ) ;
#141659=ORIENTED_EDGE ( 'NONE', *, *, #39277, .F. ) ;
#141685=AXIS2_PLACEMENT_3D ( 'NONE', #20902, #44873, #54995 ) ;
#141689=EDGE_CURVE ( 'NONE', #59344, #57055, #20527, .T. ) ;
#141715=CARTESIAN_POINT ( 'NONE',  ( 10.15640092694706453, 3.821174125832445049E-16, 0.000000000000000000 ) ) ;
#141721=AXIS2_PLACEMENT_3D ( 'NONE', #43140, #300, #100372 ) ;
#141729=AXIS2_PLACEMENT_3D ( 'NONE', #43292, #10626, #21532 ) ;
#141732=CIRCLE ( 'NONE', #67663, 2.500000000000000444 ) ;
#141746=DIRECTION ( 'NONE',  ( 0.000000000000000000, -1.301042606982605074E-16, 1.000000000000000000 ) ) ;
#141754=DIRECTION ( 'NONE',  ( -1.000000000000000000, -1.224606353822377258E-16, -0.000000000000000000 ) ) ;
#141764=DIRECTION ( 'NONE',  ( -1.000000000000000000, -1.224606353822377258E-16, -0.000000000000000000 ) ) ;
#141791=DIRECTION ( 'NONE',  ( 0.000000000000000000, -1.000000000000000000, 0.000000000000000000 ) ) ;
#141803=AXIS2_PLACEMENT_3D ( 'NONE', #34487, #69270, #68567 ) ;
#141811=CIRCLE ( 'NONE', #25995, 2.500000000000000444 ) ;
#141817=DIRECTION ( 'NONE',  ( -0.5735764363510499342, -0.8191520442889891340, 0.000000000000000000 ) ) ;
#141821=DIRECTION ( 'NONE',  ( -1.000000000000000000, -1.224606353822377258E-16, -0.000000000000000000 ) ) ;
#141832=CYLINDRICAL_SURFACE ( 'NONE', #8622, 2.500000000000000444 ) ;
#141867=EDGE_LOOP ( 'NONE', ( #89032, #111973, #15063, #87540, #16715, #113849 ) ) ;
#141880=VECTOR ( 'NONE', #139519, 999.9999999999998863 ) ;
#141894=VERTEX_POINT ( 'NONE', #138614 ) ;
#141895=VERTEX_POINT ( 'NONE', #50178 ) ;
#141908=DIRECTION ( 'NONE',  ( 0.000000000000000000, -1.000000000000000000, 0.000000000000000000 ) ) ;
#141910=ADVANCED_FACE ( 'NONE', ( #105255 ), #108887, .T. ) ;
#141918=AXIS2_PLACEMENT_3D ( 'NONE', #77480, #75327, #121648 ) ;
#141923=DIRECTION ( 'NONE',  ( 0.5735764363510444941, 0.8191520442889929088, 0.000000000000000000 ) ) ;
#141930=DIRECTION ( 'NONE',  ( 0.5735764363510444941, 0.8191520442889929088, 0.000000000000000000 ) ) ;
#141959=EDGE_CURVE ( 'NONE', #1859, #3259, #92953, .T. ) ;
#141974=CARTESIAN_POINT ( 'NONE',  ( 0.2569208697893815008, -0.3999999999999998002, -2.015694669338588429 ) ) ;
#142004=CIRCLE ( 'NONE', #130406, 2.500000000000000444 ) ;
#142022=LINE ( 'NONE', #64434, #104653 ) ;
#142028=CARTESIAN_POINT ( 'NONE',  ( 0.000000000000000000, 0.000000000000000000, 0.000000000000000000 ) ) ;
#142031=ADVANCED_FACE ( 'NONE', ( #129866 ), #53346, .T. ) ;
#142042=ADVANCED_FACE ( 'NONE', ( #8058 ), #27894, .T. ) ;
#142044=VERTEX_POINT ( 'NONE', #31281 ) ;
#142050=FACE_OUTER_BOUND ( 'NONE', #4179, .T. ) ;
#142053=CARTESIAN_POINT ( 'NONE',  ( 21.46453280170069888, 4.202752102959690472E-16, 0.000000000000000000 ) ) ;
#142100=LINE ( 'NONE', #55803, #106097 ) ;
#142124=EDGE_CURVE ( 'NONE', #121849, #62751, #120468, .T. ) ;
#142132=ADVANCED_FACE ( 'NONE', ( #135425 ), #90469, .T. ) ;
#142138=DIRECTION ( 'NONE',  ( -1.000000000000000000, -1.224606353822377258E-16, -0.000000000000000000 ) ) ;
#142155=CARTESIAN_POINT ( 'NONE',  ( 15.18079593298623564, 4.202752102959690472E-16, 0.000000000000000000 ) ) ;
#142158=DIRECTION ( 'NONE',  ( 1.734723475976806848E-16, -1.000000000000000000, 0.000000000000000000 ) ) ;
#142176=ORIENTED_EDGE ( 'NONE', *, *, #8206, .F. ) ;
#142178=DIRECTION ( 'NONE',  ( -1.000000000000000000, -1.224606353822377258E-16, -0.000000000000000000 ) ) ;
#142180=CONICAL_SURFACE ( 'NONE', #61184, 2.055000000000000604, 0.9599310885968764806 ) ;
#142252=VERTEX_POINT ( 'NONE', #143159 ) ;
#142340=CARTESIAN_POINT ( 'NONE',  ( 13.92145407031093818, 3.061616997868383634E-16, -2.500000000000000444 ) ) ;
#142357=CARTESIAN_POINT ( 'NONE',  ( 0.000000000000000000, 0.000000000000000000, 0.000000000000000000 ) ) ;
#142377=DIRECTION ( 'NONE',  ( 1.734723475976806848E-16, -1.000000000000000000, 0.000000000000000000 ) ) ;
#142522=ORIENTED_EDGE ( 'NONE', *, *, #5464, .T. ) ;
#142524=ADVANCED_FACE ( 'NONE', ( #108776 ), #39614, .T. ) ;
#142532=DIRECTION ( 'NONE',  ( -1.000000000000000000, -1.224606353822377258E-16, -0.000000000000000000 ) ) ;
#142560=DIRECTION ( 'NONE',  ( 1.000000000000000000, 1.224606353822377258E-16, 0.000000000000000000 ) ) ;
#142562=CARTESIAN_POINT ( 'NONE',  ( 14.86920357848291196, -2.499999999999999112, 0.000000000000000000 ) ) ;
#142566=ORIENTED_EDGE ( 'NONE', *, *, #17954, .F. ) ;
#142595=EDGE_CURVE ( 'NONE', #64781, #137282, #62793, .T. ) ;
#142602=CARTESIAN_POINT ( 'NONE',  ( 14.86920357848291196, 3.821174125832445049E-16, 0.000000000000000000 ) ) ;
#142604=EDGE_CURVE ( 'NONE', #112363, #12102, #39711, .T. ) ;
#142617=ORIENTED_EDGE ( 'NONE', *, *, #5371, .F. ) ;
#142651=ORIENTED_EDGE ( 'NONE', *, *, #48723, .F. ) ;
#142729=ADVANCED_FACE ( 'NONE', ( #72496 ), #138423, .T. ) ;
#142779=VERTEX_POINT ( 'NONE', #85439 ) ;
#142828=DIRECTION ( 'NONE',  ( -1.000000000000000000, -0.000000000000000000, -0.000000000000000000 ) ) ;
#142865=CIRCLE ( 'NONE', #54817, 2.055000000000000604 ) ;
#142891=VECTOR ( 'NONE', #4117, 1000.000000000000000 ) ;
#142900=EDGE_LOOP ( 'NONE', ( #56481, #101577, #69617, #68980, #27276 ) ) ;
#142903=DIRECTION ( 'NONE',  ( 1.000000000000000000, 1.224606353822377258E-16, 0.000000000000000000 ) ) ;
#142929=LINE ( 'NONE', #32027, #96718 ) ;
#142971=CARTESIAN_POINT ( 'NONE',  ( 10.77958563595370833, 4.584330080086930965E-16, 0.000000000000000000 ) ) ;
#143002=EDGE_LOOP ( 'NONE', ( #122985, #49035, #51001, #124993, #78472 ) ) ;
#143011=CARTESIAN_POINT ( 'NONE',  ( 0.2569208697893813897, 0.3999999999999995781, 2.015694669338588429 ) ) ;
#143019=DIRECTION ( 'NONE',  ( -1.000000000000000000, -0.000000000000000000, -0.000000000000000000 ) ) ;
#143064=DIRECTION ( 'NONE',  ( 0.000000000000000000, 1.000000000000000000, 0.000000000000000000 ) ) ;
#143117=EDGE_CURVE ( 'NONE', #5092, #60214, #40390, .T. ) ;
#143129=DIRECTION ( 'NONE',  ( -1.000000000000000000, -1.224606353822377258E-16, -0.000000000000000000 ) ) ;
#143159=CARTESIAN_POINT ( 'NONE',  ( 0.5685132242927009028, 2.500000000000000888, 0.000000000000000000 ) ) ;
#143178=ORIENTED_EDGE ( 'NONE', *, *, #110594, .T. ) ;
#143207=ADVANCED_FACE ( 'NONE', ( #28790 ), #76874, .T. ) ;
#143292=DIRECTION ( 'NONE',  ( -1.000000000000000000, -1.224606353822377258E-16, -0.000000000000000000 ) ) ;
#143342=EDGE_LOOP ( 'NONE', ( #74590, #83044, #88892, #85758, #117417, #131353 ) ) ;
#143347=EDGE_CURVE ( 'NONE', #36014, #139082, #109222, .T. ) ;
#143385=CARTESIAN_POINT ( 'NONE',  ( -12.69999999999998153, 3.061616997868383634E-16, -2.500000000000000444 ) ) ;
#143388=DIRECTION ( 'NONE',  ( 0.000000000000000000, -1.000000000000000000, 0.000000000000000000 ) ) ;
#143418=ORIENTED_EDGE ( 'NONE', *, *, #31670, .T. ) ;
#143434=FACE_OUTER_BOUND ( 'NONE', #116020, .T. ) ;
#143498=DIRECTION ( 'NONE',  ( 0.000000000000000000, -1.000000000000000000, 0.000000000000000000 ) ) ;
#143511=DIRECTION ( 'NONE',  ( -1.000000000000000000, -1.224606353822377258E-16, -0.000000000000000000 ) ) ;
#143514=CIRCLE ( 'NONE', #39334, 2.500000000000000444 ) ;
ENDSEC;
END-ISO-10303-21;
